ISO-10303-21;
HEADER;
/* Generated by software containing ST-Developer
 * from STEP Tools, Inc. (www.steptools.com) 
 */

FILE_DESCRIPTION(
/* description */ ('Independent compact industrial fixture table, bolted aluminum worktop
 on connected adjustable support base. Whole-mm nominal dimensions. No
 load rating assigned.'),
/* implementation_level */ '2;1');

FILE_NAME(
/* name */ 'Socket head cap screw M6x50.step',
/* time_stamp */ '2026-11-07T17:47:58-08:00',
/* author */ (''),
/* organization */ (''),
/* preprocessor_version */ 'ST-DEVELOPER v20.2',
/* originating_system */ 'Autodesk Translation Framework v15.17.0.0',
/* authorisation */ '');

FILE_SCHEMA (('AUTOMOTIVE_DESIGN { 1 0 10303 214 3 1 1 }'));
ENDSEC;

DATA;
#10=MECHANICAL_DESIGN_GEOMETRIC_PRESENTATION_REPRESENTATION('',(#2266),#97475);
#333=CONICAL_SURFACE('',#23426,2.5,0.78539816339745);
#374=B_SPLINE_SURFACE_WITH_KNOTS('',3,3,((#94542,#94543,#94544,#94545,#94546,
#94547,#94548,#94549,#94550,#94551,#94552,#94553,#94554,#94555,#94556,#94557,
#94558,#94559,#94560,#94561,#94562,#94563,#94564,#94565,#94566,#94567,#94568,
#94569,#94570,#94571,#94572,#94573,#94574,#94575,#94576,#94577,#94578,#94579,
#94580,#94581,#94582,#94583,#94584,#94585,#94586,#94587,#94588,#94589,#94590,
#94591,#94592,#94593,#94594,#94595,#94596,#94597,#94598,#94599,#94600,#94601,
#94602,#94603,#94604,#94605,#94606,#94607,#94608,#94609,#94610,#94611,#94612,
#94613,#94614,#94615,#94616,#94617,#94618,#94619,#94620,#94621,#94622,#94623,
#94624,#94625,#94626,#94627,#94628,#94629,#94630,#94631,#94632,#94633,#94634,
#94635,#94636,#94637,#94638,#94639,#94640,#94641,#94642,#94643,#94644,#94645,
#94646,#94647,#94648,#94649,#94650,#94651,#94652,#94653,#94654,#94655,#94656,
#94657,#94658,#94659,#94660,#94661,#94662,#94663,#94664,#94665,#94666,#94667,
#94668,#94669,#94670,#94671,#94672,#94673,#94674,#94675,#94676,#94677,#94678,
#94679,#94680,#94681,#94682,#94683,#94684,#94685,#94686,#94687,#94688,#94689,
#94690,#94691,#94692,#94693,#94694,#94695,#94696,#94697,#94698,#94699,#94700,
#94701,#94702,#94703,#94704,#94705,#94706,#94707,#94708,#94709,#94710,#94711,
#94712,#94713,#94714,#94715,#94716,#94717,#94718,#94719,#94720,#94721,#94722,
#94723,#94724,#94725,#94726,#94727,#94728,#94729,#94730,#94731,#94732,#94733,
#94734,#94735,#94736,#94737,#94738,#94739,#94740,#94741,#94742,#94743,#94744,
#94745,#94746,#94747,#94748,#94749,#94750,#94751,#94752,#94753,#94754,#94755,
#94756,#94757,#94758,#94759,#94760,#94761,#94762,#94763,#94764,#94765,#94766,
#94767,#94768,#94769,#94770,#94771,#94772,#94773,#94774,#94775,#94776,#94777,
#94778,#94779,#94780,#94781,#94782,#94783,#94784,#94785,#94786,#94787,#94788,
#94789,#94790,#94791,#94792,#94793,#94794,#94795,#94796,#94797,#94798,#94799,
#94800,#94801,#94802,#94803,#94804,#94805,#94806,#94807,#94808,#94809,#94810,
#94811,#94812,#94813,#94814,#94815,#94816,#94817,#94818,#94819,#94820,#94821,
#94822,#94823,#94824,#94825,#94826,#94827,#94828,#94829,#94830,#94831,#94832,
#94833,#94834,#94835,#94836,#94837,#94838,#94839,#94840,#94841,#94842,#94843,
#94844,#94845,#94846,#94847,#94848,#94849,#94850,#94851,#94852,#94853,#94854,
#94855,#94856),(#94857,#94858,#94859,#94860,#94861,#94862,#94863,#94864,
#94865,#94866,#94867,#94868,#94869,#94870,#94871,#94872,#94873,#94874,#94875,
#94876,#94877,#94878,#94879,#94880,#94881,#94882,#94883,#94884,#94885,#94886,
#94887,#94888,#94889,#94890,#94891,#94892,#94893,#94894,#94895,#94896,#94897,
#94898,#94899,#94900,#94901,#94902,#94903,#94904,#94905,#94906,#94907,#94908,
#94909,#94910,#94911,#94912,#94913,#94914,#94915,#94916,#94917,#94918,#94919,
#94920,#94921,#94922,#94923,#94924,#94925,#94926,#94927,#94928,#94929,#94930,
#94931,#94932,#94933,#94934,#94935,#94936,#94937,#94938,#94939,#94940,#94941,
#94942,#94943,#94944,#94945,#94946,#94947,#94948,#94949,#94950,#94951,#94952,
#94953,#94954,#94955,#94956,#94957,#94958,#94959,#94960,#94961,#94962,#94963,
#94964,#94965,#94966,#94967,#94968,#94969,#94970,#94971,#94972,#94973,#94974,
#94975,#94976,#94977,#94978,#94979,#94980,#94981,#94982,#94983,#94984,#94985,
#94986,#94987,#94988,#94989,#94990,#94991,#94992,#94993,#94994,#94995,#94996,
#94997,#94998,#94999,#95000,#95001,#95002,#95003,#95004,#95005,#95006,#95007,
#95008,#95009,#95010,#95011,#95012,#95013,#95014,#95015,#95016,#95017,#95018,
#95019,#95020,#95021,#95022,#95023,#95024,#95025,#95026,#95027,#95028,#95029,
#95030,#95031,#95032,#95033,#95034,#95035,#95036,#95037,#95038,#95039,#95040,
#95041,#95042,#95043,#95044,#95045,#95046,#95047,#95048,#95049,#95050,#95051,
#95052,#95053,#95054,#95055,#95056,#95057,#95058,#95059,#95060,#95061,#95062,
#95063,#95064,#95065,#95066,#95067,#95068,#95069,#95070,#95071,#95072,#95073,
#95074,#95075,#95076,#95077,#95078,#95079,#95080,#95081,#95082,#95083,#95084,
#95085,#95086,#95087,#95088,#95089,#95090,#95091,#95092,#95093,#95094,#95095,
#95096,#95097,#95098,#95099,#95100,#95101,#95102,#95103,#95104,#95105,#95106,
#95107,#95108,#95109,#95110,#95111,#95112,#95113,#95114,#95115,#95116,#95117,
#95118,#95119,#95120,#95121,#95122,#95123,#95124,#95125,#95126,#95127,#95128,
#95129,#95130,#95131,#95132,#95133,#95134,#95135,#95136,#95137,#95138,#95139,
#95140,#95141,#95142,#95143,#95144,#95145,#95146,#95147,#95148,#95149,#95150,
#95151,#95152,#95153,#95154,#95155,#95156,#95157,#95158,#95159,#95160,#95161,
#95162,#95163,#95164,#95165,#95166,#95167,#95168,#95169,#95170,#95171),
(#95172,#95173,#95174,#95175,#95176,#95177,#95178,#95179,#95180,#95181,
#95182,#95183,#95184,#95185,#95186,#95187,#95188,#95189,#95190,#95191,#95192,
#95193,#95194,#95195,#95196,#95197,#95198,#95199,#95200,#95201,#95202,#95203,
#95204,#95205,#95206,#95207,#95208,#95209,#95210,#95211,#95212,#95213,#95214,
#95215,#95216,#95217,#95218,#95219,#95220,#95221,#95222,#95223,#95224,#95225,
#95226,#95227,#95228,#95229,#95230,#95231,#95232,#95233,#95234,#95235,#95236,
#95237,#95238,#95239,#95240,#95241,#95242,#95243,#95244,#95245,#95246,#95247,
#95248,#95249,#95250,#95251,#95252,#95253,#95254,#95255,#95256,#95257,#95258,
#95259,#95260,#95261,#95262,#95263,#95264,#95265,#95266,#95267,#95268,#95269,
#95270,#95271,#95272,#95273,#95274,#95275,#95276,#95277,#95278,#95279,#95280,
#95281,#95282,#95283,#95284,#95285,#95286,#95287,#95288,#95289,#95290,#95291,
#95292,#95293,#95294,#95295,#95296,#95297,#95298,#95299,#95300,#95301,#95302,
#95303,#95304,#95305,#95306,#95307,#95308,#95309,#95310,#95311,#95312,#95313,
#95314,#95315,#95316,#95317,#95318,#95319,#95320,#95321,#95322,#95323,#95324,
#95325,#95326,#95327,#95328,#95329,#95330,#95331,#95332,#95333,#95334,#95335,
#95336,#95337,#95338,#95339,#95340,#95341,#95342,#95343,#95344,#95345,#95346,
#95347,#95348,#95349,#95350,#95351,#95352,#95353,#95354,#95355,#95356,#95357,
#95358,#95359,#95360,#95361,#95362,#95363,#95364,#95365,#95366,#95367,#95368,
#95369,#95370,#95371,#95372,#95373,#95374,#95375,#95376,#95377,#95378,#95379,
#95380,#95381,#95382,#95383,#95384,#95385,#95386,#95387,#95388,#95389,#95390,
#95391,#95392,#95393,#95394,#95395,#95396,#95397,#95398,#95399,#95400,#95401,
#95402,#95403,#95404,#95405,#95406,#95407,#95408,#95409,#95410,#95411,#95412,
#95413,#95414,#95415,#95416,#95417,#95418,#95419,#95420,#95421,#95422,#95423,
#95424,#95425,#95426,#95427,#95428,#95429,#95430,#95431,#95432,#95433,#95434,
#95435,#95436,#95437,#95438,#95439,#95440,#95441,#95442,#95443,#95444,#95445,
#95446,#95447,#95448,#95449,#95450,#95451,#95452,#95453,#95454,#95455,#95456,
#95457,#95458,#95459,#95460,#95461,#95462,#95463,#95464,#95465,#95466,#95467,
#95468,#95469,#95470,#95471,#95472,#95473,#95474,#95475,#95476,#95477,#95478,
#95479,#95480,#95481,#95482,#95483,#95484,#95485,#95486),(#95487,#95488,
#95489,#95490,#95491,#95492,#95493,#95494,#95495,#95496,#95497,#95498,#95499,
#95500,#95501,#95502,#95503,#95504,#95505,#95506,#95507,#95508,#95509,#95510,
#95511,#95512,#95513,#95514,#95515,#95516,#95517,#95518,#95519,#95520,#95521,
#95522,#95523,#95524,#95525,#95526,#95527,#95528,#95529,#95530,#95531,#95532,
#95533,#95534,#95535,#95536,#95537,#95538,#95539,#95540,#95541,#95542,#95543,
#95544,#95545,#95546,#95547,#95548,#95549,#95550,#95551,#95552,#95553,#95554,
#95555,#95556,#95557,#95558,#95559,#95560,#95561,#95562,#95563,#95564,#95565,
#95566,#95567,#95568,#95569,#95570,#95571,#95572,#95573,#95574,#95575,#95576,
#95577,#95578,#95579,#95580,#95581,#95582,#95583,#95584,#95585,#95586,#95587,
#95588,#95589,#95590,#95591,#95592,#95593,#95594,#95595,#95596,#95597,#95598,
#95599,#95600,#95601,#95602,#95603,#95604,#95605,#95606,#95607,#95608,#95609,
#95610,#95611,#95612,#95613,#95614,#95615,#95616,#95617,#95618,#95619,#95620,
#95621,#95622,#95623,#95624,#95625,#95626,#95627,#95628,#95629,#95630,#95631,
#95632,#95633,#95634,#95635,#95636,#95637,#95638,#95639,#95640,#95641,#95642,
#95643,#95644,#95645,#95646,#95647,#95648,#95649,#95650,#95651,#95652,#95653,
#95654,#95655,#95656,#95657,#95658,#95659,#95660,#95661,#95662,#95663,#95664,
#95665,#95666,#95667,#95668,#95669,#95670,#95671,#95672,#95673,#95674,#95675,
#95676,#95677,#95678,#95679,#95680,#95681,#95682,#95683,#95684,#95685,#95686,
#95687,#95688,#95689,#95690,#95691,#95692,#95693,#95694,#95695,#95696,#95697,
#95698,#95699,#95700,#95701,#95702,#95703,#95704,#95705,#95706,#95707,#95708,
#95709,#95710,#95711,#95712,#95713,#95714,#95715,#95716,#95717,#95718,#95719,
#95720,#95721,#95722,#95723,#95724,#95725,#95726,#95727,#95728,#95729,#95730,
#95731,#95732,#95733,#95734,#95735,#95736,#95737,#95738,#95739,#95740,#95741,
#95742,#95743,#95744,#95745,#95746,#95747,#95748,#95749,#95750,#95751,#95752,
#95753,#95754,#95755,#95756,#95757,#95758,#95759,#95760,#95761,#95762,#95763,
#95764,#95765,#95766,#95767,#95768,#95769,#95770,#95771,#95772,#95773,#95774,
#95775,#95776,#95777,#95778,#95779,#95780,#95781,#95782,#95783,#95784,#95785,
#95786,#95787,#95788,#95789,#95790,#95791,#95792,#95793,#95794,#95795,#95796,
#95797,#95798,#95799,#95800,#95801)),.UNSPECIFIED.,.F.,.F.,.F.,(4,4),(4,
1,1,1,1,1,1,1,1,1,1,1,1,1,1,1,1,1,1,1,1,1,1,1,1,1,1,1,1,1,1,1,1,1,1,1,1,
1,1,1,1,1,1,1,1,1,1,1,1,1,1,1,1,1,1,1,1,1,1,1,1,1,1,1,1,1,1,1,1,1,1,1,1,
1,1,1,1,1,1,1,1,1,1,1,1,1,1,1,1,1,1,1,1,1,1,1,1,1,1,1,1,1,1,1,1,1,1,1,1,
1,1,1,1,1,1,1,1,1,1,1,1,1,1,1,1,1,1,1,1,1,1,1,1,1,1,1,1,1,1,1,1,1,1,1,1,
1,1,1,1,1,1,1,1,1,1,1,1,1,1,1,1,1,1,1,1,1,1,1,1,1,1,1,1,1,1,1,1,1,1,1,1,
1,1,1,1,1,1,1,1,1,1,1,1,1,1,1,1,1,1,1,1,1,1,1,1,1,1,1,1,1,1,1,1,1,1,1,1,
1,1,1,1,1,1,1,1,1,1,1,1,1,1,1,1,1,1,1,1,1,1,1,1,1,1,1,1,1,1,1,1,1,1,1,1,
1,1,1,1,1,1,1,1,1,1,1,1,1,1,1,1,1,1,1,1,1,1,1,1,1,1,1,1,1,1,1,1,1,1,1,1,
1,1,1,1,1,1,1,1,1,1,1,1,1,1,1,1,1,1,1,1,1,1,1,4),(0.,0.0658467982010768),
(11.6150328478189,12.614467114553,13.6139013812871,14.6133356480212,15.6127699147553,
16.6122041814894,17.6116384482234,18.6110727149575,19.6105069816916,20.6099412484257,
21.6093755151598,22.6088097818939,23.608244048628,24.6076783153621,25.6071125820962,
26.6065468488302,27.6059811155643,28.6054153822984,29.6048496490325,30.6042839157666,
31.6037181825007,32.6031524492348,33.6025867159689,34.6020209827029,35.601455249437,
36.6008895161711,37.6003237829052,38.5997580496393,39.5991923163734,40.5986265831075,
41.5980608498416,42.5974951165757,43.5969293833097,44.5963636500438,45.5957979167779,
46.595232183512,47.5946664502461,48.5941007169802,49.5935349837143,50.5929692504484,
51.5924035171824,52.5918377839165,53.5912720506506,54.5907063173847,55.5901405841188,
56.5895748508529,57.589009117587,58.5884433843211,59.5878776510552,60.5873119177892,
61.5867461845233,62.5861804512574,63.5856147179915,64.5850489847256,65.5844832514597,
66.5839175181938,67.5833517849279,68.582786051662,69.582220318396,70.5816545851301,
71.5810888518642,72.5805231185983,73.5799573853324,74.5793916520665,75.5788259188006,
76.5782601855347,77.5776944522688,78.5771287190028,79.5765629857369,80.575997252471,
81.5754315192051,82.5748657859392,83.5743000526733,84.5737343194074,85.5731685861415,
86.5726028528755,87.5720371196096,88.5714713863437,89.5709056530778,90.5703399198119,
91.569774186546,92.5692084532801,93.5686427200142,94.5680769867483,95.5675112534823,
96.5669455202164,97.5663797869505,98.5658140536846,99.5652483204187,100.564682587153,
101.564116853887,102.563551120621,103.562985387355,104.562419654089,105.561853920823,
106.561288187557,107.560722454291,108.560156721025,109.55959098776,110.559025254494,
111.558459521228,112.557893787962,113.557328054696,114.55676232143,115.556196588164,
116.555630854898,117.555065121632,118.554499388366,119.5539336551,120.553367921835,
121.552802188569,122.552236455303,123.551670722037,124.551104988771,125.550539255505,
126.549973522239,127.549407788973,128.548842055707,129.548276322441,130.547710589175,
131.54714485591,132.546579122644,133.546013389378,134.545447656112,135.544881922846,
136.54431618958,137.543750456314,138.543184723048,139.542618989782,140.542053256516,
141.54148752325,142.540921789984,143.540356056719,144.539790323453,145.539224590187,
146.538658856921,147.538093123655,148.537527390389,149.536961657123,150.536395923857,
151.535830190591,152.535264457325,153.534698724059,154.534132990794,155.533567257528,
156.533001524262,157.532435790996,158.53187005773,159.531304324464,160.530738591198,
161.530172857932,162.529607124666,163.5290413914,164.528475658134,165.527909924869,
166.527344191603,167.526778458337,168.526212725071,169.525646991805,170.525081258539,
171.524515525273,172.523949792007,173.523384058741,174.522818325475,175.522252592209,
176.521686858943,177.521121125678,178.520555392412,179.519989659146,180.51942392588,
181.518858192614,182.518292459348,183.517726726082,184.517160992816,185.51659525955,
186.516029526284,187.515463793018,188.514898059753,189.514332326487,190.513766593221,
191.513200859955,192.512635126689,193.512069393423,194.511503660157,195.510937926891,
196.510372193625,197.509806460359,198.509240727093,199.508674993828,200.508109260562,
201.507543527296,202.50697779403,203.506412060764,204.505846327498,205.505280594232,
206.504714860966,207.5041491277,208.503583394434,209.503017661168,210.502451927902,
211.501886194637,212.501320461371,213.500754728105,214.500188994839,215.499623261573,
216.499057528307,217.498491795041,218.497926061775,219.497360328509,220.496794595243,
221.496228861977,222.495663128712,223.495097395446,224.49453166218,225.493965928914,
226.493400195648,227.492834462382,228.492268729116,229.49170299585,230.491137262584,
231.490571529318,232.490005796052,233.489440062787,234.488874329521,235.488308596255,
236.487742862989,237.487177129723,238.486611396457,239.486045663191,240.485479929925,
241.484914196659,242.484348463393,243.483782730127,244.483216996862,245.482651263596,
246.48208553033,247.481519797064,248.480954063798,249.480388330532,250.479822597266,
251.479256864,252.478691130734,253.478125397468,254.477559664202,255.476993930936,
256.476428197671,257.475862464405,258.475296731139,259.474730997873,260.474165264607,
261.473599531341,262.473033798075,263.472468064809,264.471902331543,265.471336598277,
266.470770865011,267.470205131746,268.46963939848,269.469073665214,270.468507931948,
271.467942198682,272.467376465416,273.46681073215,274.466244998884,275.465679265618,
276.465113532352,277.464547799086,278.46398206582,279.463416332555,280.462850599289,
281.462284866023,282.461719132757,283.461153399491,284.460587666225,285.460021932959,
286.459456199693,287.458890466427,288.458324733161,289.457758999895,290.45719326663,
291.456627533364,292.456061800098,293.455496066832,294.454930333566,295.4543646003,
296.453798867034,297.453233133768,298.452667400502,299.452101667236,300.45153593397,
301.450970200704,302.450404467439,303.449838734173,304.449273000907,305.448707267641,
306.448141534375,307.447575801109,308.447010067843,309.446444334577,310.445878601311,
311.445312868045,312.444747134779,313.444181401514,314.443615668248,315.443049934982,
316.442484201716,317.44191846845,318.441352735184,319.440787001918,320.440221268652,
321.439655535386,322.43908980212,323.438524068854),.UNSPECIFIED.);
#375=B_SPLINE_SURFACE_WITH_KNOTS('',3,3,((#95936,#95937,#95938,#95939,#95940,
#95941,#95942,#95943,#95944,#95945,#95946,#95947,#95948,#95949,#95950,#95951,
#95952,#95953,#95954,#95955,#95956,#95957,#95958,#95959,#95960,#95961,#95962,
#95963,#95964,#95965,#95966,#95967,#95968,#95969,#95970,#95971,#95972,#95973,
#95974,#95975,#95976,#95977,#95978,#95979,#95980,#95981,#95982,#95983,#95984,
#95985,#95986,#95987,#95988,#95989,#95990,#95991,#95992,#95993,#95994,#95995,
#95996,#95997,#95998,#95999,#96000,#96001,#96002,#96003,#96004,#96005,#96006,
#96007,#96008,#96009,#96010,#96011,#96012,#96013,#96014,#96015,#96016,#96017,
#96018,#96019,#96020,#96021,#96022,#96023,#96024,#96025,#96026,#96027,#96028,
#96029,#96030,#96031,#96032,#96033,#96034,#96035,#96036,#96037,#96038,#96039,
#96040,#96041,#96042,#96043,#96044,#96045,#96046,#96047,#96048,#96049,#96050,
#96051,#96052,#96053,#96054,#96055,#96056,#96057,#96058,#96059,#96060,#96061,
#96062,#96063,#96064,#96065,#96066,#96067,#96068,#96069,#96070,#96071,#96072,
#96073,#96074,#96075,#96076,#96077,#96078,#96079,#96080,#96081,#96082,#96083,
#96084,#96085,#96086,#96087,#96088,#96089,#96090,#96091,#96092,#96093,#96094,
#96095,#96096,#96097,#96098,#96099,#96100,#96101,#96102,#96103,#96104,#96105,
#96106,#96107,#96108,#96109,#96110,#96111,#96112,#96113,#96114,#96115,#96116,
#96117,#96118,#96119,#96120,#96121,#96122,#96123,#96124,#96125,#96126,#96127,
#96128,#96129,#96130,#96131,#96132,#96133,#96134,#96135,#96136,#96137,#96138,
#96139,#96140,#96141,#96142,#96143,#96144,#96145,#96146,#96147,#96148,#96149,
#96150,#96151,#96152,#96153,#96154,#96155,#96156,#96157,#96158,#96159,#96160,
#96161,#96162,#96163,#96164,#96165,#96166,#96167,#96168,#96169,#96170,#96171,
#96172,#96173,#96174,#96175,#96176,#96177,#96178,#96179,#96180,#96181,#96182,
#96183,#96184,#96185,#96186,#96187,#96188,#96189,#96190,#96191,#96192,#96193,
#96194,#96195,#96196,#96197,#96198,#96199,#96200,#96201,#96202,#96203,#96204,
#96205,#96206,#96207,#96208,#96209,#96210,#96211,#96212,#96213,#96214,#96215,
#96216,#96217,#96218,#96219,#96220,#96221,#96222,#96223,#96224,#96225,#96226,
#96227,#96228,#96229,#96230,#96231,#96232,#96233,#96234,#96235,#96236,#96237,
#96238,#96239,#96240,#96241,#96242,#96243,#96244,#96245,#96246,#96247,#96248,
#96249,#96250,#96251,#96252),(#96253,#96254,#96255,#96256,#96257,#96258,
#96259,#96260,#96261,#96262,#96263,#96264,#96265,#96266,#96267,#96268,#96269,
#96270,#96271,#96272,#96273,#96274,#96275,#96276,#96277,#96278,#96279,#96280,
#96281,#96282,#96283,#96284,#96285,#96286,#96287,#96288,#96289,#96290,#96291,
#96292,#96293,#96294,#96295,#96296,#96297,#96298,#96299,#96300,#96301,#96302,
#96303,#96304,#96305,#96306,#96307,#96308,#96309,#96310,#96311,#96312,#96313,
#96314,#96315,#96316,#96317,#96318,#96319,#96320,#96321,#96322,#96323,#96324,
#96325,#96326,#96327,#96328,#96329,#96330,#96331,#96332,#96333,#96334,#96335,
#96336,#96337,#96338,#96339,#96340,#96341,#96342,#96343,#96344,#96345,#96346,
#96347,#96348,#96349,#96350,#96351,#96352,#96353,#96354,#96355,#96356,#96357,
#96358,#96359,#96360,#96361,#96362,#96363,#96364,#96365,#96366,#96367,#96368,
#96369,#96370,#96371,#96372,#96373,#96374,#96375,#96376,#96377,#96378,#96379,
#96380,#96381,#96382,#96383,#96384,#96385,#96386,#96387,#96388,#96389,#96390,
#96391,#96392,#96393,#96394,#96395,#96396,#96397,#96398,#96399,#96400,#96401,
#96402,#96403,#96404,#96405,#96406,#96407,#96408,#96409,#96410,#96411,#96412,
#96413,#96414,#96415,#96416,#96417,#96418,#96419,#96420,#96421,#96422,#96423,
#96424,#96425,#96426,#96427,#96428,#96429,#96430,#96431,#96432,#96433,#96434,
#96435,#96436,#96437,#96438,#96439,#96440,#96441,#96442,#96443,#96444,#96445,
#96446,#96447,#96448,#96449,#96450,#96451,#96452,#96453,#96454,#96455,#96456,
#96457,#96458,#96459,#96460,#96461,#96462,#96463,#96464,#96465,#96466,#96467,
#96468,#96469,#96470,#96471,#96472,#96473,#96474,#96475,#96476,#96477,#96478,
#96479,#96480,#96481,#96482,#96483,#96484,#96485,#96486,#96487,#96488,#96489,
#96490,#96491,#96492,#96493,#96494,#96495,#96496,#96497,#96498,#96499,#96500,
#96501,#96502,#96503,#96504,#96505,#96506,#96507,#96508,#96509,#96510,#96511,
#96512,#96513,#96514,#96515,#96516,#96517,#96518,#96519,#96520,#96521,#96522,
#96523,#96524,#96525,#96526,#96527,#96528,#96529,#96530,#96531,#96532,#96533,
#96534,#96535,#96536,#96537,#96538,#96539,#96540,#96541,#96542,#96543,#96544,
#96545,#96546,#96547,#96548,#96549,#96550,#96551,#96552,#96553,#96554,#96555,
#96556,#96557,#96558,#96559,#96560,#96561,#96562,#96563,#96564,#96565,#96566,
#96567,#96568,#96569),(#96570,#96571,#96572,#96573,#96574,#96575,#96576,
#96577,#96578,#96579,#96580,#96581,#96582,#96583,#96584,#96585,#96586,#96587,
#96588,#96589,#96590,#96591,#96592,#96593,#96594,#96595,#96596,#96597,#96598,
#96599,#96600,#96601,#96602,#96603,#96604,#96605,#96606,#96607,#96608,#96609,
#96610,#96611,#96612,#96613,#96614,#96615,#96616,#96617,#96618,#96619,#96620,
#96621,#96622,#96623,#96624,#96625,#96626,#96627,#96628,#96629,#96630,#96631,
#96632,#96633,#96634,#96635,#96636,#96637,#96638,#96639,#96640,#96641,#96642,
#96643,#96644,#96645,#96646,#96647,#96648,#96649,#96650,#96651,#96652,#96653,
#96654,#96655,#96656,#96657,#96658,#96659,#96660,#96661,#96662,#96663,#96664,
#96665,#96666,#96667,#96668,#96669,#96670,#96671,#96672,#96673,#96674,#96675,
#96676,#96677,#96678,#96679,#96680,#96681,#96682,#96683,#96684,#96685,#96686,
#96687,#96688,#96689,#96690,#96691,#96692,#96693,#96694,#96695,#96696,#96697,
#96698,#96699,#96700,#96701,#96702,#96703,#96704,#96705,#96706,#96707,#96708,
#96709,#96710,#96711,#96712,#96713,#96714,#96715,#96716,#96717,#96718,#96719,
#96720,#96721,#96722,#96723,#96724,#96725,#96726,#96727,#96728,#96729,#96730,
#96731,#96732,#96733,#96734,#96735,#96736,#96737,#96738,#96739,#96740,#96741,
#96742,#96743,#96744,#96745,#96746,#96747,#96748,#96749,#96750,#96751,#96752,
#96753,#96754,#96755,#96756,#96757,#96758,#96759,#96760,#96761,#96762,#96763,
#96764,#96765,#96766,#96767,#96768,#96769,#96770,#96771,#96772,#96773,#96774,
#96775,#96776,#96777,#96778,#96779,#96780,#96781,#96782,#96783,#96784,#96785,
#96786,#96787,#96788,#96789,#96790,#96791,#96792,#96793,#96794,#96795,#96796,
#96797,#96798,#96799,#96800,#96801,#96802,#96803,#96804,#96805,#96806,#96807,
#96808,#96809,#96810,#96811,#96812,#96813,#96814,#96815,#96816,#96817,#96818,
#96819,#96820,#96821,#96822,#96823,#96824,#96825,#96826,#96827,#96828,#96829,
#96830,#96831,#96832,#96833,#96834,#96835,#96836,#96837,#96838,#96839,#96840,
#96841,#96842,#96843,#96844,#96845,#96846,#96847,#96848,#96849,#96850,#96851,
#96852,#96853,#96854,#96855,#96856,#96857,#96858,#96859,#96860,#96861,#96862,
#96863,#96864,#96865,#96866,#96867,#96868,#96869,#96870,#96871,#96872,#96873,
#96874,#96875,#96876,#96877,#96878,#96879,#96880,#96881,#96882,#96883,#96884,
#96885,#96886),(#96887,#96888,#96889,#96890,#96891,#96892,#96893,#96894,
#96895,#96896,#96897,#96898,#96899,#96900,#96901,#96902,#96903,#96904,#96905,
#96906,#96907,#96908,#96909,#96910,#96911,#96912,#96913,#96914,#96915,#96916,
#96917,#96918,#96919,#96920,#96921,#96922,#96923,#96924,#96925,#96926,#96927,
#96928,#96929,#96930,#96931,#96932,#96933,#96934,#96935,#96936,#96937,#96938,
#96939,#96940,#96941,#96942,#96943,#96944,#96945,#96946,#96947,#96948,#96949,
#96950,#96951,#96952,#96953,#96954,#96955,#96956,#96957,#96958,#96959,#96960,
#96961,#96962,#96963,#96964,#96965,#96966,#96967,#96968,#96969,#96970,#96971,
#96972,#96973,#96974,#96975,#96976,#96977,#96978,#96979,#96980,#96981,#96982,
#96983,#96984,#96985,#96986,#96987,#96988,#96989,#96990,#96991,#96992,#96993,
#96994,#96995,#96996,#96997,#96998,#96999,#97000,#97001,#97002,#97003,#97004,
#97005,#97006,#97007,#97008,#97009,#97010,#97011,#97012,#97013,#97014,#97015,
#97016,#97017,#97018,#97019,#97020,#97021,#97022,#97023,#97024,#97025,#97026,
#97027,#97028,#97029,#97030,#97031,#97032,#97033,#97034,#97035,#97036,#97037,
#97038,#97039,#97040,#97041,#97042,#97043,#97044,#97045,#97046,#97047,#97048,
#97049,#97050,#97051,#97052,#97053,#97054,#97055,#97056,#97057,#97058,#97059,
#97060,#97061,#97062,#97063,#97064,#97065,#97066,#97067,#97068,#97069,#97070,
#97071,#97072,#97073,#97074,#97075,#97076,#97077,#97078,#97079,#97080,#97081,
#97082,#97083,#97084,#97085,#97086,#97087,#97088,#97089,#97090,#97091,#97092,
#97093,#97094,#97095,#97096,#97097,#97098,#97099,#97100,#97101,#97102,#97103,
#97104,#97105,#97106,#97107,#97108,#97109,#97110,#97111,#97112,#97113,#97114,
#97115,#97116,#97117,#97118,#97119,#97120,#97121,#97122,#97123,#97124,#97125,
#97126,#97127,#97128,#97129,#97130,#97131,#97132,#97133,#97134,#97135,#97136,
#97137,#97138,#97139,#97140,#97141,#97142,#97143,#97144,#97145,#97146,#97147,
#97148,#97149,#97150,#97151,#97152,#97153,#97154,#97155,#97156,#97157,#97158,
#97159,#97160,#97161,#97162,#97163,#97164,#97165,#97166,#97167,#97168,#97169,
#97170,#97171,#97172,#97173,#97174,#97175,#97176,#97177,#97178,#97179,#97180,
#97181,#97182,#97183,#97184,#97185,#97186,#97187,#97188,#97189,#97190,#97191,
#97192,#97193,#97194,#97195,#97196,#97197,#97198,#97199,#97200,#97201,#97202,
#97203)),.UNSPECIFIED.,.F.,.F.,.F.,(4,4),(4,1,1,1,1,1,1,1,1,1,1,1,1,1,1,
1,1,1,1,1,1,1,1,1,1,1,1,1,1,1,1,1,1,1,1,1,1,1,1,1,1,1,1,1,1,1,1,1,1,1,1,
1,1,1,1,1,1,1,1,1,1,1,1,1,1,1,1,1,1,1,1,1,1,1,1,1,1,1,1,1,1,1,1,1,1,1,1,
1,1,1,1,1,1,1,1,1,1,1,1,1,1,1,1,1,1,1,1,1,1,1,1,1,1,1,1,1,1,1,1,1,1,1,1,
1,1,1,1,1,1,1,1,1,1,1,1,1,1,1,1,1,1,1,1,1,1,1,1,1,1,1,1,1,1,1,1,1,1,1,1,
1,1,1,1,1,1,1,1,1,1,1,1,1,1,1,1,1,1,1,1,1,1,1,1,1,1,1,1,1,1,1,1,1,1,1,1,
1,1,1,1,1,1,1,1,1,1,1,1,1,1,1,1,1,1,1,1,1,1,1,1,1,1,1,1,1,1,1,1,1,1,1,1,
1,1,1,1,1,1,1,1,1,1,1,1,1,1,1,1,1,1,1,1,1,1,1,1,1,1,1,1,1,1,1,1,1,1,1,1,
1,1,1,1,1,1,1,1,1,1,1,1,1,1,1,1,1,1,1,1,1,1,1,1,1,1,1,1,1,1,1,1,1,1,1,1,
1,1,1,1,1,1,1,1,1,1,1,4),(0.,0.0658467982010768),(8.30747755240155,9.30713401544597,
10.3067904784904,11.3064469415348,12.3061034045792,13.3057598676236,14.305416330668,
15.3050727937124,16.3047292567569,17.3043857198013,18.3040421828457,19.3036986458901,
20.3033551089345,21.3030115719789,22.3026680350233,23.3023244980677,24.3019809611122,
25.3016374241566,26.301293887201,27.3009503502454,28.3006068132898,29.3002632763342,
30.2999197393786,31.299576202423,32.2992326654675,33.2988891285119,34.2985455915563,
35.2982020546007,36.2978585176451,37.2975149806895,38.2971714437339,39.2968279067783,
40.2964843698228,41.2961408328672,42.2957972959116,43.295453758956,44.2951102220004,
45.2947666850448,46.2944231480892,47.2940796111337,48.2937360741781,49.2933925372225,
50.2930490002669,51.2927054633113,52.2923619263557,53.2920183894001,54.2916748524445,
55.2913313154889,56.2909877785334,57.2906442415778,58.2903007046222,59.2899571676666,
60.289613630711,61.2892700937554,62.2889265567998,63.2885830198443,64.2882394828887,
65.2878959459331,66.2875524089775,67.2872088720219,68.2868653350663,69.2865217981107,
70.2861782611551,71.2858347241996,72.285491187244,73.2851476502884,74.2848041133328,
75.2844605763772,76.2841170394216,77.283773502466,78.2834299655104,79.2830864285549,
80.2827428915993,81.2823993546437,82.2820558176881,83.2817122807325,84.2813687437769,
85.2810252068213,86.2806816698657,87.2803381329102,88.2799945959546,89.279651058999,
90.2793075220434,91.2789639850878,92.2786204481322,93.2782769111766,94.277933374221,
95.2775898372655,96.2772463003099,97.2769027633543,98.2765592263987,99.2762156894431,
100.275872152488,101.275528615532,102.275185078576,103.274841541621,104.274498004665,
105.27415446771,106.273810930754,107.273467393798,108.273123856843,109.272780319887,
110.272436782932,111.272093245976,112.27174970902,113.271406172065,114.271062635109,
115.270719098154,116.270375561198,117.270032024243,118.269688487287,119.269344950331,
120.269001413376,121.26865787642,122.268314339465,123.267970802509,124.267627265553,
125.267283728598,126.266940191642,127.266596654687,128.266253117731,129.265909580775,
130.26556604382,131.265222506864,132.264878969909,133.264535432953,134.264191895998,
135.263848359042,136.263504822086,137.263161285131,138.262817748175,139.26247421122,
140.262130674264,141.261787137308,142.261443600353,143.261100063397,144.260756526442,
145.260412989486,146.260069452531,147.259725915575,148.259382378619,149.259038841664,
150.258695304708,151.258351767753,152.258008230797,153.257664693841,154.257321156886,
155.25697761993,156.256634082975,157.256290546019,158.255947009063,159.255603472108,
160.255259935152,161.254916398197,162.254572861241,163.254229324286,164.25388578733,
165.253542250374,166.253198713419,167.252855176463,168.252511639508,169.252168102552,
170.251824565596,171.251481028641,172.251137491685,173.25079395473,174.250450417774,
175.250106880818,176.249763343863,177.249419806907,178.249076269952,179.248732732996,
180.248389196041,181.248045659085,182.247702122129,183.247358585174,184.247015048218,
185.246671511263,186.246327974307,187.245984437351,188.245640900396,189.24529736344,
190.244953826485,191.244610289529,192.244266752574,193.243923215618,194.243579678662,
195.243236141707,196.242892604751,197.242549067796,198.24220553084,199.241861993884,
200.241518456929,201.241174919973,202.240831383018,203.240487846062,204.240144309106,
205.239800772151,206.239457235195,207.23911369824,208.238770161284,209.238426624329,
210.238083087373,211.237739550417,212.237396013462,213.237052476506,214.236708939551,
215.236365402595,216.236021865639,217.235678328684,218.235334791728,219.234991254773,
220.234647717817,221.234304180861,222.233960643906,223.23361710695,224.233273569995,
225.232930033039,226.232586496084,227.232242959128,228.231899422172,229.231555885217,
230.231212348261,231.230868811306,232.23052527435,233.230181737394,234.229838200439,
235.229494663483,236.229151126528,237.228807589572,238.228464052616,239.228120515661,
240.227776978705,241.22743344175,242.227089904794,243.226746367839,244.226402830883,
245.226059293927,246.225715756972,247.225372220016,248.225028683061,249.224685146105,
250.224341609149,251.223998072194,252.223654535238,253.223310998283,254.222967461327,
255.222623924372,256.222280387416,257.22193685046,258.221593313505,259.221249776549,
260.220906239594,261.220562702638,262.220219165682,263.219875628727,264.219532091771,
265.219188554816,266.21884501786,267.218501480904,268.218157943949,269.217814406993,
270.217470870038,271.217127333082,272.216783796126,273.216440259171,274.216096722215,
275.21575318526,276.215409648304,277.215066111349,278.214722574393,279.214379037437,
280.214035500482,281.213691963526,282.213348426571,283.213004889615,284.212661352659,
285.212317815704,286.211974278748,287.211630741793,288.211287204837,289.210943667882,
290.210600130926,291.21025659397,292.209913057015,293.209569520059,294.209225983104,
295.208882446148,296.208538909192,297.208195372237,298.207851835281,299.207508298326,
300.20716476137,301.206821224415,302.206477687459,303.206134150503,304.205790613548,
305.205447076592,306.205103539637,307.204760002681,308.204416465725,309.20407292877,
310.203729391814,311.203385854859,312.203042317903,313.202698780947,314.202355243992,
315.202011707036,316.201668170081,317.201324633125,318.200981096169,319.200637559214,
320.200294022258,321.199950485303,322.199606948347),.UNSPECIFIED.);
#2007=B_SPLINE_CURVE_WITH_KNOTS('',3,(#90617,#90618,#90619,#90620,#90621,
#90622,#90623,#90624,#90625,#90626),.UNSPECIFIED.,.F.,.F.,(4,3,3,4),(-4.09293042013064,
-3.99773706693635,-2.99830280020227,-2.06863817490912),.UNSPECIFIED.);
#2008=B_SPLINE_CURVE_WITH_KNOTS('',3,(#90629,#90630,#90631,#90632,#90633,
#90634,#90635),.UNSPECIFIED.,.F.,.F.,(4,3,4),(0.,0.999656463044431,1.11730040836905),
 .UNSPECIFIED.);
#2009=B_SPLINE_CURVE_WITH_KNOTS('',3,(#90640,#90641,#90642,#90643,#90644,
#90645,#90646,#90647,#90648,#90649,#90650,#90651,#90652,#90653,#90654,#90655,
#90656,#90657,#90658,#90659,#90660,#90661),.UNSPECIFIED.,.F.,.F.,(4,3,3,
3,3,3,3,4),(-10.3761157273102,-9.99434266734088,-8.99490840060679,-7.99547413387271,
-6.99603986713862,-5.99660560040453,-4.99717133367044,-4.09293042013064),
 .UNSPECIFIED.);
#2010=B_SPLINE_CURVE_WITH_KNOTS('',3,(#90662,#90663,#90664,#90665,#90666,
#90667,#90668,#90669,#90670,#90671,#90672,#90673,#90674,#90675,#90676,#90677,
#90678,#90679,#90680,#90681,#90682,#90683),.UNSPECIFIED.,.F.,.F.,(4,3,3,
3,3,3,3,4),(1.11730040836905,1.99931292608883,2.99896938913324,3.99862585217764,
4.99828231522204,5.99793877826645,6.99759524131085,7.40048571554864),
 .UNSPECIFIED.);
#2011=B_SPLINE_CURVE_WITH_KNOTS('',3,(#90688,#90689,#90690,#90691,#90692,
#90693,#90694,#90695,#90696,#90697,#90698,#90699,#90700,#90701,#90702,#90703,
#90704,#90705,#90706,#90707,#90708,#90709),.UNSPECIFIED.,.F.,.F.,(4,3,3,
3,3,3,3,4),(-16.6593010344898,-15.9909482677454,-14.9915140010113,-13.9920797342772,
-12.9926454675431,-11.9932112008091,-10.993776934075,-10.3761157273102),
 .UNSPECIFIED.);
#2012=B_SPLINE_CURVE_WITH_KNOTS('',3,(#90710,#90711,#90712,#90713,#90714,
#90715,#90716,#90717,#90718,#90719,#90720,#90721,#90722,#90723,#90724,#90725,
#90726,#90727,#90728,#90729,#90730,#90731),.UNSPECIFIED.,.F.,.F.,(4,3,3,
3,3,3,3,4),(7.40048571554864,7.99725170435527,8.99690816739968,9.99656463044411,
10.9962210934885,11.9958775565329,12.9955340195774,13.6836710227282),
 .UNSPECIFIED.);
#2013=B_SPLINE_CURVE_WITH_KNOTS('',3,(#90736,#90737,#90738,#90739,#90740,
#90741,#90742,#90743,#90744,#90745,#90746,#90747,#90748,#90749,#90750,#90751,
#90752,#90753,#90754,#90755,#90756,#90757),.UNSPECIFIED.,.F.,.F.,(4,3,3,
3,3,3,3,4),(-22.9424863416694,-21.9875538681499,-20.9881196014159,-19.9886853346818,
-18.9892510679477,-17.9898168012136,-16.9903825344795,-16.6593010344898),
 .UNSPECIFIED.);
#2014=B_SPLINE_CURVE_WITH_KNOTS('',3,(#90758,#90759,#90760,#90761,#90762,
#90763,#90764,#90765,#90766,#90767,#90768,#90769,#90770,#90771,#90772,#90773,
#90774,#90775,#90776,#90777,#90778,#90779),.UNSPECIFIED.,.F.,.F.,(4,3,3,
3,3,3,3,4),(13.6836710227282,13.9951904826218,14.9948469456662,15.9945034087106,
16.994159871755,17.9938163347994,18.9934727978439,19.9668563299078),
 .UNSPECIFIED.);
#2015=B_SPLINE_CURVE_WITH_KNOTS('',3,(#90784,#90785,#90786,#90787,#90788,
#90789,#90790,#90791,#90792,#90793,#90794,#90795,#90796,#90797,#90798,#90799,
#90800,#90801,#90802,#90803,#90804,#90805,#90806,#90807,#90808),
 .UNSPECIFIED.,.F.,.F.,(4,3,3,3,3,3,3,3,4),(-29.225671648849,-28.9835937352886,
-27.9841594685545,-26.9847252018204,-25.9852909350863,-24.9858566683522,
-23.9864224016181,-22.986988134884,-22.9424863416694),.UNSPECIFIED.);
#2016=B_SPLINE_CURVE_WITH_KNOTS('',3,(#90809,#90810,#90811,#90812,#90813,
#90814,#90815,#90816,#90817,#90818,#90819,#90820,#90821,#90822,#90823,#90824,
#90825,#90826,#90827,#90828,#90829,#90830,#90831,#90832,#90833),
 .UNSPECIFIED.,.F.,.F.,(4,3,3,3,3,3,3,3,4),(19.9668563299078,19.9931292608883,
20.9927857239327,21.9924421869771,22.9920986500215,23.9917551130659,24.9914115761103,
25.9910680391547,26.2500416370874),.UNSPECIFIED.);
#2017=B_SPLINE_CURVE_WITH_KNOTS('',3,(#90838,#90839,#90840,#90841,#90842,
#90843,#90844,#90845,#90846,#90847,#90848,#90849,#90850,#90851,#90852,#90853,
#90854,#90855,#90856,#90857,#90858,#90859),.UNSPECIFIED.,.F.,.F.,(4,3,3,
3,3,3,3,4),(-35.5088569560286,-34.9801993356931,-33.980765068959,-32.9813308022249,
-31.9818965354908,-30.9824622687567,-29.9830280020227,-29.225671648849),
 .UNSPECIFIED.);
#2018=B_SPLINE_CURVE_WITH_KNOTS('',3,(#90860,#90861,#90862,#90863,#90864,
#90865,#90866,#90867,#90868,#90869,#90870,#90871,#90872,#90873,#90874,#90875,
#90876,#90877,#90878,#90879,#90880,#90881),.UNSPECIFIED.,.F.,.F.,(4,3,3,
3,3,3,3,4),(26.2500416370874,26.9907245021991,27.9903809652435,28.990037428288,
29.9896938913324,30.9893503543768,31.9890068174212,32.533226944267),
 .UNSPECIFIED.);
#2019=B_SPLINE_CURVE_WITH_KNOTS('',3,(#90886,#90887,#90888,#90889,#90890,
#90891,#90892,#90893,#90894,#90895,#90896,#90897,#90898,#90899,#90900,#90901,
#90902,#90903,#90904,#90905,#90906,#90907),.UNSPECIFIED.,.F.,.F.,(4,3,3,
3,3,3,3,4),(-41.7920422632082,-40.9768049360976,-39.9773706693635,-38.9779364026294,
-37.9785021358954,-36.9790678691613,-35.9796336024272,-35.5088569560286),
 .UNSPECIFIED.);
#2020=B_SPLINE_CURVE_WITH_KNOTS('',3,(#90908,#90909,#90910,#90911,#90912,
#90913,#90914,#90915,#90916,#90917,#90918,#90919,#90920,#90921,#90922,#90923,
#90924,#90925,#90926,#90927,#90928,#90929),.UNSPECIFIED.,.F.,.F.,(4,3,3,
3,3,3,3,4),(32.533226944267,32.9886632804656,33.98831974351,34.9879762065544,
35.9876326695989,36.9872891326432,37.9869455956877,38.8164122514466),
 .UNSPECIFIED.);
#2021=B_SPLINE_CURVE_WITH_KNOTS('',3,(#90934,#90935,#90936,#90937,#90938,
#90939,#90940,#90941,#90942,#90943,#90944,#90945,#90946,#90947,#90948,#90949,
#90950,#90951,#90952,#90953,#90954,#90955,#90956,#90957,#90958),
 .UNSPECIFIED.,.F.,.F.,(4,3,3,3,3,3,3,3,4),(-48.0752275703878,-47.9728448032362,
-46.9734105365022,-45.9739762697681,-44.974542003034,-43.9751077362999,
-42.9756734695658,-41.9762392028317,-41.7920422632082),.UNSPECIFIED.);
#2022=B_SPLINE_CURVE_WITH_KNOTS('',3,(#90959,#90960,#90961,#90962,#90963,
#90964,#90965,#90966,#90967,#90968,#90969,#90970,#90971,#90972,#90973,#90974,
#90975,#90976,#90977,#90978,#90979,#90980,#90981,#90982,#90983),
 .UNSPECIFIED.,.F.,.F.,(4,3,3,3,3,3,3,3,4),(38.8164122514466,38.9866020587321,
39.9862585217765,40.9859149848209,41.9855714478653,42.9852279109097,43.9848843739542,
44.9845408369986,45.0995975586262),.UNSPECIFIED.);
#2023=B_SPLINE_CURVE_WITH_KNOTS('',3,(#90988,#90989,#90990,#90991,#90992,
#90993,#90994,#90995,#90996,#90997,#90998,#90999,#91000,#91001,#91002,#91003,
#91004,#91005,#91006,#91007,#91008,#91009),.UNSPECIFIED.,.F.,.F.,(4,3,3,
3,3,3,3,4),(-54.3584128775674,-53.9694504036408,-52.9700161369067,-51.9705818701726,
-50.9711476034385,-49.9717133367044,-48.9722790699703,-48.0752275703878),
 .UNSPECIFIED.);
#2024=B_SPLINE_CURVE_WITH_KNOTS('',3,(#91010,#91011,#91012,#91013,#91014,
#91015,#91016,#91017,#91018,#91019,#91020,#91021,#91022,#91023,#91024,#91025,
#91026,#91027,#91028,#91029,#91030,#91031),.UNSPECIFIED.,.F.,.F.,(4,3,3,
3,3,3,3,4),(45.0995975586262,45.984197300043,46.9838537630874,47.9835102261318,
48.9831666891762,49.9828231522206,50.982479615265,51.3827828658058),
 .UNSPECIFIED.);
#2025=B_SPLINE_CURVE_WITH_KNOTS('',3,(#91036,#91037,#91038,#91039,#91040,
#91041,#91042,#91043,#91044,#91045,#91046,#91047,#91048,#91049,#91050,#91051,
#91052,#91053,#91054,#91055,#91056,#91057),.UNSPECIFIED.,.F.,.F.,(4,3,3,
3,3,3,3,4),(-60.641598184747,-59.9660560040453,-58.9666217373112,-57.9671874705771,
-56.967753203843,-55.968318937109,-54.9688846703749,-54.3584128775674),
 .UNSPECIFIED.);
#2026=B_SPLINE_CURVE_WITH_KNOTS('',3,(#91058,#91059,#91060,#91061,#91062,
#91063,#91064,#91065,#91066,#91067,#91068,#91069,#91070,#91071,#91072,#91073,
#91074,#91075,#91076,#91077,#91078,#91079),.UNSPECIFIED.,.F.,.F.,(4,3,3,
3,3,3,3,4),(51.3827828658058,51.9821360783094,52.9817925413539,53.9814490043983,
54.9811054674427,55.9807619304871,56.9804183935315,57.6659681729854),
 .UNSPECIFIED.);
#2027=B_SPLINE_CURVE_WITH_KNOTS('',3,(#91084,#91085,#91086,#91087,#91088,
#91089,#91090,#91091,#91092,#91093,#91094,#91095,#91096,#91097,#91098,#91099,
#91100,#91101,#91102,#91103,#91104,#91105),.UNSPECIFIED.,.F.,.F.,(4,3,3,
3,3,3,3,4),(-66.9247834919265,-65.9626616044498,-64.9632273377157,-63.9637930709817,
-62.9643588042476,-61.9649245375135,-60.9654902707794,-60.641598184747),
 .UNSPECIFIED.);
#2028=B_SPLINE_CURVE_WITH_KNOTS('',3,(#91106,#91107,#91108,#91109,#91110,
#91111,#91112,#91113,#91114,#91115,#91116,#91117,#91118,#91119,#91120,#91121,
#91122,#91123,#91124,#91125,#91126,#91127),.UNSPECIFIED.,.F.,.F.,(4,3,3,
3,3,3,3,4),(57.6659681729854,57.980074856576,58.9797313196204,59.9793877826648,
60.9790442457092,61.9787007087536,62.978357171798,63.949153480165),
 .UNSPECIFIED.);
#2029=B_SPLINE_CURVE_WITH_KNOTS('',3,(#91132,#91133,#91134,#91135,#91136,
#91137,#91138,#91139,#91140,#91141,#91142,#91143,#91144,#91145,#91146,#91147,
#91148,#91149,#91150,#91151,#91152,#91153,#91154,#91155,#91156),
 .UNSPECIFIED.,.F.,.F.,(4,3,3,3,3,3,3,3,4),(-73.2079687991061,-72.9587014715884,
-71.9592672048544,-70.9598329381203,-69.9603986713862,-68.9609644046521,
-67.961530137918,-66.9620958711839,-66.9247834919265),.UNSPECIFIED.);
#2030=B_SPLINE_CURVE_WITH_KNOTS('',3,(#91157,#91158,#91159,#91160,#91161,
#91162,#91163,#91164,#91165,#91166,#91167,#91168,#91169,#91170,#91171,#91172,
#91173,#91174,#91175,#91176,#91177,#91178,#91179,#91180,#91181),
 .UNSPECIFIED.,.F.,.F.,(4,3,3,3,3,3,3,3,4),(63.949153480165,63.9780136348424,
64.9776700978868,65.9773265609312,66.9769830239756,67.9766394870201,68.9762959500645,
69.9759524131089,70.2323387873446),.UNSPECIFIED.);
#2031=B_SPLINE_CURVE_WITH_KNOTS('',3,(#91186,#91187,#91188,#91189,#91190,
#91191,#91192,#91193,#91194,#91195,#91196,#91197,#91198,#91199,#91200,#91201,
#91202,#91203,#91204,#91205,#91206,#91207),.UNSPECIFIED.,.F.,.F.,(4,3,3,
3,3,3,3,4),(-79.4911541062857,-78.955307071993,-77.9558728052589,-76.9564385385248,
-75.9570042717907,-74.9575700050566,-73.9581357383226,-73.2079687991061),
 .UNSPECIFIED.);
#2032=B_SPLINE_CURVE_WITH_KNOTS('',3,(#91208,#91209,#91210,#91211,#91212,
#91213,#91214,#91215,#91216,#91217,#91218,#91219,#91220,#91221,#91222,#91223,
#91224,#91225,#91226,#91227,#91228,#91229),.UNSPECIFIED.,.F.,.F.,(4,3,3,
3,3,3,3,4),(70.2323387873446,70.9756088761533,71.9752653391977,72.9749218022421,
73.9745782652865,74.9742347283309,75.9738911913753,76.5155240945241),
 .UNSPECIFIED.);
#2033=B_SPLINE_CURVE_WITH_KNOTS('',3,(#91234,#91235,#91236,#91237,#91238,
#91239,#91240,#91241,#91242,#91243,#91244,#91245,#91246,#91247,#91248,#91249,
#91250,#91251,#91252,#91253,#91254,#91255),.UNSPECIFIED.,.F.,.F.,(4,3,3,
3,3,3,3,4),(-85.7743394134653,-84.9519126723975,-83.9524784056634,-82.9530441389293,
-81.9536098721953,-80.9541756054612,-79.9547413387271,-79.4911541062857),
 .UNSPECIFIED.);
#2034=B_SPLINE_CURVE_WITH_KNOTS('',3,(#91256,#91257,#91258,#91259,#91260,
#91261,#91262,#91263,#91264,#91265,#91266,#91267,#91268,#91269,#91270,#91271,
#91272,#91273,#91274,#91275,#91276,#91277),.UNSPECIFIED.,.F.,.F.,(4,3,3,
3,3,3,3,4),(76.5155240945241,76.9735476544198,77.9732041174642,78.9728605805086,
79.972517043553,80.9721735065974,81.9718299696419,82.7987094017037),
 .UNSPECIFIED.);
#2035=B_SPLINE_CURVE_WITH_KNOTS('',3,(#91282,#91283,#91284,#91285,#91286,
#91287,#91288,#91289,#91290,#91291,#91292,#91293,#91294,#91295,#91296,#91297,
#91298,#91299,#91300,#91301,#91302,#91303,#91304,#91305,#91306),
 .UNSPECIFIED.,.F.,.F.,(4,3,3,3,3,3,3,3,4),(-92.0575247206449,-91.9479525395361,
-90.948518272802,-89.9490840060679,-88.9496497393339,-87.9502154725998,
-86.9507812058657,-85.9513469391316,-85.7743394134653),.UNSPECIFIED.);
#2036=B_SPLINE_CURVE_WITH_KNOTS('',3,(#91307,#91308,#91309,#91310,#91311,
#91312,#91313,#91314,#91315,#91316,#91317,#91318,#91319,#91320,#91321,#91322,
#91323,#91324,#91325,#91326,#91327,#91328,#91329,#91330,#91331),
 .UNSPECIFIED.,.F.,.F.,(4,3,3,3,3,3,3,3,4),(82.7987094017037,82.9714864326863,
83.9711428957307,84.9707993587751,85.9704558218195,86.9701122848639,87.9697687479083,
88.9694252109527,89.0818947088833),.UNSPECIFIED.);
#2037=B_SPLINE_CURVE_WITH_KNOTS('',3,(#91336,#91337,#91338,#91339,#91340,
#91341,#91342,#91343,#91344,#91345,#91346,#91347,#91348,#91349,#91350,#91351,
#91352,#91353,#91354,#91355,#91356,#91357),.UNSPECIFIED.,.F.,.F.,(4,3,3,
3,3,3,3,4),(-98.3407100278245,-97.9445581399407,-96.9451238732066,-95.9456896064725,
-94.9462553397384,-93.9468210730043,-92.9473868062702,-92.0575247206449),
 .UNSPECIFIED.);
#2038=B_SPLINE_CURVE_WITH_KNOTS('',3,(#91358,#91359,#91360,#91361,#91362,
#91363,#91364,#91365,#91366,#91367,#91368,#91369,#91370,#91371,#91372,#91373,
#91374,#91375,#91376,#91377,#91378,#91379),.UNSPECIFIED.,.F.,.F.,(4,3,3,
3,3,3,3,4),(89.0818947088833,89.9690816739971,90.9687381370416,91.968394600086,
92.9680510631304,93.9677075261748,94.9673639892192,95.3650800160629),
 .UNSPECIFIED.);
#2039=B_SPLINE_CURVE_WITH_KNOTS('',3,(#91384,#91385,#91386,#91387,#91388,
#91389,#91390,#91391,#91392,#91393,#91394,#91395,#91396,#91397,#91398,#91399,
#91400,#91401,#91402,#91403,#91404,#91405),.UNSPECIFIED.,.F.,.F.,(4,3,3,
3,3,3,3,4),(-104.623895335004,-103.941163740345,-102.941729473611,-101.942295206877,
-100.942860940143,-99.9434266734089,-98.9439924066748,-98.3407100278245),
 .UNSPECIFIED.);
#2040=B_SPLINE_CURVE_WITH_KNOTS('',3,(#91406,#91407,#91408,#91409,#91410,
#91411,#91412,#91413,#91414,#91415,#91416,#91417,#91418,#91419,#91420,#91421,
#91422,#91423,#91424,#91425,#91426,#91427),.UNSPECIFIED.,.F.,.F.,(4,3,3,
3,3,3,3,4),(95.3650800160629,95.9670204522636,96.966676915308,97.9663333783524,
98.9659898413969,99.9656463044413,100.965302767486,101.648265323242),
 .UNSPECIFIED.);
#2041=B_SPLINE_CURVE_WITH_KNOTS('',3,(#91432,#91433,#91434,#91435,#91436,
#91437,#91438,#91439,#91440,#91441,#91442,#91443,#91444,#91445,#91446,#91447,
#91448,#91449,#91450,#91451,#91452,#91453),.UNSPECIFIED.,.F.,.F.,(4,3,3,
3,3,3,3,4),(-110.907080642184,-109.93776934075,-108.938335074016,-107.938900807282,
-106.939466540547,-105.940032273813,-104.940598007079,-104.623895335004),
 .UNSPECIFIED.);
#2042=B_SPLINE_CURVE_WITH_KNOTS('',3,(#91454,#91455,#91456,#91457,#91458,
#91459,#91460,#91461,#91462,#91463,#91464,#91465,#91466,#91467,#91468,#91469,
#91470,#91471,#91472,#91473,#91474,#91475),.UNSPECIFIED.,.F.,.F.,(4,3,3,
3,3,3,3,4),(101.648265323242,101.96495923053,102.964615693575,103.964272156619,
104.963928619663,105.963585082708,106.963241545752,107.931450630422),
 .UNSPECIFIED.);
#2043=B_SPLINE_CURVE_WITH_KNOTS('',3,(#91480,#91481,#91482,#91483,#91484,
#91485,#91486,#91487,#91488,#91489,#91490,#91491,#91492,#91493,#91494,#91495,
#91496,#91497,#91498,#91499,#91500,#91501,#91502,#91503,#91504),
 .UNSPECIFIED.,.F.,.F.,(4,3,3,3,3,3,3,3,4),(-117.190265949363,-116.933809207888,
-115.934374941154,-114.93494067442,-113.935506407686,-112.936072140952,
-111.936637874218,-110.937203607484,-110.907080642184),.UNSPECIFIED.);
#2044=B_SPLINE_CURVE_WITH_KNOTS('',3,(#91505,#91506,#91507,#91508,#91509,
#91510,#91511,#91512,#91513,#91514,#91515,#91516,#91517,#91518,#91519,#91520,
#91521,#91522,#91523,#91524,#91525,#91526,#91527,#91528,#91529),
 .UNSPECIFIED.,.F.,.F.,(4,3,3,3,3,3,3,3,4),(107.931450630422,107.962898008797,
108.962554471841,109.962210934885,110.96186739793,111.961523860974,112.961180324019,
113.960836787063,114.214635937602),.UNSPECIFIED.);
#2045=B_SPLINE_CURVE_WITH_KNOTS('',3,(#91534,#91535,#91536,#91537,#91538,
#91539,#91540,#91541,#91542,#91543,#91544,#91545,#91546,#91547,#91548,#91549,
#91550,#91551,#91552,#91553,#91554,#91555),.UNSPECIFIED.,.F.,.F.,(4,3,3,
3,3,3,3,4),(-123.473451256543,-122.930414808293,-121.930980541559,-120.931546274825,
-119.932112008091,-118.932677741357,-117.933243474622,-117.190265949363),
 .UNSPECIFIED.);
#2046=B_SPLINE_CURVE_WITH_KNOTS('',3,(#91556,#91557,#91558,#91559,#91560,
#91561,#91562,#91563,#91564,#91565,#91566,#91567,#91568,#91569,#91570,#91571,
#91572,#91573,#91574,#91575,#91576,#91577),.UNSPECIFIED.,.F.,.F.,(4,3,3,
3,3,3,3,4),(114.214635937602,114.960493250107,115.960149713152,116.959806176196,
117.959462639241,118.959119102285,119.95877556533,120.497821244781),
 .UNSPECIFIED.);
#2047=B_SPLINE_CURVE_WITH_KNOTS('',3,(#91582,#91583,#91584,#91585,#91586,
#91587,#91588,#91589,#91590,#91591,#91592,#91593,#91594,#91595,#91596,#91597,
#91598,#91599,#91600,#91601,#91602,#91603),.UNSPECIFIED.,.F.,.F.,(4,3,3,
3,3,3,3,4),(-129.756636563722,-128.927020408697,-127.927586141963,-126.928151875229,
-125.928717608495,-124.929283341761,-123.929849075027,-123.473451256543),
 .UNSPECIFIED.);
#2048=B_SPLINE_CURVE_WITH_KNOTS('',3,(#91604,#91605,#91606,#91607,#91608,
#91609,#91610,#91611,#91612,#91613,#91614,#91615,#91616,#91617,#91618,#91619,
#91620,#91621,#91622,#91623,#91624,#91625),.UNSPECIFIED.,.F.,.F.,(4,3,3,
3,3,3,3,4),(120.497821244781,120.958432028374,121.958088491418,122.957744954463,
123.957401417507,124.957057880552,125.956714343596,126.781006551961),
 .UNSPECIFIED.);
#2049=B_SPLINE_CURVE_WITH_KNOTS('',3,(#91630,#91631,#91632,#91633,#91634,
#91635,#91636,#91637,#91638,#91639,#91640,#91641,#91642,#91643,#91644,#91645,
#91646,#91647,#91648,#91649,#91650,#91651,#91652,#91653,#91654),
 .UNSPECIFIED.,.F.,.F.,(4,3,3,3,3,3,3,3,4),(-136.039821870902,-135.923060275836,
-134.923626009102,-133.924191742368,-132.924757475634,-131.9253232089,-130.925888942166,
-129.926454675432,-129.756636563722),.UNSPECIFIED.);
#2050=B_SPLINE_CURVE_WITH_KNOTS('',3,(#91655,#91656,#91657,#91658,#91659,
#91660,#91661,#91662,#91663,#91664,#91665,#91666,#91667,#91668,#91669,#91670,
#91671,#91672,#91673,#91674,#91675,#91676,#91677,#91678,#91679),
 .UNSPECIFIED.,.F.,.F.,(4,3,3,3,3,3,3,3,4),(126.781006551961,126.95637080664,
127.956027269685,128.955683732729,129.955340195774,130.954996658818,131.954653121862,
132.954309584907,133.06419185914),.UNSPECIFIED.);
#2051=B_SPLINE_CURVE_WITH_KNOTS('',3,(#91684,#91685,#91686,#91687,#91688,
#91689,#91690,#91691,#91692,#91693,#91694,#91695,#91696,#91697,#91698,#91699,
#91700,#91701,#91702,#91703,#91704,#91705),.UNSPECIFIED.,.F.,.F.,(4,3,3,
3,3,3,3,4),(-142.323007178082,-141.919665876241,-140.920231609506,-139.920797342772,
-138.921363076038,-137.921928809304,-136.92249454257,-136.039821870902),
 .UNSPECIFIED.);
#2052=B_SPLINE_CURVE_WITH_KNOTS('',3,(#91706,#91707,#91708,#91709,#91710,
#91711,#91712,#91713,#91714,#91715,#91716,#91717,#91718,#91719,#91720,#91721,
#91722,#91723,#91724,#91725,#91726,#91727),.UNSPECIFIED.,.F.,.F.,(4,3,3,
3,3,3,3,4),(133.06419185914,133.953966047951,134.953622510996,135.95327897404,
136.952935437085,137.952591900129,138.952248363173,139.34737716632),
 .UNSPECIFIED.);
#2053=B_SPLINE_CURVE_WITH_KNOTS('',3,(#91732,#91733,#91734,#91735,#91736,
#91737,#91738,#91739,#91740,#91741,#91742,#91743,#91744,#91745,#91746,#91747,
#91748,#91749,#91750,#91751,#91752,#91753),.UNSPECIFIED.,.F.,.F.,(4,3,3,
3,3,3,3,4),(-148.606192485261,-147.916271476645,-146.916837209911,-145.917402943177,
-144.917968676443,-143.918534409709,-142.919100142975,-142.323007178082),
 .UNSPECIFIED.);
#2054=B_SPLINE_CURVE_WITH_KNOTS('',3,(#91754,#91755,#91756,#91757,#91758,
#91759,#91760,#91761,#91762,#91763,#91764,#91765,#91766,#91767,#91768,#91769,
#91770,#91771,#91772,#91773,#91774,#91775),.UNSPECIFIED.,.F.,.F.,(4,3,3,
3,3,3,3,4),(139.34737716632,139.951904826218,140.951561289262,141.951217752307,
142.950874215351,143.950530678395,144.95018714144,145.6305624735),
 .UNSPECIFIED.);
#2055=B_SPLINE_CURVE_WITH_KNOTS('',3,(#91780,#91781,#91782,#91783,#91784,
#91785,#91786,#91787,#91788,#91789,#91790,#91791,#91792,#91793,#91794,#91795,
#91796,#91797,#91798,#91799,#91800,#91801),.UNSPECIFIED.,.F.,.F.,(4,3,3,
3,3,3,3,4),(-154.889377792441,-153.91287707705,-152.913442810316,-151.914008543581,
-150.914574276847,-149.915140010113,-148.915705743379,-148.606192485261),
 .UNSPECIFIED.);
#2056=B_SPLINE_CURVE_WITH_KNOTS('',3,(#91802,#91803,#91804,#91805,#91806,
#91807,#91808,#91809,#91810,#91811,#91812,#91813,#91814,#91815,#91816,#91817,
#91818,#91819,#91820,#91821,#91822,#91823),.UNSPECIFIED.,.F.,.F.,(4,3,3,
3,3,3,3,4),(145.6305624735,145.949843604484,146.949500067529,147.949156530573,
148.948812993617,149.948469456662,150.948125919706,151.913747780679),
 .UNSPECIFIED.);
#2057=B_SPLINE_CURVE_WITH_KNOTS('',3,(#91828,#91829,#91830,#91831,#91832,
#91833,#91834,#91835,#91836,#91837,#91838,#91839,#91840,#91841,#91842,#91843,
#91844,#91845,#91846,#91847,#91848,#91849,#91850,#91851,#91852),
 .UNSPECIFIED.,.F.,.F.,(4,3,3,3,3,3,3,3,4),(-161.17256309962,-160.908916944188,
-159.909482677454,-158.91004841072,-157.910614143986,-156.911179877252,
-155.911745610518,-154.912311343784,-154.889377792441),.UNSPECIFIED.);
#2058=B_SPLINE_CURVE_WITH_KNOTS('',3,(#91853,#91854,#91855,#91856,#91857,
#91858,#91859,#91860,#91861,#91862,#91863,#91864,#91865,#91866,#91867,#91868,
#91869,#91870,#91871,#91872,#91873,#91874,#91875,#91876,#91877),
 .UNSPECIFIED.,.F.,.F.,(4,3,3,3,3,3,3,3,4),(151.913747780679,151.947782382751,
152.947438845795,153.94709530884,154.946751771884,155.946408234928,156.946064697973,
157.945721161017,158.196933087859),.UNSPECIFIED.);
#2059=B_SPLINE_CURVE_WITH_KNOTS('',3,(#91882,#91883,#91884,#91885,#91886,
#91887,#91888,#91889,#91890,#91891,#91892,#91893,#91894,#91895,#91896,#91897,
#91898,#91899,#91900,#91901,#91902,#91903),.UNSPECIFIED.,.F.,.F.,(4,3,3,
3,3,3,3,4),(-167.4557484068,-166.905522544593,-165.906088277859,-164.906654011125,
-163.90721974439,-162.907785477656,-161.908351210922,-161.17256309962),
 .UNSPECIFIED.);
#2060=B_SPLINE_CURVE_WITH_KNOTS('',3,(#91904,#91905,#91906,#91907,#91908,
#91909,#91910,#91911,#91912,#91913,#91914,#91915,#91916,#91917,#91918,#91919,
#91920,#91921,#91922,#91923,#91924,#91925),.UNSPECIFIED.,.F.,.F.,(4,3,3,
3,3,3,3,4),(158.196933087859,158.945377624062,159.945034087106,160.944690550151,
161.944347013195,162.944003476239,163.943659939284,164.480118395038),
 .UNSPECIFIED.);
#2061=B_SPLINE_CURVE_WITH_KNOTS('',3,(#91930,#91931,#91932,#91933,#91934,
#91935,#91936,#91937,#91938,#91939,#91940,#91941,#91942,#91943,#91944,#91945,
#91946,#91947,#91948,#91949,#91950,#91951),.UNSPECIFIED.,.F.,.F.,(4,3,3,
3,3,3,3,4),(-173.738933713979,-172.902128144997,-171.902693878263,-170.903259611529,
-169.903825344795,-168.904391078061,-167.904956811327,-167.4557484068),
 .UNSPECIFIED.);
#2062=B_SPLINE_CURVE_WITH_KNOTS('',3,(#91952,#91953,#91954,#91955,#91956,
#91957,#91958,#91959,#91960,#91961,#91962,#91963,#91964,#91965,#91966,#91967,
#91968,#91969,#91970,#91971,#91972,#91973),.UNSPECIFIED.,.F.,.F.,(4,3,3,
3,3,3,3,4),(164.480118395038,164.943316402328,165.942972865373,166.942629328417,
167.942285791461,168.941942254506,169.94159871755,170.763303702218),
 .UNSPECIFIED.);
#2063=B_SPLINE_CURVE_WITH_KNOTS('',3,(#91978,#91979,#91980,#91981,#91982,
#91983,#91984,#91985,#91986,#91987,#91988,#91989,#91990,#91991,#91992,#91993,
#91994,#91995,#91996,#91997,#91998,#91999,#92000,#92001,#92002),
 .UNSPECIFIED.,.F.,.F.,(4,3,3,3,3,3,3,3,4),(-180.022119021159,-179.898168012136,
-178.898733745402,-177.899299478668,-176.899865211934,-175.9004309452,-174.900996678466,
-173.901562411731,-173.738933713979),.UNSPECIFIED.);
#2064=B_SPLINE_CURVE_WITH_KNOTS('',3,(#92003,#92004,#92005,#92006,#92007,
#92008,#92009,#92010,#92011,#92012,#92013,#92014,#92015,#92016,#92017,#92018,
#92019,#92020,#92021,#92022,#92023,#92024,#92025,#92026,#92027),
 .UNSPECIFIED.,.F.,.F.,(4,3,3,3,3,3,3,3,4),(170.763303702218,170.941255180595,
171.940911643639,172.940568106683,173.940224569728,174.939881032772,175.939537495817,
176.939193958861,177.046489009397),.UNSPECIFIED.);
#2065=B_SPLINE_CURVE_WITH_KNOTS('',3,(#92032,#92033,#92034,#92035,#92036,
#92037,#92038,#92039,#92040,#92041,#92042,#92043,#92044,#92045,#92046,#92047,
#92048,#92049,#92050,#92051,#92052,#92053),.UNSPECIFIED.,.F.,.F.,(4,3,3,
3,3,3,3,4),(-186.305304328339,-185.89477361254,-184.895339345806,-183.895905079072,
-182.896470812338,-181.897036545604,-180.89760227887,-180.022119021159),
 .UNSPECIFIED.);
#2066=B_SPLINE_CURVE_WITH_KNOTS('',3,(#92054,#92055,#92056,#92057,#92058,
#92059,#92060,#92061,#92062,#92063,#92064,#92065,#92066,#92067,#92068,#92069,
#92070,#92071,#92072,#92073,#92074,#92075),.UNSPECIFIED.,.F.,.F.,(4,3,3,
3,3,3,3,4),(177.046489009397,177.938850421905,178.93850688495,179.938163347994,
180.937819811039,181.937476274083,182.937132737128,183.329674316577),
 .UNSPECIFIED.);
#2067=B_SPLINE_CURVE_WITH_KNOTS('',3,(#92080,#92081,#92082,#92083,#92084,
#92085,#92086,#92087,#92088,#92089,#92090,#92091,#92092,#92093,#92094,#92095,
#92096,#92097,#92098,#92099,#92100,#92101),.UNSPECIFIED.,.F.,.F.,(4,3,3,
3,3,3,3,4),(-192.588489635518,-191.891379212945,-190.891944946211,-189.892510679477,
-188.893076412743,-187.893642146009,-186.894207879275,-186.305304328339),
 .UNSPECIFIED.);
#2068=B_SPLINE_CURVE_WITH_KNOTS('',3,(#92102,#92103,#92104,#92105,#92106,
#92107,#92108,#92109,#92110,#92111,#92112,#92113,#92114,#92115,#92116,#92117,
#92118,#92119,#92120,#92121,#92122,#92123),.UNSPECIFIED.,.F.,.F.,(4,3,3,
3,3,3,3,4),(183.329674316577,183.936789200172,184.936445663216,185.936102126261,
186.935758589305,187.93541505235,188.935071515394,189.612859623757),
 .UNSPECIFIED.);
#2069=B_SPLINE_CURVE_WITH_KNOTS('',3,(#92128,#92129,#92130,#92131,#92132,
#92133,#92134,#92135,#92136,#92137,#92138,#92139,#92140,#92141,#92142,#92143,
#92144,#92145,#92146,#92147,#92148,#92149),.UNSPECIFIED.,.F.,.F.,(4,3,3,
3,3,3,3,4),(-198.871674942698,-197.887984813349,-196.888550546615,-195.889116279881,
-194.889682013147,-193.890247746413,-192.890813479679,-192.588489635518),
 .UNSPECIFIED.);
#2070=B_SPLINE_CURVE_WITH_KNOTS('',3,(#92150,#92151,#92152,#92153,#92154,
#92155,#92156,#92157,#92158,#92159,#92160,#92161,#92162,#92163,#92164,#92165,
#92166,#92167,#92168,#92169,#92170,#92171),.UNSPECIFIED.,.F.,.F.,(4,3,3,
3,3,3,3,4),(189.612859623757,189.934727978438,190.934384441483,191.934040904527,
192.933697367572,193.933353830616,194.93301029366,195.896044930936),
 .UNSPECIFIED.);
#2071=B_SPLINE_CURVE_WITH_KNOTS('',3,(#92176,#92177,#92178,#92179,#92180,
#92181,#92182,#92183,#92184,#92185,#92186,#92187,#92188,#92189,#92190,#92191,
#92192,#92193,#92194,#92195,#92196,#92197,#92198,#92199,#92200),
 .UNSPECIFIED.,.F.,.F.,(4,3,3,3,3,3,3,3,4),(-205.154860249877,-204.884024680488,
-203.884590413754,-202.88515614702,-201.885721880286,-200.886287613552,
-199.886853346818,-198.887419080084,-198.871674942698),.UNSPECIFIED.);
#2072=B_SPLINE_CURVE_WITH_KNOTS('',3,(#92201,#92202,#92203,#92204,#92205,
#92206,#92207,#92208,#92209,#92210,#92211,#92212,#92213,#92214,#92215,#92216,
#92217,#92218,#92219,#92220,#92221,#92222,#92223,#92224,#92225),
 .UNSPECIFIED.,.F.,.F.,(4,3,3,3,3,3,3,3,4),(195.896044930936,195.932666756705,
196.932323219749,197.931979682794,198.931636145838,199.931292608883,200.930949071927,
201.930605534971,202.179230238116),.UNSPECIFIED.);
#2073=B_SPLINE_CURVE_WITH_KNOTS('',3,(#92230,#92231,#92232,#92233,#92234,
#92235,#92236,#92237,#92238,#92239,#92240,#92241,#92242,#92243,#92244,#92245,
#92246,#92247,#92248,#92249,#92250,#92251),.UNSPECIFIED.,.F.,.F.,(4,3,3,
3,3,3,3,4),(-211.438045557057,-210.880630280893,-209.881196014159,-208.881761747424,
-207.88232748069,-206.882893213956,-205.883458947222,-205.154860249877),
 .UNSPECIFIED.);
#2074=B_SPLINE_CURVE_WITH_KNOTS('',3,(#92252,#92253,#92254,#92255,#92256,
#92257,#92258,#92259,#92260,#92261,#92262,#92263,#92264,#92265,#92266,#92267,
#92268,#92269,#92270,#92271,#92272,#92273),.UNSPECIFIED.,.F.,.F.,(4,3,3,
3,3,3,3,4),(202.179230238116,202.930261998016,203.92991846106,204.929574924105,
205.929231387149,206.928887850193,207.928544313238,208.462415545295),
 .UNSPECIFIED.);
#2075=B_SPLINE_CURVE_WITH_KNOTS('',3,(#92278,#92279,#92280,#92281,#92282,
#92283,#92284,#92285,#92286,#92287,#92288,#92289,#92290,#92291,#92292,#92293,
#92294,#92295,#92296,#92297,#92298,#92299),.UNSPECIFIED.,.F.,.F.,(4,3,3,
3,3,3,3,4),(-217.721230864236,-216.877235881297,-215.877801614563,-214.878367347829,
-213.878933081095,-212.879498814361,-211.880064547627,-211.438045557057),
 .UNSPECIFIED.);
#2076=B_SPLINE_CURVE_WITH_KNOTS('',3,(#92300,#92301,#92302,#92303,#92304,
#92305,#92306,#92307,#92308,#92309,#92310,#92311,#92312,#92313,#92314,#92315,
#92316,#92317,#92318,#92319,#92320,#92321),.UNSPECIFIED.,.F.,.F.,(4,3,3,
3,3,3,3,4),(208.462415545295,208.928200776282,209.927857239327,210.927513702371,
211.927170165416,212.92682662846,213.926483091504,214.745600852475),
 .UNSPECIFIED.);
#2077=B_SPLINE_CURVE_WITH_KNOTS('',3,(#92326,#92327,#92328,#92329,#92330,
#92331,#92332,#92333,#92334,#92335,#92336,#92337,#92338,#92339,#92340,#92341,
#92342,#92343,#92344,#92345,#92346,#92347,#92348,#92349,#92350),
 .UNSPECIFIED.,.F.,.F.,(4,3,3,3,3,3,3,3,4),(-224.004416171416,-223.873275748436,
-222.873841481702,-221.874407214968,-220.874972948234,-219.875538681499,
-218.876104414765,-217.876670148031,-217.721230864236),.UNSPECIFIED.);
#2078=B_SPLINE_CURVE_WITH_KNOTS('',3,(#92351,#92352,#92353,#92354,#92355,
#92356,#92357,#92358,#92359,#92360,#92361,#92362,#92363,#92364,#92365,#92366,
#92367,#92368,#92369,#92370,#92371,#92372,#92373,#92374,#92375),
 .UNSPECIFIED.,.F.,.F.,(4,3,3,3,3,3,3,3,4),(214.745600852475,214.926139554549,
215.925796017593,216.925452480638,217.925108943682,218.924765406726,219.924421869771,
220.924078332815,221.028786159654),.UNSPECIFIED.);
#2079=B_SPLINE_CURVE_WITH_KNOTS('',3,(#92380,#92381,#92382,#92383,#92384,
#92385,#92386,#92387,#92388,#92389,#92390,#92391,#92392,#92393,#92394,#92395,
#92396,#92397,#92398,#92399,#92400,#92401),.UNSPECIFIED.,.F.,.F.,(4,3,3,
3,3,3,3,4),(-230.287601478596,-229.86988134884,-228.870447082106,-227.871012815372,
-226.871578548638,-225.872144281904,-224.87271001517,-224.004416171416),
 .UNSPECIFIED.);
#2080=B_SPLINE_CURVE_WITH_KNOTS('',3,(#92402,#92403,#92404,#92405,#92406,
#92407,#92408,#92409,#92410,#92411,#92412,#92413,#92414,#92415,#92416,#92417,
#92418,#92419,#92420,#92421,#92422,#92423),.UNSPECIFIED.,.F.,.F.,(4,3,3,
3,3,3,3,4),(221.028786159654,221.92373479586,222.923391258904,223.923047721948,
224.922704184993,225.922360648037,226.922017111082,227.311971466834),
 .UNSPECIFIED.);
#2081=B_SPLINE_CURVE_WITH_KNOTS('',3,(#92428,#92429,#92430,#92431,#92432,
#92433,#92434,#92435,#92436,#92437,#92438,#92439,#92440,#92441,#92442,#92443,
#92444,#92445,#92446,#92447,#92448,#92449),.UNSPECIFIED.,.F.,.F.,(4,3,3,
3,3,3,3,4),(-236.570786785775,-235.866486949245,-234.867052682511,-233.867618415777,
-232.868184149043,-231.868749882309,-230.869315615574,-230.287601478596),
 .UNSPECIFIED.);
#2082=B_SPLINE_CURVE_WITH_KNOTS('',3,(#92450,#92451,#92452,#92453,#92454,
#92455,#92456,#92457,#92458,#92459,#92460,#92461,#92462,#92463,#92464,#92465,
#92466,#92467,#92468,#92469,#92470,#92471),.UNSPECIFIED.,.F.,.F.,(4,3,3,
3,3,3,3,4),(227.311971466834,227.921673574126,228.921330037171,229.920986500215,
230.920642963259,231.920299426304,232.919955889348,233.595156774013),
 .UNSPECIFIED.);
#2083=B_SPLINE_CURVE_WITH_KNOTS('',3,(#92476,#92477,#92478,#92479,#92480,
#92481,#92482,#92483,#92484,#92485,#92486,#92487,#92488,#92489,#92490,#92491,
#92492,#92493,#92494,#92495,#92496,#92497),.UNSPECIFIED.,.F.,.F.,(4,3,3,
3,3,3,3,4),(-242.853972092955,-241.863092549649,-240.863658282915,-239.864224016181,
-238.864789749447,-237.865355482713,-236.865921215979,-236.570786785775),
 .UNSPECIFIED.);
#2084=B_SPLINE_CURVE_WITH_KNOTS('',3,(#92498,#92499,#92500,#92501,#92502,
#92503,#92504,#92505,#92506,#92507,#92508,#92509,#92510,#92511,#92512,#92513,
#92514,#92515,#92516,#92517,#92518,#92519),.UNSPECIFIED.,.F.,.F.,(4,3,3,
3,3,3,3,4),(233.595156774013,233.919612352393,234.919268815437,235.918925278481,
236.918581741526,237.91823820457,238.917894667615,239.878342081193),
 .UNSPECIFIED.);
#2085=B_SPLINE_CURVE_WITH_KNOTS('',3,(#92524,#92525,#92526,#92527,#92528,
#92529,#92530,#92531,#92532,#92533,#92534,#92535,#92536,#92537,#92538,#92539,
#92540,#92541,#92542,#92543,#92544,#92545,#92546,#92547,#92548),
 .UNSPECIFIED.,.F.,.F.,(4,3,3,3,3,3,3,3,4),(-249.137157400134,-248.859132416788,
-247.859698150054,-246.86026388332,-245.860829616586,-244.861395349852,
-243.861961083118,-242.862526816383,-242.853972092955),.UNSPECIFIED.);
#2086=B_SPLINE_CURVE_WITH_KNOTS('',3,(#92549,#92550,#92551,#92552,#92553,
#92554,#92555,#92556,#92557,#92558,#92559,#92560,#92561,#92562,#92563,#92564,
#92565,#92566,#92567,#92568,#92569,#92570,#92571,#92572,#92573),
 .UNSPECIFIED.,.F.,.F.,(4,3,3,3,3,3,3,3,4),(239.878342081193,239.917551130659,
240.917207593703,241.916864056748,242.916520519792,243.916176982837,244.915833445881,
245.915489908926,246.161527388373),.UNSPECIFIED.);
#2087=B_SPLINE_CURVE_WITH_KNOTS('',3,(#92578,#92579,#92580,#92581,#92582,
#92583,#92584,#92585,#92586,#92587,#92588,#92589,#92590,#92591,#92592,#92593,
#92594,#92595,#92596,#92597,#92598,#92599),.UNSPECIFIED.,.F.,.F.,(4,3,3,
3,3,3,3,4),(-255.420342707314,-254.855738017193,-253.856303750458,-252.856869483724,
-251.85743521699,-250.858000950256,-249.858566683522,-249.137157400134),
 .UNSPECIFIED.);
#2088=B_SPLINE_CURVE_WITH_KNOTS('',3,(#92600,#92601,#92602,#92603,#92604,
#92605,#92606,#92607,#92608,#92609,#92610,#92611,#92612,#92613,#92614,#92615,
#92616,#92617,#92618,#92619,#92620,#92621),.UNSPECIFIED.,.F.,.F.,(4,3,3,
3,3,3,3,4),(246.161527388373,246.91514637197,247.914802835014,248.914459298059,
249.914115761103,250.913772224148,251.913428687192,252.444712695552),
 .UNSPECIFIED.);
#2089=B_SPLINE_CURVE_WITH_KNOTS('',3,(#92626,#92627,#92628,#92629,#92630,
#92631,#92632,#92633,#92634,#92635,#92636,#92637,#92638,#92639,#92640,#92641,
#92642,#92643,#92644,#92645,#92646,#92647),.UNSPECIFIED.,.F.,.F.,(4,3,3,
3,3,3,3,4),(-261.703528014493,-260.852343617597,-259.852909350863,-258.853475084129,
-257.854040817395,-256.854606550661,-255.855172283927,-255.420342707314),
 .UNSPECIFIED.);
#2090=B_SPLINE_CURVE_WITH_KNOTS('',3,(#92648,#92649,#92650,#92651,#92652,
#92653,#92654,#92655,#92656,#92657,#92658,#92659,#92660,#92661,#92662,#92663,
#92664,#92665,#92666,#92667,#92668,#92669),.UNSPECIFIED.,.F.,.F.,(4,3,3,
3,3,3,3,4),(252.444712695552,252.913085150236,253.912741613281,254.912398076325,
255.91205453937,256.911711002414,257.911367465458,258.727898002732),
 .UNSPECIFIED.);
#2091=B_SPLINE_CURVE_WITH_KNOTS('',3,(#92674,#92675,#92676,#92677,#92678,
#92679,#92680,#92681,#92682,#92683,#92684,#92685,#92686,#92687,#92688,#92689,
#92690,#92691,#92692,#92693,#92694,#92695,#92696,#92697,#92698),
 .UNSPECIFIED.,.F.,.F.,(4,3,3,3,3,3,3,3,4),(-267.986713321673,-267.848383484736,
-266.848949218002,-265.849514951268,-264.850080684533,-263.850646417799,
-262.851212151065,-261.851777884331,-261.703528014493),.UNSPECIFIED.);
#2092=B_SPLINE_CURVE_WITH_KNOTS('',3,(#92699,#92700,#92701,#92702,#92703,
#92704,#92705,#92706,#92707,#92708,#92709,#92710,#92711,#92712,#92713,#92714,
#92715,#92716,#92717,#92718,#92719,#92720,#92721,#92722,#92723),
 .UNSPECIFIED.,.F.,.F.,(4,3,3,3,3,3,3,3,4),(258.727898002732,258.911023928503,
259.910680391547,260.910336854592,261.909993317636,262.909649780681,263.909306243725,
264.908962706769,265.011083309911),.UNSPECIFIED.);
#2093=B_SPLINE_CURVE_WITH_KNOTS('',3,(#92728,#92729,#92730,#92731,#92732,
#92733,#92734,#92735,#92736,#92737,#92738,#92739,#92740,#92741,#92742,#92743,
#92744,#92745,#92746,#92747,#92748,#92749),.UNSPECIFIED.,.F.,.F.,(4,3,3,
3,3,3,3,4),(-274.269898628852,-273.84498908514,-272.845554818406,-271.846120551672,
-270.846686284938,-269.847252018204,-268.84781775147,-267.986713321673),
 .UNSPECIFIED.);
#2094=B_SPLINE_CURVE_WITH_KNOTS('',3,(#92750,#92751,#92752,#92753,#92754,
#92755,#92756,#92757,#92758,#92759,#92760,#92761,#92762,#92763,#92764,#92765,
#92766,#92767,#92768,#92769,#92770,#92771),.UNSPECIFIED.,.F.,.F.,(4,3,3,
3,3,3,3,4),(265.011083309911,265.908619169814,266.908275632858,267.907932095903,
268.907588558947,269.907245021991,270.906901485036,271.294268617091),
 .UNSPECIFIED.);
#2095=B_SPLINE_CURVE_WITH_KNOTS('',3,(#92776,#92777,#92778,#92779,#92780,
#92781,#92782,#92783,#92784,#92785,#92786,#92787,#92788,#92789,#92790,#92791,
#92792,#92793,#92794,#92795,#92796,#92797),.UNSPECIFIED.,.F.,.F.,(4,3,3,
3,3,3,3,4),(-280.553083936032,-279.841594685545,-278.842160418811,-277.842726152076,
-276.843291885342,-275.843857618608,-274.844423351874,-274.269898628852),
 .UNSPECIFIED.);
#2096=B_SPLINE_CURVE_WITH_KNOTS('',3,(#92798,#92799,#92800,#92801,#92802,
#92803,#92804,#92805,#92806,#92807,#92808,#92809,#92810,#92811,#92812,#92813,
#92814,#92815,#92816,#92817,#92818,#92819),.UNSPECIFIED.,.F.,.F.,(4,3,3,
3,3,3,3,4),(271.294268617091,271.90655794808,272.906214411125,273.905870874169,
274.905527337214,275.905183800258,276.904840263302,277.57745392427),
 .UNSPECIFIED.);
#2097=B_SPLINE_CURVE_WITH_KNOTS('',3,(#92824,#92825,#92826,#92827,#92828,
#92829,#92830,#92831,#92832,#92833,#92834,#92835,#92836,#92837,#92838,#92839,
#92840,#92841,#92842,#92843,#92844,#92845),.UNSPECIFIED.,.F.,.F.,(4,3,3,
3,3,3,3,4),(-286.836269243212,-285.838200285949,-284.838766019215,-283.839331752481,
-282.839897485747,-281.840463219013,-280.841028952279,-280.553083936032),
 .UNSPECIFIED.);
#2098=B_SPLINE_CURVE_WITH_KNOTS('',3,(#92846,#92847,#92848,#92849,#92850,
#92851,#92852,#92853,#92854,#92855,#92856,#92857,#92858,#92859,#92860,#92861,
#92862,#92863,#92864,#92865,#92866,#92867),.UNSPECIFIED.,.F.,.F.,(4,3,3,
3,3,3,3,4),(277.57745392427,277.904496726347,278.904153189391,279.903809652436,
280.90346611548,281.903122578524,282.902779041569,283.86063923145),
 .UNSPECIFIED.);
#2099=B_SPLINE_CURVE_WITH_KNOTS('',3,(#92872,#92873,#92874,#92875,#92876,
#92877,#92878,#92879,#92880,#92881,#92882,#92883,#92884,#92885,#92886,#92887,
#92888,#92889,#92890,#92891,#92892,#92893),.UNSPECIFIED.,.F.,.F.,(4,3,3,
3,3,3,3,4),(-293.119454550391,-292.834240153088,-291.834805886354,-290.83537161962,
-289.835937352886,-288.836503086152,-287.837068819417,-286.836269243212),
 .UNSPECIFIED.);
#2100=B_SPLINE_CURVE_WITH_KNOTS('',3,(#92894,#92895,#92896,#92897,#92898,
#92899,#92900,#92901,#92902,#92903,#92904,#92905,#92906,#92907,#92908,#92909,
#92910,#92911,#92912,#92913,#92914,#92915,#92916,#92917,#92918),
 .UNSPECIFIED.,.F.,.F.,(4,3,3,3,3,3,3,3,4),(283.86063923145,283.902435504613,
284.902091967658,285.901748430702,286.901404893746,287.901061356791,288.900717819835,
289.90037428288,290.14382453863),.UNSPECIFIED.);
#2101=B_SPLINE_CURVE_WITH_KNOTS('',3,(#92923,#92924,#92925,#92926,#92927,
#92928,#92929,#92930,#92931,#92932,#92933,#92934,#92935,#92936,#92937,#92938,
#92939,#92940,#92941,#92942,#92943,#92944),.UNSPECIFIED.,.F.,.F.,(4,3,3,
3,3,3,3,4),(-299.402639857571,-298.830845753492,-297.831411486758,-296.831977220024,
-295.83254295329,-294.833108686556,-293.833674419822,-293.119454550391),
 .UNSPECIFIED.);
#2102=B_SPLINE_CURVE_WITH_KNOTS('',3,(#92945,#92946,#92947,#92948,#92949,
#92950,#92951,#92952,#92953,#92954,#92955,#92956,#92957,#92958,#92959,#92960,
#92961,#92962,#92963,#92964,#92965,#92966),.UNSPECIFIED.,.F.,.F.,(4,3,3,
3,3,3,3,4),(290.14382453863,290.900030745924,291.899687208968,292.899343672013,
293.899000135057,294.898656598102,295.898313061146,296.427009845809),
 .UNSPECIFIED.);
#2103=B_SPLINE_CURVE_WITH_KNOTS('',3,(#92971,#92972,#92973,#92974,#92975,
#92976,#92977,#92978,#92979,#92980,#92981,#92982,#92983,#92984,#92985,#92986,
#92987,#92988,#92989,#92990,#92991,#92992),.UNSPECIFIED.,.F.,.F.,(4,3,3,
3,3,3,3,4),(-305.68582516475,-304.827451353897,-303.828017087163,-302.828582820429,
-301.829148553695,-300.829714286961,-299.830280020226,-299.402639857571),
 .UNSPECIFIED.);
#2104=B_SPLINE_CURVE_WITH_KNOTS('',3,(#92993,#92994,#92995,#92996,#92997,
#92998,#92999,#93000,#93001,#93002,#93003,#93004,#93005,#93006,#93007,#93008,
#93009,#93010,#93011,#93012,#93013,#93014),.UNSPECIFIED.,.F.,.F.,(4,3,3,
3,3,3,3,4),(296.427009845809,296.897969524191,297.897625987235,298.897282450279,
299.896938913324,300.896595376368,301.896251839413,302.710195152989),
 .UNSPECIFIED.);
#2105=B_SPLINE_CURVE_WITH_KNOTS('',3,(#93020,#93021,#93022,#93023,#93024,
#93025,#93026,#93027,#93028,#93029),.UNSPECIFIED.,.F.,.F.,(4,1,1,1,1,1,
1,4),(317.300858012569,317.44191846845,318.441352735184,319.440787001918,
320.440221268652,321.439655535386,322.43908980212,323.438524068854),
 .UNSPECIFIED.);
#2106=B_SPLINE_CURVE_WITH_KNOTS('',3,(#93032,#93033,#93034,#93035,#93036,
#93037,#93038,#93039),.UNSPECIFIED.,.F.,.F.,(4,1,1,1,1,4),(317.300858012569,
318.200981096169,319.200637559214,320.200294022258,321.199950485303,322.199606948347),
 .UNSPECIFIED.);
#2107=B_SPLINE_CURVE_WITH_KNOTS('',3,(#93044,#93045,#93046,#93047,#93048,
#93049,#93050,#93051,#93052,#93053),.UNSPECIFIED.,.F.,.F.,(4,1,1,1,1,1,
1,4),(311.017672705389,311.445312868045,312.444747134779,313.444181401514,
314.443615668248,315.443049934982,316.442484201716,317.300858012569),
 .UNSPECIFIED.);
#2108=B_SPLINE_CURVE_WITH_KNOTS('',3,(#93054,#93055,#93056,#93057,#93058,
#93059,#93060,#93061,#93062,#93063,#93064),.UNSPECIFIED.,.F.,.F.,(4,1,1,
1,1,1,1,1,4),(311.017672705389,311.203385854859,312.203042317903,313.202698780947,
314.202355243992,315.202011707036,316.201668170081,317.201324633125,317.300858012569),
 .UNSPECIFIED.);
#2109=B_SPLINE_CURVE_WITH_KNOTS('',3,(#93069,#93070,#93071,#93072,#93073,
#93074,#93075,#93076,#93077,#93078),.UNSPECIFIED.,.F.,.F.,(4,1,1,1,1,1,
1,4),(304.73448739821,305.448707267641,306.448141534375,307.447575801109,
308.447010067843,309.446444334577,310.445878601311,311.017672705389),
 .UNSPECIFIED.);
#2110=B_SPLINE_CURVE_WITH_KNOTS('',3,(#93079,#93080,#93081,#93082,#93083,
#93084,#93085,#93086,#93087,#93088),.UNSPECIFIED.,.F.,.F.,(4,1,1,1,1,1,
1,4),(304.73448739821,305.205447076592,306.205103539637,307.204760002681,
308.204416465725,309.20407292877,310.203729391814,311.017672705389),
 .UNSPECIFIED.);
#2111=B_SPLINE_CURVE_WITH_KNOTS('',3,(#93093,#93094,#93095,#93096,#93097,
#93098,#93099,#93100,#93101,#93102,#93103),.UNSPECIFIED.,.F.,.F.,(4,1,1,
1,1,1,1,1,4),(298.45130209103,298.452667400502,299.452101667236,300.45153593397,
301.450970200704,302.450404467439,303.449838734173,304.449273000907,304.73448739821),
 .UNSPECIFIED.);
#2112=B_SPLINE_CURVE_WITH_KNOTS('',3,(#93104,#93105,#93106,#93107,#93108,
#93109,#93110,#93111,#93112,#93113),.UNSPECIFIED.,.F.,.F.,(4,1,1,1,1,1,
1,4),(298.45130209103,299.207508298326,300.20716476137,301.206821224415,
302.206477687459,303.206134150503,304.205790613548,304.73448739821),
 .UNSPECIFIED.);
#2113=B_SPLINE_CURVE_WITH_KNOTS('',3,(#93118,#93119,#93120,#93121,#93122,
#93123,#93124,#93125,#93126,#93127),.UNSPECIFIED.,.F.,.F.,(4,1,1,1,1,1,
1,4),(292.168116783851,292.456061800098,293.455496066832,294.454930333566,
295.4543646003,296.453798867034,297.453233133768,298.45130209103),
 .UNSPECIFIED.);
#2114=B_SPLINE_CURVE_WITH_KNOTS('',3,(#93128,#93129,#93130,#93131,#93132,
#93133,#93134,#93135,#93136,#93137,#93138),.UNSPECIFIED.,.F.,.F.,(4,1,1,
1,1,1,1,1,4),(292.168116783851,292.209913057015,293.209569520059,294.209225983104,
295.208882446148,296.208538909192,297.208195372237,298.207851835281,298.45130209103),
 .UNSPECIFIED.);
#2115=B_SPLINE_CURVE_WITH_KNOTS('',3,(#93143,#93144,#93145,#93146,#93147,
#93148,#93149,#93150,#93151,#93152),.UNSPECIFIED.,.F.,.F.,(4,1,1,1,1,1,
1,4),(285.884931476671,286.459456199693,287.458890466427,288.458324733161,
289.457758999895,290.45719326663,291.456627533364,292.168116783851),
 .UNSPECIFIED.);
#2116=B_SPLINE_CURVE_WITH_KNOTS('',3,(#93153,#93154,#93155,#93156,#93157,
#93158,#93159,#93160,#93161,#93162),.UNSPECIFIED.,.F.,.F.,(4,1,1,1,1,1,
1,4),(285.884931476671,286.211974278748,287.211630741793,288.211287204837,
289.210943667882,290.210600130926,291.21025659397,292.168116783851),
 .UNSPECIFIED.);
#2117=B_SPLINE_CURVE_WITH_KNOTS('',3,(#93167,#93168,#93169,#93170,#93171,
#93172,#93173,#93174,#93175,#93176),.UNSPECIFIED.,.F.,.F.,(4,1,1,1,1,1,
1,4),(279.601746169491,280.462850599289,281.462284866023,282.461719132757,
283.461153399491,284.460587666225,285.460021932959,285.884931476671),
 .UNSPECIFIED.);
#2118=B_SPLINE_CURVE_WITH_KNOTS('',3,(#93177,#93178,#93179,#93180,#93181,
#93182,#93183,#93184,#93185,#93186),.UNSPECIFIED.,.F.,.F.,(4,1,1,1,1,1,
1,4),(279.601746169492,280.214035500482,281.213691963526,282.213348426571,
283.213004889615,284.212661352659,285.212317815704,285.884931476671),
 .UNSPECIFIED.);
#2119=B_SPLINE_CURVE_WITH_KNOTS('',3,(#93191,#93192,#93193,#93194,#93195,
#93196,#93197,#93198,#93199,#93200,#93201),.UNSPECIFIED.,.F.,.F.,(4,1,1,
1,1,1,1,1,4),(273.318560862312,273.46681073215,274.466244998884,275.465679265618,
276.465113532352,277.464547799086,278.46398206582,279.463416332555,279.601746169491),
 .UNSPECIFIED.);
#2120=B_SPLINE_CURVE_WITH_KNOTS('',3,(#93202,#93203,#93204,#93205,#93206,
#93207,#93208,#93209,#93210,#93211),.UNSPECIFIED.,.F.,.F.,(4,1,1,1,1,1,
1,4),(273.318560862312,274.216096722215,275.21575318526,276.215409648304,
277.215066111349,278.214722574393,279.214379037437,279.601746169492),
 .UNSPECIFIED.);
#2121=B_SPLINE_CURVE_WITH_KNOTS('',3,(#93216,#93217,#93218,#93219,#93220,
#93221,#93222,#93223,#93224,#93225),.UNSPECIFIED.,.F.,.F.,(4,1,1,1,1,1,
1,4),(267.035375555132,267.470205131746,268.46963939848,269.469073665214,
270.468507931948,271.467942198682,272.467376465416,273.318560862312),
 .UNSPECIFIED.);
#2122=B_SPLINE_CURVE_WITH_KNOTS('',3,(#93226,#93227,#93228,#93229,#93230,
#93231,#93232,#93233,#93234,#93235,#93236),.UNSPECIFIED.,.F.,.F.,(4,1,1,
1,1,1,1,1,4),(267.035375555133,267.218501480904,268.218157943949,269.217814406993,
270.217470870038,271.217127333082,272.216783796126,273.216440259171,273.318560862312),
 .UNSPECIFIED.);
#2123=B_SPLINE_CURVE_WITH_KNOTS('',3,(#93241,#93242,#93243,#93244,#93245,
#93246,#93247,#93248,#93249,#93250),.UNSPECIFIED.,.F.,.F.,(4,1,1,1,1,1,
1,4),(260.752190247953,261.473599531341,262.473033798075,263.472468064809,
264.471902331543,265.471336598277,266.470770865011,267.035375555132),
 .UNSPECIFIED.);
#2124=B_SPLINE_CURVE_WITH_KNOTS('',3,(#93251,#93252,#93253,#93254,#93255,
#93256,#93257,#93258,#93259,#93260),.UNSPECIFIED.,.F.,.F.,(4,1,1,1,1,1,
1,4),(260.752190247953,261.220562702638,262.220219165682,263.219875628727,
264.219532091771,265.219188554816,266.21884501786,267.035375555133),
 .UNSPECIFIED.);
#2125=B_SPLINE_CURVE_WITH_KNOTS('',3,(#93265,#93266,#93267,#93268,#93269,
#93270,#93271,#93272,#93273,#93274,#93275),.UNSPECIFIED.,.F.,.F.,(4,1,1,
1,1,1,1,1,4),(254.469004940773,254.477559664202,255.476993930936,256.476428197671,
257.475862464405,258.475296731139,259.474730997873,260.474165264607,260.752190247953),
 .UNSPECIFIED.);
#2126=B_SPLINE_CURVE_WITH_KNOTS('',3,(#93276,#93277,#93278,#93279,#93280,
#93281,#93282,#93283,#93284,#93285),.UNSPECIFIED.,.F.,.F.,(4,1,1,1,1,1,
1,4),(254.469004940773,255.222623924372,256.222280387416,257.22193685046,
258.221593313505,259.221249776549,260.220906239594,260.752190247953),
 .UNSPECIFIED.);
#2127=B_SPLINE_CURVE_WITH_KNOTS('',3,(#93290,#93291,#93292,#93293,#93294,
#93295,#93296,#93297,#93298,#93299),.UNSPECIFIED.,.F.,.F.,(4,1,1,1,1,1,
1,4),(248.185819633594,248.480954063798,249.480388330532,250.479822597266,
251.479256864,252.478691130734,253.478125397468,254.469004940773),
 .UNSPECIFIED.);
#2128=B_SPLINE_CURVE_WITH_KNOTS('',3,(#93300,#93301,#93302,#93303,#93304,
#93305,#93306,#93307,#93308,#93309,#93310),.UNSPECIFIED.,.F.,.F.,(4,1,1,
1,1,1,1,1,4),(248.185819633594,248.225028683061,249.224685146105,250.224341609149,
251.223998072194,252.223654535238,253.223310998283,254.222967461327,254.469004940773),
 .UNSPECIFIED.);
#2129=B_SPLINE_CURVE_WITH_KNOTS('',3,(#93315,#93316,#93317,#93318,#93319,
#93320,#93321,#93322,#93323,#93324),.UNSPECIFIED.,.F.,.F.,(4,1,1,1,1,1,
1,4),(241.902634326414,242.484348463393,243.483782730127,244.483216996862,
245.482651263596,246.48208553033,247.481519797064,248.185819633594),
 .UNSPECIFIED.);
#2130=B_SPLINE_CURVE_WITH_KNOTS('',3,(#93325,#93326,#93327,#93328,#93329,
#93330,#93331,#93332,#93333,#93334),.UNSPECIFIED.,.F.,.F.,(4,1,1,1,1,1,
1,4),(241.902634326414,242.227089904794,243.226746367839,244.226402830883,
245.226059293927,246.225715756972,247.225372220016,248.185819633594),
 .UNSPECIFIED.);
#2131=B_SPLINE_CURVE_WITH_KNOTS('',3,(#93339,#93340,#93341,#93342,#93343,
#93344,#93345,#93346,#93347,#93348),.UNSPECIFIED.,.F.,.F.,(4,1,1,1,1,1,
1,4),(235.619449019235,236.487742862989,237.487177129723,238.486611396457,
239.486045663191,240.485479929925,241.484914196659,241.902634326414),
 .UNSPECIFIED.);
#2132=B_SPLINE_CURVE_WITH_KNOTS('',3,(#93349,#93350,#93351,#93352,#93353,
#93354,#93355,#93356,#93357,#93358),.UNSPECIFIED.,.F.,.F.,(4,1,1,1,1,1,
1,4),(235.619449019235,236.229151126528,237.228807589572,238.228464052616,
239.228120515661,240.227776978705,241.22743344175,241.902634326414),
 .UNSPECIFIED.);
#2133=B_SPLINE_CURVE_WITH_KNOTS('',3,(#93363,#93364,#93365,#93366,#93367,
#93368,#93369,#93370,#93371,#93372,#93373),.UNSPECIFIED.,.F.,.F.,(4,1,1,
1,1,1,1,1,4),(229.336263712055,229.49170299585,230.491137262584,231.490571529318,
232.490005796052,233.489440062787,234.488874329521,235.488308596255,235.619449019235),
 .UNSPECIFIED.);
#2134=B_SPLINE_CURVE_WITH_KNOTS('',3,(#93374,#93375,#93376,#93377,#93378,
#93379,#93380,#93381,#93382,#93383),.UNSPECIFIED.,.F.,.F.,(4,1,1,1,1,1,
1,4),(229.336263712055,230.231212348261,231.230868811306,232.23052527435,
233.230181737394,234.229838200439,235.229494663483,235.619449019235),
 .UNSPECIFIED.);
#2135=B_SPLINE_CURVE_WITH_KNOTS('',3,(#93388,#93389,#93390,#93391,#93392,
#93393,#93394,#93395,#93396,#93397),.UNSPECIFIED.,.F.,.F.,(4,1,1,1,1,1,
1,4),(223.053078404875,223.495097395446,224.49453166218,225.493965928914,
226.493400195648,227.492834462382,228.492268729116,229.336263712055),
 .UNSPECIFIED.);
#2136=B_SPLINE_CURVE_WITH_KNOTS('',3,(#93398,#93399,#93400,#93401,#93402,
#93403,#93404,#93405,#93406,#93407,#93408),.UNSPECIFIED.,.F.,.F.,(4,1,1,
1,1,1,1,1,4),(223.053078404876,223.23361710695,224.233273569995,225.232930033039,
226.232586496084,227.232242959128,228.231899422172,229.231555885217,229.336263712055),
 .UNSPECIFIED.);
#2137=B_SPLINE_CURVE_WITH_KNOTS('',3,(#93413,#93414,#93415,#93416,#93417,
#93418,#93419,#93420,#93421,#93422),.UNSPECIFIED.,.F.,.F.,(4,1,1,1,1,1,
1,4),(216.769893097696,217.498491795041,218.497926061775,219.497360328509,
220.496794595243,221.496228861977,222.495663128712,223.053078404875),
 .UNSPECIFIED.);
#2138=B_SPLINE_CURVE_WITH_KNOTS('',3,(#93423,#93424,#93425,#93426,#93427,
#93428,#93429,#93430,#93431,#93432),.UNSPECIFIED.,.F.,.F.,(4,1,1,1,1,1,
1,4),(216.769893097696,217.235678328684,218.235334791728,219.234991254773,
220.234647717817,221.234304180861,222.233960643906,223.053078404876),
 .UNSPECIFIED.);
#2139=B_SPLINE_CURVE_WITH_KNOTS('',3,(#93437,#93438,#93439,#93440,#93441,
#93442,#93443,#93444,#93445,#93446,#93447),.UNSPECIFIED.,.F.,.F.,(4,1,1,
1,1,1,1,1,4),(210.486707790516,210.502451927902,211.501886194637,212.501320461371,
213.500754728105,214.500188994839,215.499623261573,216.499057528307,216.769893097696),
 .UNSPECIFIED.);
#2140=B_SPLINE_CURVE_WITH_KNOTS('',3,(#93448,#93449,#93450,#93451,#93452,
#93453,#93454,#93455,#93456,#93457),.UNSPECIFIED.,.F.,.F.,(4,1,1,1,1,1,
1,4),(210.486707790517,211.237739550417,212.237396013462,213.237052476506,
214.236708939551,215.236365402595,216.236021865639,216.769893097696),
 .UNSPECIFIED.);
#2141=B_SPLINE_CURVE_WITH_KNOTS('',3,(#93462,#93463,#93464,#93465,#93466,
#93467,#93468,#93469,#93470,#93471),.UNSPECIFIED.,.F.,.F.,(4,1,1,1,1,1,
1,4),(204.203522483337,204.505846327498,205.505280594232,206.504714860966,
207.5041491277,208.503583394434,209.503017661168,210.486707790516),
 .UNSPECIFIED.);
#2142=B_SPLINE_CURVE_WITH_KNOTS('',3,(#93472,#93473,#93474,#93475,#93476,
#93477,#93478,#93479,#93480,#93481,#93482),.UNSPECIFIED.,.F.,.F.,(4,1,1,
1,1,1,1,1,4),(204.203522483337,204.240144309106,205.239800772151,206.239457235195,
207.23911369824,208.238770161284,209.238426624329,210.238083087373,210.486707790517),
 .UNSPECIFIED.);
#2143=B_SPLINE_CURVE_WITH_KNOTS('',3,(#93487,#93488,#93489,#93490,#93491,
#93492,#93493,#93494,#93495,#93496),.UNSPECIFIED.,.F.,.F.,(4,1,1,1,1,1,
1,4),(197.920337176157,198.509240727093,199.508674993828,200.508109260562,
201.507543527296,202.50697779403,203.506412060764,204.203522483337),
 .UNSPECIFIED.);
#2144=B_SPLINE_CURVE_WITH_KNOTS('',3,(#93497,#93498,#93499,#93500,#93501,
#93502,#93503,#93504,#93505,#93506),.UNSPECIFIED.,.F.,.F.,(4,1,1,1,1,1,
1,4),(197.920337176157,198.24220553084,199.241861993884,200.241518456929,
201.241174919973,202.240831383018,203.240487846062,204.203522483337),
 .UNSPECIFIED.);
#2145=B_SPLINE_CURVE_WITH_KNOTS('',3,(#93511,#93512,#93513,#93514,#93515,
#93516,#93517,#93518,#93519,#93520),.UNSPECIFIED.,.F.,.F.,(4,1,1,1,1,1,
1,4),(191.637151868978,192.512635126689,193.512069393423,194.511503660157,
195.510937926891,196.510372193625,197.509806460359,197.920337176157),
 .UNSPECIFIED.);
#2146=B_SPLINE_CURVE_WITH_KNOTS('',3,(#93521,#93522,#93523,#93524,#93525,
#93526,#93527,#93528,#93529,#93530),.UNSPECIFIED.,.F.,.F.,(4,1,1,1,1,1,
1,4),(191.637151868978,192.244266752574,193.243923215618,194.243579678662,
195.243236141707,196.242892604751,197.242549067796,197.920337176157),
 .UNSPECIFIED.);
#2147=B_SPLINE_CURVE_WITH_KNOTS('',3,(#93535,#93536,#93537,#93538,#93539,
#93540,#93541,#93542,#93543,#93544,#93545),.UNSPECIFIED.,.F.,.F.,(4,1,1,
1,1,1,1,1,4),(185.353966561798,185.51659525955,186.516029526284,187.515463793018,
188.514898059753,189.514332326487,190.513766593221,191.513200859955,191.637151868978),
 .UNSPECIFIED.);
#2148=B_SPLINE_CURVE_WITH_KNOTS('',3,(#93546,#93547,#93548,#93549,#93550,
#93551,#93552,#93553,#93554,#93555),.UNSPECIFIED.,.F.,.F.,(4,1,1,1,1,1,
1,4),(185.353966561798,186.246327974307,187.245984437351,188.245640900396,
189.24529736344,190.244953826485,191.244610289529,191.637151868978),
 .UNSPECIFIED.);
#2149=B_SPLINE_CURVE_WITH_KNOTS('',3,(#93560,#93561,#93562,#93563,#93564,
#93565,#93566,#93567,#93568,#93569),.UNSPECIFIED.,.F.,.F.,(4,1,1,1,1,1,
1,4),(179.070781254618,179.519989659146,180.51942392588,181.518858192614,
182.518292459348,183.517726726082,184.517160992816,185.353966561798),
 .UNSPECIFIED.);
#2150=B_SPLINE_CURVE_WITH_KNOTS('',3,(#93570,#93571,#93572,#93573,#93574,
#93575,#93576,#93577,#93578,#93579,#93580),.UNSPECIFIED.,.F.,.F.,(4,1,1,
1,1,1,1,1,4),(179.070781254619,179.248732732996,180.248389196041,181.248045659085,
182.247702122129,183.247358585174,184.247015048218,185.246671511263,185.353966561798),
 .UNSPECIFIED.);
#2151=B_SPLINE_CURVE_WITH_KNOTS('',3,(#93585,#93586,#93587,#93588,#93589,
#93590,#93591,#93592,#93593,#93594),.UNSPECIFIED.,.F.,.F.,(4,1,1,1,1,1,
1,4),(172.787595947439,173.523384058741,174.522818325475,175.522252592209,
176.521686858943,177.521121125678,178.520555392412,179.070781254618),
 .UNSPECIFIED.);
#2152=B_SPLINE_CURVE_WITH_KNOTS('',3,(#93595,#93596,#93597,#93598,#93599,
#93600,#93601,#93602,#93603,#93604),.UNSPECIFIED.,.F.,.F.,(4,1,1,1,1,1,
1,4),(172.787595947439,173.25079395473,174.250450417774,175.250106880818,
176.249763343863,177.249419806907,178.249076269952,179.070781254619),
 .UNSPECIFIED.);
#2153=B_SPLINE_CURVE_WITH_KNOTS('',3,(#93609,#93610,#93611,#93612,#93613,
#93614,#93615,#93616,#93617,#93618,#93619),.UNSPECIFIED.,.F.,.F.,(4,1,1,
1,1,1,1,1,4),(166.504410640259,166.527344191603,167.526778458337,168.526212725071,
169.525646991805,170.525081258539,171.524515525273,172.523949792007,172.787595947439),
 .UNSPECIFIED.);
#2154=B_SPLINE_CURVE_WITH_KNOTS('',3,(#93620,#93621,#93622,#93623,#93624,
#93625,#93626,#93627,#93628,#93629),.UNSPECIFIED.,.F.,.F.,(4,1,1,1,1,1,
1,4),(166.50441064026,167.252855176463,168.252511639508,169.252168102552,
170.251824565596,171.251481028641,172.251137491685,172.787595947439),
 .UNSPECIFIED.);
#2155=B_SPLINE_CURVE_WITH_KNOTS('',3,(#93634,#93635,#93636,#93637,#93638,
#93639,#93640,#93641,#93642,#93643),.UNSPECIFIED.,.F.,.F.,(4,1,1,1,1,1,
1,4),(160.22122533308,160.530738591198,161.530172857932,162.529607124666,
163.5290413914,164.528475658134,165.527909924869,166.504410640259),
 .UNSPECIFIED.);
#2156=B_SPLINE_CURVE_WITH_KNOTS('',3,(#93644,#93645,#93646,#93647,#93648,
#93649,#93650,#93651,#93652,#93653,#93654),.UNSPECIFIED.,.F.,.F.,(4,1,1,
1,1,1,1,1,4),(160.22122533308,160.255259935152,161.254916398197,162.254572861241,
163.254229324286,164.25388578733,165.253542250374,166.253198713419,166.50441064026),
 .UNSPECIFIED.);
#2157=B_SPLINE_CURVE_WITH_KNOTS('',3,(#93659,#93660,#93661,#93662,#93663,
#93664,#93665,#93666,#93667,#93668),.UNSPECIFIED.,.F.,.F.,(4,1,1,1,1,1,
1,4),(153.9380400259,154.534132990794,155.533567257528,156.533001524262,
157.532435790996,158.53187005773,159.531304324464,160.22122533308),
 .UNSPECIFIED.);
#2158=B_SPLINE_CURVE_WITH_KNOTS('',3,(#93669,#93670,#93671,#93672,#93673,
#93674,#93675,#93676,#93677,#93678),.UNSPECIFIED.,.F.,.F.,(4,1,1,1,1,1,
1,4),(153.9380400259,154.257321156886,155.25697761993,156.256634082975,
157.256290546019,158.255947009063,159.255603472108,160.22122533308),
 .UNSPECIFIED.);
#2159=B_SPLINE_CURVE_WITH_KNOTS('',3,(#93683,#93684,#93685,#93686,#93687,
#93688,#93689,#93690,#93691,#93692),.UNSPECIFIED.,.F.,.F.,(4,1,1,1,1,1,
1,4),(147.654854718721,148.537527390389,149.536961657123,150.536395923857,
151.535830190591,152.535264457325,153.534698724059,153.9380400259),
 .UNSPECIFIED.);
#2160=B_SPLINE_CURVE_WITH_KNOTS('',3,(#93693,#93694,#93695,#93696,#93697,
#93698,#93699,#93700,#93701,#93702),.UNSPECIFIED.,.F.,.F.,(4,1,1,1,1,1,
1,4),(147.654854718721,148.259382378619,149.259038841664,150.258695304708,
151.258351767753,152.258008230797,153.257664693841,153.9380400259),
 .UNSPECIFIED.);
#2161=B_SPLINE_CURVE_WITH_KNOTS('',3,(#93707,#93708,#93709,#93710,#93711,
#93712,#93713,#93714,#93715,#93716,#93717),.UNSPECIFIED.,.F.,.F.,(4,1,1,
1,1,1,1,1,4),(141.371669411541,141.54148752325,142.540921789984,143.540356056719,
144.539790323453,145.539224590187,146.538658856921,147.538093123655,147.654854718721),
 .UNSPECIFIED.);
#2162=B_SPLINE_CURVE_WITH_KNOTS('',3,(#93718,#93719,#93720,#93721,#93722,
#93723,#93724,#93725,#93726,#93727),.UNSPECIFIED.,.F.,.F.,(4,1,1,1,1,1,
1,4),(141.371669411541,142.261443600353,143.261100063397,144.260756526442,
145.260412989486,146.260069452531,147.259725915575,147.654854718721),
 .UNSPECIFIED.);
#2163=B_SPLINE_CURVE_WITH_KNOTS('',3,(#93732,#93733,#93734,#93735,#93736,
#93737,#93738,#93739,#93740,#93741),.UNSPECIFIED.,.F.,.F.,(4,1,1,1,1,1,
1,4),(135.088484104362,135.544881922846,136.54431618958,137.543750456314,
138.543184723048,139.542618989782,140.542053256516,141.371669411541),
 .UNSPECIFIED.);
#2164=B_SPLINE_CURVE_WITH_KNOTS('',3,(#93742,#93743,#93744,#93745,#93746,
#93747,#93748,#93749,#93750,#93751,#93752),.UNSPECIFIED.,.F.,.F.,(4,1,1,
1,1,1,1,1,4),(135.088484104362,135.263848359042,136.263504822086,137.263161285131,
138.262817748175,139.26247421122,140.262130674264,141.261787137308,141.371669411541),
 .UNSPECIFIED.);
#2165=B_SPLINE_CURVE_WITH_KNOTS('',3,(#93757,#93758,#93759,#93760,#93761,
#93762,#93763,#93764,#93765,#93766),.UNSPECIFIED.,.F.,.F.,(4,1,1,1,1,1,
1,4),(128.805298797182,129.548276322441,130.547710589175,131.54714485591,
132.546579122644,133.546013389378,134.545447656112,135.088484104362),
 .UNSPECIFIED.);
#2166=B_SPLINE_CURVE_WITH_KNOTS('',3,(#93767,#93768,#93769,#93770,#93771,
#93772,#93773,#93774,#93775,#93776),.UNSPECIFIED.,.F.,.F.,(4,1,1,1,1,1,
1,4),(128.805298797182,129.265909580775,130.26556604382,131.265222506864,
132.264878969909,133.264535432953,134.264191895998,135.088484104362),
 .UNSPECIFIED.);
#2167=B_SPLINE_CURVE_WITH_KNOTS('',3,(#93781,#93782,#93783,#93784,#93785,
#93786,#93787,#93788,#93789,#93790,#93791),.UNSPECIFIED.,.F.,.F.,(4,1,1,
1,1,1,1,1,4),(122.522113490002,122.552236455303,123.551670722037,124.551104988771,
125.550539255505,126.549973522239,127.549407788973,128.548842055707,128.805298797182),
 .UNSPECIFIED.);
#2168=B_SPLINE_CURVE_WITH_KNOTS('',3,(#93792,#93793,#93794,#93795,#93796,
#93797,#93798,#93799,#93800,#93801),.UNSPECIFIED.,.F.,.F.,(4,1,1,1,1,1,
1,4),(122.522113490003,123.267970802509,124.267627265553,125.267283728598,
126.266940191642,127.266596654687,128.266253117731,128.805298797182),
 .UNSPECIFIED.);
#2169=B_SPLINE_CURVE_WITH_KNOTS('',3,(#93806,#93807,#93808,#93809,#93810,
#93811,#93812,#93813,#93814,#93815),.UNSPECIFIED.,.F.,.F.,(4,1,1,1,1,1,
1,4),(116.238928182823,116.555630854898,117.555065121632,118.554499388366,
119.5539336551,120.553367921835,121.552802188569,122.522113490002),
 .UNSPECIFIED.);
#2170=B_SPLINE_CURVE_WITH_KNOTS('',3,(#93816,#93817,#93818,#93819,#93820,
#93821,#93822,#93823,#93824,#93825,#93826),.UNSPECIFIED.,.F.,.F.,(4,1,1,
1,1,1,1,1,4),(116.238928182823,116.270375561198,117.270032024243,118.269688487287,
119.269344950331,120.269001413376,121.26865787642,122.268314339465,122.522113490003),
 .UNSPECIFIED.);
#2171=B_SPLINE_CURVE_WITH_KNOTS('',3,(#93831,#93832,#93833,#93834,#93835,
#93836,#93837,#93838,#93839,#93840),.UNSPECIFIED.,.F.,.F.,(4,1,1,1,1,1,
1,4),(109.955742875643,110.559025254494,111.558459521228,112.557893787962,
113.557328054696,114.55676232143,115.556196588164,116.238928182823),
 .UNSPECIFIED.);
#2172=B_SPLINE_CURVE_WITH_KNOTS('',3,(#93841,#93842,#93843,#93844,#93845,
#93846,#93847,#93848,#93849,#93850),.UNSPECIFIED.,.F.,.F.,(4,1,1,1,1,1,
1,4),(109.955742875643,110.272436782932,111.272093245976,112.27174970902,
113.271406172065,114.271062635109,115.270719098154,116.238928182823),
 .UNSPECIFIED.);
#2173=B_SPLINE_CURVE_WITH_KNOTS('',3,(#93855,#93856,#93857,#93858,#93859,
#93860,#93861,#93862,#93863,#93864),.UNSPECIFIED.,.F.,.F.,(4,1,1,1,1,1,
1,4),(103.672557568464,104.562419654089,105.561853920823,106.561288187557,
107.560722454291,108.560156721025,109.55959098776,109.955742875643),
 .UNSPECIFIED.);
#2174=B_SPLINE_CURVE_WITH_KNOTS('',3,(#93865,#93866,#93867,#93868,#93869,
#93870,#93871,#93872,#93873,#93874),.UNSPECIFIED.,.F.,.F.,(4,1,1,1,1,1,
1,4),(103.672557568464,104.274498004665,105.27415446771,106.273810930754,
107.273467393798,108.273123856843,109.272780319887,109.955742875643),
 .UNSPECIFIED.);
#2175=B_SPLINE_CURVE_WITH_KNOTS('',3,(#93879,#93880,#93881,#93882,#93883,
#93884,#93885,#93886,#93887,#93888,#93889),.UNSPECIFIED.,.F.,.F.,(4,1,1,
1,1,1,1,1,4),(97.389372261284,97.5663797869505,98.5658140536846,99.5652483204187,
100.564682587153,101.564116853887,102.563551120621,103.562985387355,103.672557568464),
 .UNSPECIFIED.);
#2176=B_SPLINE_CURVE_WITH_KNOTS('',3,(#93890,#93891,#93892,#93893,#93894,
#93895,#93896,#93897,#93898,#93899),.UNSPECIFIED.,.F.,.F.,(4,1,1,1,1,1,
1,4),(97.3893722612842,98.2765592263987,99.2762156894431,100.275872152488,
101.275528615532,102.275185078576,103.274841541621,103.672557568464),
 .UNSPECIFIED.);
#2177=B_SPLINE_CURVE_WITH_KNOTS('',3,(#93904,#93905,#93906,#93907,#93908,
#93909,#93910,#93911,#93912,#93913),.UNSPECIFIED.,.F.,.F.,(4,1,1,1,1,1,
1,4),(91.1061869541044,91.569774186546,92.5692084532801,93.5686427200142,
94.5680769867483,95.5675112534823,96.5669455202164,97.389372261284),
 .UNSPECIFIED.);
#2178=B_SPLINE_CURVE_WITH_KNOTS('',3,(#93914,#93915,#93916,#93917,#93918,
#93919,#93920,#93921,#93922,#93923,#93924),.UNSPECIFIED.,.F.,.F.,(4,1,1,
1,1,1,1,1,4),(91.1061869541046,91.2789639850878,92.2786204481322,93.2782769111766,
94.277933374221,95.2775898372655,96.2772463003099,97.2769027633543,97.3893722612842),
 .UNSPECIFIED.);
#2179=B_SPLINE_CURVE_WITH_KNOTS('',3,(#93929,#93930,#93931,#93932,#93933,
#93934,#93935,#93936,#93937,#93938),.UNSPECIFIED.,.F.,.F.,(4,1,1,1,1,1,
1,4),(84.8230016469248,85.5731685861415,86.5726028528755,87.5720371196096,
88.5714713863437,89.5709056530778,90.5703399198119,91.1061869541044),
 .UNSPECIFIED.);
#2180=B_SPLINE_CURVE_WITH_KNOTS('',3,(#93939,#93940,#93941,#93942,#93943,
#93944,#93945,#93946,#93947,#93948),.UNSPECIFIED.,.F.,.F.,(4,1,1,1,1,1,
1,4),(84.823001646925,85.2810252068213,86.2806816698657,87.2803381329102,
88.2799945959546,89.279651058999,90.2793075220434,91.1061869541046),
 .UNSPECIFIED.);
#2181=B_SPLINE_CURVE_WITH_KNOTS('',3,(#93953,#93954,#93955,#93956,#93957,
#93958,#93959,#93960,#93961,#93962,#93963),.UNSPECIFIED.,.F.,.F.,(4,1,1,
1,1,1,1,1,4),(78.5398163397452,78.5771287190028,79.5765629857369,80.575997252471,
81.5754315192051,82.5748657859392,83.5743000526733,84.5737343194074,84.8230016469248),
 .UNSPECIFIED.);
#2182=B_SPLINE_CURVE_WITH_KNOTS('',3,(#93964,#93965,#93966,#93967,#93968,
#93969,#93970,#93971,#93972,#93973),.UNSPECIFIED.,.F.,.F.,(4,1,1,1,1,1,
1,4),(78.5398163397454,79.2830864285549,80.2827428915993,81.2823993546437,
82.2820558176881,83.2817122807325,84.2813687437769,84.823001646925),
 .UNSPECIFIED.);
#2183=B_SPLINE_CURVE_WITH_KNOTS('',3,(#93978,#93979,#93980,#93981,#93982,
#93983,#93984,#93985,#93986,#93987),.UNSPECIFIED.,.F.,.F.,(4,1,1,1,1,1,
1,4),(72.2566310325657,72.5805231185983,73.5799573853324,74.5793916520665,
75.5788259188006,76.5782601855347,77.5776944522688,78.5398163397452),
 .UNSPECIFIED.);
#2184=B_SPLINE_CURVE_WITH_KNOTS('',3,(#93988,#93989,#93990,#93991,#93992,
#93993,#93994,#93995,#93996,#93997,#93998),.UNSPECIFIED.,.F.,.F.,(4,1,1,
1,1,1,1,1,4),(72.2566310325658,72.285491187244,73.2851476502884,74.2848041133328,
75.2844605763772,76.2841170394216,77.283773502466,78.2834299655104,78.5398163397454),
 .UNSPECIFIED.);
#2185=B_SPLINE_CURVE_WITH_KNOTS('',3,(#94003,#94004,#94005,#94006,#94007,
#94008,#94009,#94010,#94011,#94012),.UNSPECIFIED.,.F.,.F.,(4,1,1,1,1,1,
1,4),(65.973445725386,66.5839175181938,67.5833517849279,68.582786051662,
69.582220318396,70.5816545851301,71.5810888518642,72.2566310325657),
 .UNSPECIFIED.);
#2186=B_SPLINE_CURVE_WITH_KNOTS('',3,(#94013,#94014,#94015,#94016,#94017,
#94018,#94019,#94020,#94021,#94022),.UNSPECIFIED.,.F.,.F.,(4,1,1,1,1,1,
1,4),(65.9734457253862,66.2875524089775,67.2872088720219,68.2868653350663,
69.2865217981107,70.2861782611551,71.2858347241996,72.2566310325658),
 .UNSPECIFIED.);
#2187=B_SPLINE_CURVE_WITH_KNOTS('',3,(#94027,#94028,#94029,#94030,#94031,
#94032,#94033,#94034,#94035,#94036),.UNSPECIFIED.,.F.,.F.,(4,1,1,1,1,1,
1,4),(59.6902604182065,60.5873119177892,61.5867461845233,62.5861804512574,
63.5856147179915,64.5850489847256,65.5844832514597,65.973445725386),
 .UNSPECIFIED.);
#2188=B_SPLINE_CURVE_WITH_KNOTS('',3,(#94037,#94038,#94039,#94040,#94041,
#94042,#94043,#94044,#94045,#94046),.UNSPECIFIED.,.F.,.F.,(4,1,1,1,1,1,
1,4),(59.6902604182066,60.289613630711,61.2892700937554,62.2889265567998,
63.2885830198443,64.2882394828887,65.2878959459331,65.9734457253862),
 .UNSPECIFIED.);
#2189=B_SPLINE_CURVE_WITH_KNOTS('',3,(#94051,#94052,#94053,#94054,#94055,
#94056,#94057,#94058,#94059,#94060,#94061),.UNSPECIFIED.,.F.,.F.,(4,1,1,
1,1,1,1,1,4),(53.4070751110269,53.5912720506506,54.5907063173847,55.5901405841188,
56.5895748508529,57.589009117587,58.5884433843211,59.5878776510552,59.6902604182065),
 .UNSPECIFIED.);
#2190=B_SPLINE_CURVE_WITH_KNOTS('',3,(#94062,#94063,#94064,#94065,#94066,
#94067,#94068,#94069,#94070,#94071),.UNSPECIFIED.,.F.,.F.,(4,1,1,1,1,1,
1,4),(53.407075111027,54.2916748524445,55.2913313154889,56.2909877785334,
57.2906442415778,58.2903007046222,59.2899571676666,59.6902604182066),
 .UNSPECIFIED.);
#2191=B_SPLINE_CURVE_WITH_KNOTS('',3,(#94076,#94077,#94078,#94079,#94080,
#94081,#94082,#94083,#94084,#94085),.UNSPECIFIED.,.F.,.F.,(4,1,1,1,1,1,
1,4),(47.1238898038473,47.5946664502461,48.5941007169802,49.5935349837143,
50.5929692504484,51.5924035171824,52.5918377839165,53.4070751110269),
 .UNSPECIFIED.);
#2192=B_SPLINE_CURVE_WITH_KNOTS('',3,(#94086,#94087,#94088,#94089,#94090,
#94091,#94092,#94093,#94094,#94095,#94096),.UNSPECIFIED.,.F.,.F.,(4,1,1,
1,1,1,1,1,4),(47.1238898038474,47.2940796111337,48.2937360741781,49.2933925372225,
50.2930490002669,51.2927054633113,52.2923619263557,53.2920183894001,53.407075111027),
 .UNSPECIFIED.);
#2193=B_SPLINE_CURVE_WITH_KNOTS('',3,(#94101,#94102,#94103,#94104,#94105,
#94106,#94107,#94108,#94109,#94110),.UNSPECIFIED.,.F.,.F.,(4,1,1,1,1,1,
1,4),(40.8407044966677,41.5980608498416,42.5974951165757,43.5969293833097,
44.5963636500438,45.5957979167779,46.595232183512,47.1238898038473),
 .UNSPECIFIED.);
#2194=B_SPLINE_CURVE_WITH_KNOTS('',3,(#94111,#94112,#94113,#94114,#94115,
#94116,#94117,#94118,#94119,#94120),.UNSPECIFIED.,.F.,.F.,(4,1,1,1,1,1,
1,4),(40.8407044966679,41.2961408328672,42.2957972959116,43.295453758956,
44.2951102220004,45.2947666850448,46.2944231480892,47.1238898038474),
 .UNSPECIFIED.);
#2195=B_SPLINE_CURVE_WITH_KNOTS('',3,(#94125,#94126,#94127,#94128,#94129,
#94130,#94131,#94132,#94133,#94134,#94135),.UNSPECIFIED.,.F.,.F.,(4,1,1,
1,1,1,1,1,4),(34.5575191894881,34.6020209827029,35.601455249437,36.6008895161711,
37.6003237829052,38.5997580496393,39.5991923163734,40.5986265831075,40.8407044966677),
 .UNSPECIFIED.);
#2196=B_SPLINE_CURVE_WITH_KNOTS('',3,(#94136,#94137,#94138,#94139,#94140,
#94141,#94142,#94143,#94144,#94145),.UNSPECIFIED.,.F.,.F.,(4,1,1,1,1,1,
1,4),(34.5575191894883,35.2982020546007,36.2978585176451,37.2975149806895,
38.2971714437339,39.2968279067783,40.2964843698228,40.8407044966679),
 .UNSPECIFIED.);
#2197=B_SPLINE_CURVE_WITH_KNOTS('',3,(#94150,#94151,#94152,#94153,#94154,
#94155,#94156,#94157,#94158,#94159),.UNSPECIFIED.,.F.,.F.,(4,1,1,1,1,1,
1,4),(28.2743338823085,28.6054153822984,29.6048496490325,30.6042839157666,
31.6037181825007,32.6031524492348,33.6025867159689,34.5575191894881),
 .UNSPECIFIED.);
#2198=B_SPLINE_CURVE_WITH_KNOTS('',3,(#94160,#94161,#94162,#94163,#94164,
#94165,#94166,#94167,#94168,#94169,#94170),.UNSPECIFIED.,.F.,.F.,(4,1,1,
1,1,1,1,1,4),(28.2743338823087,28.3006068132898,29.3002632763342,30.2999197393786,
31.299576202423,32.2992326654675,33.2988891285119,34.2985455915563,34.5575191894883),
 .UNSPECIFIED.);
#2199=B_SPLINE_CURVE_WITH_KNOTS('',3,(#94175,#94176,#94177,#94178,#94179,
#94180,#94181,#94182,#94183,#94184),.UNSPECIFIED.,.F.,.F.,(4,1,1,1,1,1,
1,4),(21.9911485751289,22.6088097818939,23.608244048628,24.6076783153621,
25.6071125820962,26.6065468488302,27.6059811155643,28.2743338823085),
 .UNSPECIFIED.);
#2200=B_SPLINE_CURVE_WITH_KNOTS('',3,(#94185,#94186,#94187,#94188,#94189,
#94190,#94191,#94192,#94193,#94194),.UNSPECIFIED.,.F.,.F.,(4,1,1,1,1,1,
1,4),(21.9911485751291,22.3026680350233,23.3023244980677,24.3019809611122,
25.3016374241566,26.301293887201,27.3009503502454,28.2743338823087),
 .UNSPECIFIED.);
#2201=B_SPLINE_CURVE_WITH_KNOTS('',3,(#94199,#94200,#94201,#94202,#94203,
#94204,#94205,#94206,#94207,#94208),.UNSPECIFIED.,.F.,.F.,(4,1,1,1,1,1,
1,4),(15.7079632679493,16.6122041814894,17.6116384482234,18.6110727149575,
19.6105069816916,20.6099412484257,21.6093755151598,21.9911485751289),
 .UNSPECIFIED.);
#2202=B_SPLINE_CURVE_WITH_KNOTS('',3,(#94209,#94210,#94211,#94212,#94213,
#94214,#94215,#94216,#94217,#94218),.UNSPECIFIED.,.F.,.F.,(4,1,1,1,1,1,
1,4),(15.7079632679495,16.3047292567569,17.3043857198013,18.3040421828457,
19.3036986458901,20.3033551089345,21.3030115719789,21.9911485751291),
 .UNSPECIFIED.);
#2203=B_SPLINE_CURVE_WITH_KNOTS('',3,(#94221,#94222,#94223,#94224,#94225,
#94226,#94227,#94228,#94229,#94230,#94231,#94232,#94233,#94234,#94235,#94236,
#94237,#94238,#94239,#94240,#94241,#94242,#94243,#94244,#94245,#94246,#94247,
#94248,#94249,#94250,#94251,#94252,#94253,#94254,#94255,#94256,#94257,#94258,
#94259,#94260,#94261,#94262,#94263,#94264,#94265,#94266,#94267,#94268,#94269,
#94270,#94271,#94272,#94273,#94274,#94275,#94276,#94277,#94278,#94279,#94280,
#94281,#94282,#94283,#94284,#94285,#94286,#94287,#94288,#94289,#94290,#94291,
#94292,#94293,#94294,#94295,#94296,#94297,#94298,#94299,#94300,#94301,#94302,
#94303,#94304,#94305,#94306,#94307,#94308,#94309,#94310,#94311,#94312,#94313,
#94314,#94315,#94316,#94317,#94318,#94319,#94320,#94321,#94322,#94323,#94324,
#94325,#94326,#94327,#94328,#94329,#94330,#94331,#94332,#94333,#94334,#94335,
#94336,#94337,#94338,#94339,#94340,#94341,#94342,#94343,#94344,#94345,#94346,
#94347,#94348,#94349,#94350,#94351,#94352,#94353,#94354,#94355,#94356,#94357,
#94358,#94359,#94360,#94361,#94362,#94363,#94364,#94365,#94366,#94367,#94368,
#94369,#94370,#94371,#94372,#94373,#94374,#94375,#94376,#94377,#94378,#94379,
#94380,#94381,#94382,#94383,#94384,#94385,#94386,#94387,#94388,#94389,#94390,
#94391,#94392,#94393,#94394,#94395,#94396,#94397,#94398,#94399,#94400,#94401,
#94402,#94403,#94404,#94405,#94406,#94407,#94408,#94409,#94410,#94411,#94412,
#94413,#94414,#94415,#94416,#94417,#94418,#94419,#94420,#94421,#94422,#94423,
#94424,#94425,#94426,#94427,#94428,#94429,#94430,#94431,#94432,#94433,#94434,
#94435,#94436,#94437,#94438,#94439,#94440),.UNSPECIFIED.,.F.,.F.,(4,3,3,
3,3,3,3,3,3,3,3,3,3,3,3,3,3,3,3,3,3,3,3,3,3,3,3,3,3,3,3,3,3,3,3,3,3,3,3,
3,3,3,3,3,3,3,3,3,3,3,3,3,3,3,3,3,3,3,3,3,3,3,3,3,3,3,3,3,3,3,3,3,3,4),
(-1.51155304937021,-1.4867986341959,-1.46138663739248,-1.44926455530148,
-1.44198566695448,-1.43723139879395,-1.41129478811863,-1.38512863143085,
-1.36856346812421,-1.36399889752397,-1.33754355936836,-1.3112352326583,
-1.28933427829745,-1.27838380111703,-1.27269882676012,-1.26908809076141,
-1.2674333239366,-1.24208236385033,-1.21599084244255,-1.19063509328497,
-1.17954195302853,-1.17503012203446,-1.17142816095389,-1.1446505933564,
-1.11755538034957,-1.09145274755766,-1.08166426026069,-1.07535319071695,
-1.07096221841427,-1.04359919185664,-1.0166438108283,-1.01314484918191,
-0.98625222361255,-0.977200099492379,-0.971299394604424,-0.943514789093585,
-0.91597930726476,-0.888306650336328,-0.877800787937313,-0.872097086036976,
-0.867897812831546,-0.840032330792451,-0.812153981120299,-0.784705375823936,
-0.774482071494278,-0.768979249185249,-0.764756614985413,-0.749022550517709,
-0.721911653675323,-0.694106265473056,-0.66670330991581,-0.66275818307286,
-0.63460112991406,-0.606031897351057,-0.577483417867562,-0.564658318261003,
-0.558122567947299,-0.553679410026387,-0.524793660942482,-0.496363213790454,
-0.474882621015088,-0.459389954623598,-0.450074377816351,-0.44490829563357,
-0.416625100495465,-0.387728608299678,-0.358542858111977,-0.342099995691886,
-0.337681523304568,-0.308264569892219,-0.278761910588203,-0.24982670716456,
-0.226999958751254,-0.219677966287731),.UNSPECIFIED.);
#2204=B_SPLINE_CURVE_WITH_KNOTS('',3,(#94442,#94443,#94444,#94445,#94446,
#94447,#94448,#94449,#94450,#94451,#94452,#94453,#94454,#94455,#94456,#94457,
#94458,#94459,#94460,#94461,#94462,#94463,#94464,#94465,#94466,#94467,#94468,
#94469,#94470,#94471,#94472,#94473,#94474,#94475,#94476,#94477,#94478,#94479,
#94480,#94481,#94482,#94483,#94484,#94485,#94486,#94487,#94488,#94489,#94490,
#94491,#94492,#94493,#94494,#94495,#94496,#94497,#94498,#94499,#94500,#94501,
#94502,#94503,#94504,#94505),.UNSPECIFIED.,.F.,.F.,(4,3,3,3,3,3,3,3,3,3,
3,3,3,3,3,3,3,3,3,3,3,4),(-0.410648750431908,-0.381299054024905,-0.351414515897952,
-0.323345095993572,-0.314306783515406,-0.307608364286677,-0.302981488408948,
-0.275425436471569,-0.261760901517091,-0.233519805708424,-0.204329829994871,
-0.19862199232604,-0.194416727168087,-0.167215385011146,-0.140139152408172,
-0.113537500932685,-0.0982440424338316,-0.093782918547421,-0.0680367361001279,
-0.0426830224365629,-0.0180658198696843,0.),.UNSPECIFIED.);
#2205=B_SPLINE_CURVE_WITH_KNOTS('',3,(#94508,#94509,#94510,#94511,#94512,
#94513,#94514,#94515,#94516,#94517,#94518,#94519,#94520,#94521,#94522,#94523,
#94524,#94525,#94526,#94527,#94528,#94529,#94530,#94531,#94532,#94533,#94534,
#94535,#94536,#94537,#94538),.UNSPECIFIED.,.F.,.F.,(4,3,3,3,3,3,3,3,3,3,
4),(-0.219677966287731,-0.190969587719715,-0.161999262949595,-0.132480874583944,
-0.12283591709848,-0.116345167945464,-0.111098549044977,-0.0814759057122038,
-0.0514613231781522,-0.0214845368738984,0.),.UNSPECIFIED.);
#2206=B_SPLINE_CURVE_WITH_KNOTS('',3,(#95803,#95804,#95805,#95806,#95807,
#95808,#95809,#95810),.UNSPECIFIED.,.F.,.F.,(4,1,1,1,1,4),(11.6150328478189,
12.614467114553,13.6139013812871,14.6133356480212,15.6127699147553,15.7079632679493),
 .UNSPECIFIED.);
#2207=B_SPLINE_CURVE_WITH_KNOTS('',3,(#95811,#95812,#95813,#95814,#95815,
#95816,#95817,#95818,#95819,#95820,#95821,#95822,#95823,#95824,#95825,#95826,
#95827,#95828,#95829,#95830,#95831,#95832,#95833,#95834,#95835,#95836,#95837,
#95838,#95839,#95840,#95841,#95842,#95843,#95844,#95845,#95846,#95847,#95848,
#95849,#95850,#95851,#95852,#95853,#95854,#95855,#95856,#95857,#95858,#95859,
#95860,#95861,#95862,#95863,#95864,#95865,#95866,#95867,#95868,#95869,#95870,
#95871,#95872,#95873,#95874,#95875,#95876,#95877,#95878,#95879,#95880,#95881,
#95882,#95883,#95884,#95885,#95886,#95887,#95888,#95889,#95890,#95891,#95892,
#95893,#95894,#95895,#95896,#95897,#95898,#95899,#95900,#95901,#95902,#95903,
#95904),.UNSPECIFIED.,.F.,.F.,(4,3,3,3,3,3,3,3,3,3,3,3,3,3,3,3,3,3,3,3,
3,3,3,3,3,3,3,3,3,3,3,4),(-0.552745378375083,-0.532258650239557,-0.502894553245675,
-0.487265296433606,-0.479829702030211,-0.472037404847164,-0.442982148603388,
-0.419212685559536,-0.408392313611654,-0.401996182412567,-0.397451439969464,
-0.369143868093339,-0.340064512133147,-0.312946502615706,-0.297653419419827,
-0.291369319786409,-0.264567360030501,-0.252826444252568,-0.225465117340262,
-0.197281977672729,-0.192689798637887,-0.188527732452548,-0.16188748095911,
-0.135285222784929,-0.109106515899472,-0.100476530872862,-0.0940367162764452,
-0.0901450819999103,-0.0646019269342215,-0.0394615527910846,-0.015105273416719,
0.),.UNSPECIFIED.);
#2208=B_SPLINE_CURVE_WITH_KNOTS('',3,(#95905,#95906,#95907,#95908,#95909,
#95910,#95911,#95912,#95913,#95914,#95915,#95916,#95917,#95918,#95919,#95920,
#95921,#95922,#95923),.UNSPECIFIED.,.F.,.F.,(4,3,3,3,3,3,4),(-310.309142974525,
-309.824622687567,-308.825188420833,-307.825754154099,-306.826319887365,
-305.826885620631,-305.68582516475),.UNSPECIFIED.);
#2209=B_SPLINE_CURVE_WITH_KNOTS('',3,(#95926,#95927,#95928,#95929,#95930,
#95931,#95932,#95933,#95934),.UNSPECIFIED.,.F.,.F.,(4,1,1,1,1,1,4),(10.3761157273108,
11.3064469415348,12.3061034045792,13.3057598676236,14.305416330668,15.3050727937124,
15.7079632679495),.UNSPECIFIED.);
#2210=B_SPLINE_CURVE_WITH_KNOTS('',3,(#97204,#97205,#97206,#97207,#97208,
#97209,#97210,#97211,#97212,#97213,#97214,#97215,#97216,#97217,#97218,#97219,
#97220,#97221,#97222,#97223,#97224,#97225),.UNSPECIFIED.,.F.,.F.,(4,3,3,
3,3,3,3,4),(302.710195152989,302.895908302457,303.895564765501,304.895221228546,
305.89487769159,306.894534154635,307.894190617679,308.240504799617),
 .UNSPECIFIED.);
#2211=B_SPLINE_CURVE_WITH_KNOTS('',3,(#97226,#97227,#97228,#97229,#97230,
#97231,#97232,#97233,#97234,#97235,#97236,#97237,#97238,#97239,#97240,#97241,
#97242,#97243,#97244,#97245,#97246,#97247,#97248,#97249,#97250,#97251,#97252,
#97253,#97254,#97255,#97256,#97257,#97258,#97259,#97260,#97261,#97262,#97263,
#97264,#97265,#97266,#97267,#97268,#97269,#97270,#97271,#97272,#97273,#97274,
#97275,#97276,#97277,#97278,#97279,#97280,#97281,#97282,#97283,#97284,#97285,
#97286,#97287,#97288,#97289,#97290,#97291,#97292,#97293,#97294,#97295,#97296,
#97297,#97298,#97299,#97300,#97301,#97302,#97303,#97304,#97305,#97306,#97307,
#97308,#97309,#97310,#97311,#97312,#97313),.UNSPECIFIED.,.F.,.F.,(4,3,3,
3,3,3,3,3,3,3,3,3,3,3,3,3,3,3,3,3,3,3,3,3,3,3,3,3,3,4),(-0.555272788399347,
-0.538572946039236,-0.513888794201686,-0.499451161420365,-0.49303522077673,
-0.487943566425205,-0.462157372443835,-0.439748534600925,-0.429096047695605,
-0.424937757521379,-0.398410712364184,-0.371397275485531,-0.34441519227878,
-0.329033061634225,-0.324656870658717,-0.296742049498124,-0.282886669700559,
-0.255957572647936,-0.228482562489743,-0.22261183304744,-0.217969609570416,
-0.190037432453959,-0.161560762906833,-0.132831919803823,-0.116227929828345,
-0.111827184570658,-0.082369349120359,-0.0528160418819264,-0.0238157996808501,
0.),.UNSPECIFIED.);
#2228=SHAPE_REPRESENTATION_RELATIONSHIP('SRR','None',#97622,#2247);
#2247=ADVANCED_BREP_SHAPE_REPRESENTATION('',(#2285),#97472);
#2266=STYLED_ITEM('',(#97720),#2285);
#2285=MANIFOLD_SOLID_BREP('Body1',#21827);
#2373=FACE_BOUND('',#4919,.T.);
#2374=FACE_BOUND('',#4922,.T.);
#2523=PLANE('',#23432);
#2524=PLANE('',#23433);
#2525=PLANE('',#23434);
#2526=PLANE('',#23435);
#2527=PLANE('',#23436);
#2528=PLANE('',#23437);
#2529=PLANE('',#23438);
#2530=PLANE('',#23439);
#2531=PLANE('',#23443);
#2532=PLANE('',#23444);
#3569=FACE_OUTER_BOUND('',#4808,.T.);
#3570=FACE_OUTER_BOUND('',#4809,.T.);
#3571=FACE_OUTER_BOUND('',#4810,.T.);
#3572=FACE_OUTER_BOUND('',#4811,.T.);
#3573=FACE_OUTER_BOUND('',#4812,.T.);
#3574=FACE_OUTER_BOUND('',#4813,.T.);
#3575=FACE_OUTER_BOUND('',#4814,.T.);
#3576=FACE_OUTER_BOUND('',#4815,.T.);
#3577=FACE_OUTER_BOUND('',#4816,.T.);
#3578=FACE_OUTER_BOUND('',#4817,.T.);
#3579=FACE_OUTER_BOUND('',#4818,.T.);
#3580=FACE_OUTER_BOUND('',#4819,.T.);
#3581=FACE_OUTER_BOUND('',#4820,.T.);
#3582=FACE_OUTER_BOUND('',#4821,.T.);
#3583=FACE_OUTER_BOUND('',#4822,.T.);
#3584=FACE_OUTER_BOUND('',#4823,.T.);
#3585=FACE_OUTER_BOUND('',#4824,.T.);
#3586=FACE_OUTER_BOUND('',#4825,.T.);
#3587=FACE_OUTER_BOUND('',#4826,.T.);
#3588=FACE_OUTER_BOUND('',#4827,.T.);
#3589=FACE_OUTER_BOUND('',#4828,.T.);
#3590=FACE_OUTER_BOUND('',#4829,.T.);
#3591=FACE_OUTER_BOUND('',#4830,.T.);
#3592=FACE_OUTER_BOUND('',#4831,.T.);
#3593=FACE_OUTER_BOUND('',#4832,.T.);
#3594=FACE_OUTER_BOUND('',#4833,.T.);
#3595=FACE_OUTER_BOUND('',#4834,.T.);
#3596=FACE_OUTER_BOUND('',#4835,.T.);
#3597=FACE_OUTER_BOUND('',#4836,.T.);
#3598=FACE_OUTER_BOUND('',#4837,.T.);
#3599=FACE_OUTER_BOUND('',#4838,.T.);
#3600=FACE_OUTER_BOUND('',#4839,.T.);
#3601=FACE_OUTER_BOUND('',#4840,.T.);
#3602=FACE_OUTER_BOUND('',#4841,.T.);
#3603=FACE_OUTER_BOUND('',#4842,.T.);
#3604=FACE_OUTER_BOUND('',#4843,.T.);
#3605=FACE_OUTER_BOUND('',#4844,.T.);
#3606=FACE_OUTER_BOUND('',#4845,.T.);
#3607=FACE_OUTER_BOUND('',#4846,.T.);
#3608=FACE_OUTER_BOUND('',#4847,.T.);
#3609=FACE_OUTER_BOUND('',#4848,.T.);
#3610=FACE_OUTER_BOUND('',#4849,.T.);
#3611=FACE_OUTER_BOUND('',#4850,.T.);
#3612=FACE_OUTER_BOUND('',#4851,.T.);
#3613=FACE_OUTER_BOUND('',#4852,.T.);
#3614=FACE_OUTER_BOUND('',#4853,.T.);
#3615=FACE_OUTER_BOUND('',#4854,.T.);
#3616=FACE_OUTER_BOUND('',#4855,.T.);
#3617=FACE_OUTER_BOUND('',#4856,.T.);
#3618=FACE_OUTER_BOUND('',#4857,.T.);
#3619=FACE_OUTER_BOUND('',#4858,.T.);
#3620=FACE_OUTER_BOUND('',#4859,.T.);
#3621=FACE_OUTER_BOUND('',#4860,.T.);
#3622=FACE_OUTER_BOUND('',#4861,.T.);
#3623=FACE_OUTER_BOUND('',#4862,.T.);
#3624=FACE_OUTER_BOUND('',#4863,.T.);
#3625=FACE_OUTER_BOUND('',#4864,.T.);
#3626=FACE_OUTER_BOUND('',#4865,.T.);
#3627=FACE_OUTER_BOUND('',#4866,.T.);
#3628=FACE_OUTER_BOUND('',#4867,.T.);
#3629=FACE_OUTER_BOUND('',#4868,.T.);
#3630=FACE_OUTER_BOUND('',#4869,.T.);
#3631=FACE_OUTER_BOUND('',#4870,.T.);
#3632=FACE_OUTER_BOUND('',#4871,.T.);
#3633=FACE_OUTER_BOUND('',#4872,.T.);
#3634=FACE_OUTER_BOUND('',#4873,.T.);
#3635=FACE_OUTER_BOUND('',#4874,.T.);
#3636=FACE_OUTER_BOUND('',#4875,.T.);
#3637=FACE_OUTER_BOUND('',#4876,.T.);
#3638=FACE_OUTER_BOUND('',#4877,.T.);
#3639=FACE_OUTER_BOUND('',#4878,.T.);
#3640=FACE_OUTER_BOUND('',#4879,.T.);
#3641=FACE_OUTER_BOUND('',#4880,.T.);
#3642=FACE_OUTER_BOUND('',#4881,.T.);
#3643=FACE_OUTER_BOUND('',#4882,.T.);
#3644=FACE_OUTER_BOUND('',#4883,.T.);
#3645=FACE_OUTER_BOUND('',#4884,.T.);
#3646=FACE_OUTER_BOUND('',#4885,.T.);
#3647=FACE_OUTER_BOUND('',#4886,.T.);
#3648=FACE_OUTER_BOUND('',#4887,.T.);
#3649=FACE_OUTER_BOUND('',#4888,.T.);
#3650=FACE_OUTER_BOUND('',#4889,.T.);
#3651=FACE_OUTER_BOUND('',#4890,.T.);
#3652=FACE_OUTER_BOUND('',#4891,.T.);
#3653=FACE_OUTER_BOUND('',#4892,.T.);
#3654=FACE_OUTER_BOUND('',#4893,.T.);
#3655=FACE_OUTER_BOUND('',#4894,.T.);
#3656=FACE_OUTER_BOUND('',#4895,.T.);
#3657=FACE_OUTER_BOUND('',#4896,.T.);
#3658=FACE_OUTER_BOUND('',#4897,.T.);
#3659=FACE_OUTER_BOUND('',#4898,.T.);
#3660=FACE_OUTER_BOUND('',#4899,.T.);
#3661=FACE_OUTER_BOUND('',#4900,.T.);
#3662=FACE_OUTER_BOUND('',#4901,.T.);
#3663=FACE_OUTER_BOUND('',#4902,.T.);
#3664=FACE_OUTER_BOUND('',#4903,.T.);
#3665=FACE_OUTER_BOUND('',#4904,.T.);
#3666=FACE_OUTER_BOUND('',#4905,.T.);
#3667=FACE_OUTER_BOUND('',#4906,.T.);
#3668=FACE_OUTER_BOUND('',#4907,.T.);
#3669=FACE_OUTER_BOUND('',#4908,.T.);
#3670=FACE_OUTER_BOUND('',#4909,.T.);
#3671=FACE_OUTER_BOUND('',#4910,.T.);
#3672=FACE_OUTER_BOUND('',#4911,.T.);
#3673=FACE_OUTER_BOUND('',#4912,.T.);
#3674=FACE_OUTER_BOUND('',#4913,.T.);
#3675=FACE_OUTER_BOUND('',#4914,.T.);
#3676=FACE_OUTER_BOUND('',#4915,.T.);
#3677=FACE_OUTER_BOUND('',#4916,.T.);
#3678=FACE_OUTER_BOUND('',#4917,.T.);
#3679=FACE_OUTER_BOUND('',#4918,.T.);
#3680=FACE_OUTER_BOUND('',#4920,.T.);
#3681=FACE_OUTER_BOUND('',#4921,.T.);
#3682=FACE_OUTER_BOUND('',#4923,.T.);
#4808=EDGE_LOOP('',(#19026,#19027,#19028,#19029));
#4809=EDGE_LOOP('',(#19030,#19031,#19032,#19033));
#4810=EDGE_LOOP('',(#19034,#19035,#19036,#19037));
#4811=EDGE_LOOP('',(#19038,#19039,#19040,#19041));
#4812=EDGE_LOOP('',(#19042,#19043,#19044,#19045));
#4813=EDGE_LOOP('',(#19046,#19047,#19048,#19049));
#4814=EDGE_LOOP('',(#19050,#19051,#19052,#19053));
#4815=EDGE_LOOP('',(#19054,#19055,#19056,#19057));
#4816=EDGE_LOOP('',(#19058,#19059,#19060,#19061));
#4817=EDGE_LOOP('',(#19062,#19063,#19064,#19065));
#4818=EDGE_LOOP('',(#19066,#19067,#19068,#19069));
#4819=EDGE_LOOP('',(#19070,#19071,#19072,#19073));
#4820=EDGE_LOOP('',(#19074,#19075,#19076,#19077));
#4821=EDGE_LOOP('',(#19078,#19079,#19080,#19081));
#4822=EDGE_LOOP('',(#19082,#19083,#19084,#19085));
#4823=EDGE_LOOP('',(#19086,#19087,#19088,#19089));
#4824=EDGE_LOOP('',(#19090,#19091,#19092,#19093));
#4825=EDGE_LOOP('',(#19094,#19095,#19096,#19097));
#4826=EDGE_LOOP('',(#19098,#19099,#19100,#19101));
#4827=EDGE_LOOP('',(#19102,#19103,#19104,#19105));
#4828=EDGE_LOOP('',(#19106,#19107,#19108,#19109));
#4829=EDGE_LOOP('',(#19110,#19111,#19112,#19113));
#4830=EDGE_LOOP('',(#19114,#19115,#19116,#19117));
#4831=EDGE_LOOP('',(#19118,#19119,#19120,#19121));
#4832=EDGE_LOOP('',(#19122,#19123,#19124,#19125));
#4833=EDGE_LOOP('',(#19126,#19127,#19128,#19129));
#4834=EDGE_LOOP('',(#19130,#19131,#19132,#19133));
#4835=EDGE_LOOP('',(#19134,#19135,#19136,#19137));
#4836=EDGE_LOOP('',(#19138,#19139,#19140,#19141));
#4837=EDGE_LOOP('',(#19142,#19143,#19144,#19145));
#4838=EDGE_LOOP('',(#19146,#19147,#19148,#19149));
#4839=EDGE_LOOP('',(#19150,#19151,#19152,#19153));
#4840=EDGE_LOOP('',(#19154,#19155,#19156,#19157));
#4841=EDGE_LOOP('',(#19158,#19159,#19160,#19161));
#4842=EDGE_LOOP('',(#19162,#19163,#19164,#19165));
#4843=EDGE_LOOP('',(#19166,#19167,#19168,#19169));
#4844=EDGE_LOOP('',(#19170,#19171,#19172,#19173));
#4845=EDGE_LOOP('',(#19174,#19175,#19176,#19177));
#4846=EDGE_LOOP('',(#19178,#19179,#19180,#19181));
#4847=EDGE_LOOP('',(#19182,#19183,#19184,#19185));
#4848=EDGE_LOOP('',(#19186,#19187,#19188,#19189));
#4849=EDGE_LOOP('',(#19190,#19191,#19192,#19193));
#4850=EDGE_LOOP('',(#19194,#19195,#19196,#19197));
#4851=EDGE_LOOP('',(#19198,#19199,#19200,#19201));
#4852=EDGE_LOOP('',(#19202,#19203,#19204,#19205));
#4853=EDGE_LOOP('',(#19206,#19207,#19208,#19209));
#4854=EDGE_LOOP('',(#19210,#19211,#19212,#19213));
#4855=EDGE_LOOP('',(#19214,#19215,#19216,#19217));
#4856=EDGE_LOOP('',(#19218,#19219,#19220,#19221));
#4857=EDGE_LOOP('',(#19222,#19223,#19224,#19225));
#4858=EDGE_LOOP('',(#19226,#19227,#19228,#19229));
#4859=EDGE_LOOP('',(#19230,#19231,#19232,#19233));
#4860=EDGE_LOOP('',(#19234,#19235,#19236,#19237));
#4861=EDGE_LOOP('',(#19238,#19239,#19240,#19241));
#4862=EDGE_LOOP('',(#19242,#19243,#19244,#19245));
#4863=EDGE_LOOP('',(#19246,#19247,#19248,#19249));
#4864=EDGE_LOOP('',(#19250,#19251,#19252,#19253));
#4865=EDGE_LOOP('',(#19254,#19255,#19256,#19257));
#4866=EDGE_LOOP('',(#19258,#19259,#19260,#19261));
#4867=EDGE_LOOP('',(#19262,#19263,#19264,#19265));
#4868=EDGE_LOOP('',(#19266,#19267,#19268,#19269));
#4869=EDGE_LOOP('',(#19270,#19271,#19272,#19273));
#4870=EDGE_LOOP('',(#19274,#19275,#19276,#19277));
#4871=EDGE_LOOP('',(#19278,#19279,#19280,#19281));
#4872=EDGE_LOOP('',(#19282,#19283,#19284,#19285));
#4873=EDGE_LOOP('',(#19286,#19287,#19288,#19289));
#4874=EDGE_LOOP('',(#19290,#19291,#19292,#19293));
#4875=EDGE_LOOP('',(#19294,#19295,#19296,#19297));
#4876=EDGE_LOOP('',(#19298,#19299,#19300,#19301));
#4877=EDGE_LOOP('',(#19302,#19303,#19304,#19305));
#4878=EDGE_LOOP('',(#19306,#19307,#19308,#19309));
#4879=EDGE_LOOP('',(#19310,#19311,#19312,#19313));
#4880=EDGE_LOOP('',(#19314,#19315,#19316,#19317));
#4881=EDGE_LOOP('',(#19318,#19319,#19320,#19321));
#4882=EDGE_LOOP('',(#19322,#19323,#19324,#19325));
#4883=EDGE_LOOP('',(#19326,#19327,#19328,#19329));
#4884=EDGE_LOOP('',(#19330,#19331,#19332,#19333));
#4885=EDGE_LOOP('',(#19334,#19335,#19336,#19337));
#4886=EDGE_LOOP('',(#19338,#19339,#19340,#19341));
#4887=EDGE_LOOP('',(#19342,#19343,#19344,#19345));
#4888=EDGE_LOOP('',(#19346,#19347,#19348,#19349));
#4889=EDGE_LOOP('',(#19350,#19351,#19352,#19353));
#4890=EDGE_LOOP('',(#19354,#19355,#19356,#19357));
#4891=EDGE_LOOP('',(#19358,#19359,#19360,#19361));
#4892=EDGE_LOOP('',(#19362,#19363,#19364,#19365));
#4893=EDGE_LOOP('',(#19366,#19367,#19368,#19369));
#4894=EDGE_LOOP('',(#19370,#19371,#19372,#19373));
#4895=EDGE_LOOP('',(#19374,#19375,#19376,#19377));
#4896=EDGE_LOOP('',(#19378,#19379,#19380,#19381));
#4897=EDGE_LOOP('',(#19382,#19383,#19384,#19385));
#4898=EDGE_LOOP('',(#19386,#19387,#19388,#19389));
#4899=EDGE_LOOP('',(#19390,#19391,#19392,#19393));
#4900=EDGE_LOOP('',(#19394,#19395,#19396,#19397));
#4901=EDGE_LOOP('',(#19398,#19399,#19400,#19401));
#4902=EDGE_LOOP('',(#19402,#19403,#19404,#19405));
#4903=EDGE_LOOP('',(#19406,#19407,#19408,#19409));
#4904=EDGE_LOOP('',(#19410,#19411,#19412,#19413));
#4905=EDGE_LOOP('',(#19414,#19415,#19416,#19417));
#4906=EDGE_LOOP('',(#19418,#19419,#19420,#19421,#19422,#19423,#19424,#19425));
#4907=EDGE_LOOP('',(#19426,#19427,#19428,#19429,#19430,#19431,#19432,#19433,
#19434,#19435,#19436,#19437,#19438,#19439,#19440,#19441,#19442,#19443,#19444,
#19445,#19446,#19447,#19448,#19449,#19450,#19451,#19452,#19453,#19454,#19455,
#19456,#19457,#19458,#19459,#19460,#19461,#19462,#19463,#19464,#19465,#19466,
#19467,#19468,#19469,#19470,#19471,#19472,#19473,#19474,#19475,#19476,#19477,
#19478,#19479,#19480,#19481,#19482,#19483,#19484,#19485,#19486,#19487,#19488,
#19489,#19490,#19491,#19492,#19493,#19494,#19495,#19496,#19497,#19498,#19499,
#19500,#19501,#19502,#19503,#19504,#19505,#19506,#19507,#19508,#19509,#19510,
#19511,#19512,#19513,#19514,#19515,#19516,#19517,#19518,#19519,#19520,#19521,
#19522,#19523,#19524,#19525,#19526,#19527));
#4908=EDGE_LOOP('',(#19528,#19529,#19530,#19531));
#4909=EDGE_LOOP('',(#19532,#19533,#19534,#19535,#19536,#19537,#19538,#19539,
#19540,#19541,#19542,#19543,#19544,#19545,#19546,#19547,#19548,#19549,#19550,
#19551,#19552,#19553,#19554,#19555,#19556,#19557,#19558,#19559,#19560,#19561,
#19562,#19563,#19564,#19565,#19566,#19567,#19568,#19569,#19570,#19571,#19572,
#19573,#19574,#19575,#19576,#19577,#19578,#19579,#19580,#19581,#19582,#19583,
#19584,#19585,#19586,#19587,#19588,#19589,#19590,#19591,#19592,#19593,#19594,
#19595,#19596,#19597,#19598,#19599,#19600,#19601,#19602,#19603,#19604,#19605,
#19606,#19607,#19608,#19609,#19610,#19611,#19612,#19613,#19614,#19615,#19616,
#19617,#19618,#19619,#19620,#19621,#19622,#19623,#19624,#19625,#19626,#19627,
#19628,#19629,#19630,#19631,#19632,#19633,#19634));
#4910=EDGE_LOOP('',(#19635,#19636,#19637,#19638));
#4911=EDGE_LOOP('',(#19639,#19640,#19641,#19642));
#4912=EDGE_LOOP('',(#19643,#19644,#19645,#19646));
#4913=EDGE_LOOP('',(#19647,#19648,#19649,#19650));
#4914=EDGE_LOOP('',(#19651,#19652,#19653,#19654));
#4915=EDGE_LOOP('',(#19655,#19656,#19657,#19658));
#4916=EDGE_LOOP('',(#19659,#19660,#19661,#19662));
#4917=EDGE_LOOP('',(#19663,#19664,#19665,#19666,#19667,#19668));
#4918=EDGE_LOOP('',(#19669));
#4919=EDGE_LOOP('',(#19670,#19671,#19672,#19673));
#4920=EDGE_LOOP('',(#19674,#19675,#19676,#19677));
#4921=EDGE_LOOP('',(#19678));
#4922=EDGE_LOOP('',(#19679,#19680,#19681,#19682,#19683,#19684));
#4923=EDGE_LOOP('',(#19685));
#6028=LINE('',#90615,#7242);
#6029=LINE('',#90639,#7243);
#6030=LINE('',#90687,#7244);
#6031=LINE('',#90735,#7245);
#6032=LINE('',#90783,#7246);
#6033=LINE('',#90837,#7247);
#6034=LINE('',#90885,#7248);
#6035=LINE('',#90933,#7249);
#6036=LINE('',#90987,#7250);
#6037=LINE('',#91035,#7251);
#6038=LINE('',#91083,#7252);
#6039=LINE('',#91131,#7253);
#6040=LINE('',#91185,#7254);
#6041=LINE('',#91233,#7255);
#6042=LINE('',#91281,#7256);
#6043=LINE('',#91335,#7257);
#6044=LINE('',#91383,#7258);
#6045=LINE('',#91431,#7259);
#6046=LINE('',#91479,#7260);
#6047=LINE('',#91533,#7261);
#6048=LINE('',#91581,#7262);
#6049=LINE('',#91629,#7263);
#6050=LINE('',#91683,#7264);
#6051=LINE('',#91731,#7265);
#6052=LINE('',#91779,#7266);
#6053=LINE('',#91827,#7267);
#6054=LINE('',#91881,#7268);
#6055=LINE('',#91929,#7269);
#6056=LINE('',#91977,#7270);
#6057=LINE('',#92031,#7271);
#6058=LINE('',#92079,#7272);
#6059=LINE('',#92127,#7273);
#6060=LINE('',#92175,#7274);
#6061=LINE('',#92229,#7275);
#6062=LINE('',#92277,#7276);
#6063=LINE('',#92325,#7277);
#6064=LINE('',#92379,#7278);
#6065=LINE('',#92427,#7279);
#6066=LINE('',#92475,#7280);
#6067=LINE('',#92523,#7281);
#6068=LINE('',#92577,#7282);
#6069=LINE('',#92625,#7283);
#6070=LINE('',#92673,#7284);
#6071=LINE('',#92727,#7285);
#6072=LINE('',#92775,#7286);
#6073=LINE('',#92823,#7287);
#6074=LINE('',#92871,#7288);
#6075=LINE('',#92922,#7289);
#6076=LINE('',#92970,#7290);
#6077=LINE('',#93018,#7291);
#6078=LINE('',#93043,#7292);
#6079=LINE('',#93068,#7293);
#6080=LINE('',#93092,#7294);
#6081=LINE('',#93117,#7295);
#6082=LINE('',#93142,#7296);
#6083=LINE('',#93166,#7297);
#6084=LINE('',#93190,#7298);
#6085=LINE('',#93215,#7299);
#6086=LINE('',#93240,#7300);
#6087=LINE('',#93264,#7301);
#6088=LINE('',#93289,#7302);
#6089=LINE('',#93314,#7303);
#6090=LINE('',#93338,#7304);
#6091=LINE('',#93362,#7305);
#6092=LINE('',#93387,#7306);
#6093=LINE('',#93412,#7307);
#6094=LINE('',#93436,#7308);
#6095=LINE('',#93461,#7309);
#6096=LINE('',#93486,#7310);
#6097=LINE('',#93510,#7311);
#6098=LINE('',#93534,#7312);
#6099=LINE('',#93559,#7313);
#6100=LINE('',#93584,#7314);
#6101=LINE('',#93608,#7315);
#6102=LINE('',#93633,#7316);
#6103=LINE('',#93658,#7317);
#6104=LINE('',#93682,#7318);
#6105=LINE('',#93706,#7319);
#6106=LINE('',#93731,#7320);
#6107=LINE('',#93756,#7321);
#6108=LINE('',#93780,#7322);
#6109=LINE('',#93805,#7323);
#6110=LINE('',#93830,#7324);
#6111=LINE('',#93854,#7325);
#6112=LINE('',#93878,#7326);
#6113=LINE('',#93903,#7327);
#6114=LINE('',#93928,#7328);
#6115=LINE('',#93952,#7329);
#6116=LINE('',#93977,#7330);
#6117=LINE('',#94002,#7331);
#6118=LINE('',#94026,#7332);
#6119=LINE('',#94050,#7333);
#6120=LINE('',#94075,#7334);
#6121=LINE('',#94100,#7335);
#6122=LINE('',#94124,#7336);
#6123=LINE('',#94149,#7337);
#6124=LINE('',#94174,#7338);
#6125=LINE('',#94198,#7339);
#6126=LINE('',#94540,#7340);
#6127=LINE('',#97318,#7341);
#6128=LINE('',#97320,#7342);
#6129=LINE('',#97322,#7343);
#6130=LINE('',#97323,#7344);
#6131=LINE('',#97326,#7345);
#6132=LINE('',#97328,#7346);
#6133=LINE('',#97329,#7347);
#6134=LINE('',#97332,#7348);
#6135=LINE('',#97334,#7349);
#6136=LINE('',#97335,#7350);
#6137=LINE('',#97338,#7351);
#6138=LINE('',#97340,#7352);
#6139=LINE('',#97341,#7353);
#6140=LINE('',#97344,#7354);
#6141=LINE('',#97346,#7355);
#6142=LINE('',#97347,#7356);
#6143=LINE('',#97349,#7357);
#6144=LINE('',#97350,#7358);
#6145=LINE('',#97357,#7359);
#7242=VECTOR('',#27168,3.);
#7243=VECTOR('',#27173,3.);
#7244=VECTOR('',#27176,3.);
#7245=VECTOR('',#27179,3.);
#7246=VECTOR('',#27182,3.);
#7247=VECTOR('',#27185,3.);
#7248=VECTOR('',#27188,3.);
#7249=VECTOR('',#27191,3.);
#7250=VECTOR('',#27194,3.);
#7251=VECTOR('',#27197,3.);
#7252=VECTOR('',#27200,3.);
#7253=VECTOR('',#27203,3.);
#7254=VECTOR('',#27206,3.);
#7255=VECTOR('',#27209,3.);
#7256=VECTOR('',#27212,3.);
#7257=VECTOR('',#27215,3.);
#7258=VECTOR('',#27218,3.);
#7259=VECTOR('',#27221,3.);
#7260=VECTOR('',#27224,3.);
#7261=VECTOR('',#27227,3.);
#7262=VECTOR('',#27230,3.);
#7263=VECTOR('',#27233,3.);
#7264=VECTOR('',#27236,3.);
#7265=VECTOR('',#27239,3.);
#7266=VECTOR('',#27242,3.);
#7267=VECTOR('',#27245,3.);
#7268=VECTOR('',#27248,3.);
#7269=VECTOR('',#27251,3.);
#7270=VECTOR('',#27254,3.);
#7271=VECTOR('',#27257,3.);
#7272=VECTOR('',#27260,3.);
#7273=VECTOR('',#27263,3.);
#7274=VECTOR('',#27266,3.);
#7275=VECTOR('',#27269,3.);
#7276=VECTOR('',#27272,3.);
#7277=VECTOR('',#27275,3.);
#7278=VECTOR('',#27278,3.);
#7279=VECTOR('',#27281,3.);
#7280=VECTOR('',#27284,3.);
#7281=VECTOR('',#27287,3.);
#7282=VECTOR('',#27290,3.);
#7283=VECTOR('',#27293,3.);
#7284=VECTOR('',#27296,3.);
#7285=VECTOR('',#27299,3.);
#7286=VECTOR('',#27302,3.);
#7287=VECTOR('',#27305,3.);
#7288=VECTOR('',#27308,3.);
#7289=VECTOR('',#27311,3.);
#7290=VECTOR('',#27314,3.);
#7291=VECTOR('',#27317,2.37175);
#7292=VECTOR('',#27322,2.37175);
#7293=VECTOR('',#27325,2.37175);
#7294=VECTOR('',#27328,2.37175);
#7295=VECTOR('',#27331,2.37175);
#7296=VECTOR('',#27334,2.37175);
#7297=VECTOR('',#27337,2.37175);
#7298=VECTOR('',#27340,2.37175);
#7299=VECTOR('',#27343,2.37175);
#7300=VECTOR('',#27346,2.37175);
#7301=VECTOR('',#27349,2.37175);
#7302=VECTOR('',#27352,2.37175);
#7303=VECTOR('',#27355,2.37175);
#7304=VECTOR('',#27358,2.37175);
#7305=VECTOR('',#27361,2.37175);
#7306=VECTOR('',#27364,2.37175);
#7307=VECTOR('',#27367,2.37175);
#7308=VECTOR('',#27370,2.37175);
#7309=VECTOR('',#27373,2.37175);
#7310=VECTOR('',#27376,2.37175);
#7311=VECTOR('',#27379,2.37175);
#7312=VECTOR('',#27382,2.37175);
#7313=VECTOR('',#27385,2.37175);
#7314=VECTOR('',#27388,2.37175);
#7315=VECTOR('',#27391,2.37175);
#7316=VECTOR('',#27394,2.37175);
#7317=VECTOR('',#27397,2.37175);
#7318=VECTOR('',#27400,2.37175);
#7319=VECTOR('',#27403,2.37175);
#7320=VECTOR('',#27406,2.37175);
#7321=VECTOR('',#27409,2.37175);
#7322=VECTOR('',#27412,2.37175);
#7323=VECTOR('',#27415,2.37175);
#7324=VECTOR('',#27418,2.37175);
#7325=VECTOR('',#27421,2.37175);
#7326=VECTOR('',#27424,2.37175);
#7327=VECTOR('',#27427,2.37175);
#7328=VECTOR('',#27430,2.37175);
#7329=VECTOR('',#27433,2.37175);
#7330=VECTOR('',#27436,2.37175);
#7331=VECTOR('',#27439,2.37175);
#7332=VECTOR('',#27442,2.37175);
#7333=VECTOR('',#27445,2.37175);
#7334=VECTOR('',#27448,2.37175);
#7335=VECTOR('',#27451,2.37175);
#7336=VECTOR('',#27454,2.37175);
#7337=VECTOR('',#27457,2.37175);
#7338=VECTOR('',#27460,2.37175);
#7339=VECTOR('',#27463,2.37175);
#7340=VECTOR('',#27468,2.5);
#7341=VECTOR('',#27479,10.);
#7342=VECTOR('',#27480,10.);
#7343=VECTOR('',#27481,10.);
#7344=VECTOR('',#27482,10.);
#7345=VECTOR('',#27485,10.);
#7346=VECTOR('',#27486,10.);
#7347=VECTOR('',#27487,10.);
#7348=VECTOR('',#27490,10.);
#7349=VECTOR('',#27491,10.);
#7350=VECTOR('',#27492,10.);
#7351=VECTOR('',#27495,10.);
#7352=VECTOR('',#27496,10.);
#7353=VECTOR('',#27497,10.);
#7354=VECTOR('',#27500,10.);
#7355=VECTOR('',#27501,10.);
#7356=VECTOR('',#27502,10.);
#7357=VECTOR('',#27505,10.);
#7358=VECTOR('',#27506,10.);
#7359=VECTOR('',#27515,5.);
#7598=CIRCLE('',#23327,2.942);
#7599=CIRCLE('',#23377,2.37175);
#7600=CIRCLE('',#23427,2.942);
#7601=CIRCLE('',#23428,2.);
#7602=CIRCLE('',#23430,2.37175);
#7603=CIRCLE('',#23440,5.);
#7604=CIRCLE('',#23442,5.);
#9585=VERTEX_POINT('',#90613);
#9586=VERTEX_POINT('',#90614);
#9587=VERTEX_POINT('',#90616);
#9588=VERTEX_POINT('',#90627);
#9589=VERTEX_POINT('',#90637);
#9590=VERTEX_POINT('',#90638);
#9591=VERTEX_POINT('',#90685);
#9592=VERTEX_POINT('',#90686);
#9593=VERTEX_POINT('',#90733);
#9594=VERTEX_POINT('',#90734);
#9595=VERTEX_POINT('',#90781);
#9596=VERTEX_POINT('',#90782);
#9597=VERTEX_POINT('',#90835);
#9598=VERTEX_POINT('',#90836);
#9599=VERTEX_POINT('',#90883);
#9600=VERTEX_POINT('',#90884);
#9601=VERTEX_POINT('',#90931);
#9602=VERTEX_POINT('',#90932);
#9603=VERTEX_POINT('',#90985);
#9604=VERTEX_POINT('',#90986);
#9605=VERTEX_POINT('',#91033);
#9606=VERTEX_POINT('',#91034);
#9607=VERTEX_POINT('',#91081);
#9608=VERTEX_POINT('',#91082);
#9609=VERTEX_POINT('',#91129);
#9610=VERTEX_POINT('',#91130);
#9611=VERTEX_POINT('',#91183);
#9612=VERTEX_POINT('',#91184);
#9613=VERTEX_POINT('',#91231);
#9614=VERTEX_POINT('',#91232);
#9615=VERTEX_POINT('',#91279);
#9616=VERTEX_POINT('',#91280);
#9617=VERTEX_POINT('',#91333);
#9618=VERTEX_POINT('',#91334);
#9619=VERTEX_POINT('',#91381);
#9620=VERTEX_POINT('',#91382);
#9621=VERTEX_POINT('',#91429);
#9622=VERTEX_POINT('',#91430);
#9623=VERTEX_POINT('',#91477);
#9624=VERTEX_POINT('',#91478);
#9625=VERTEX_POINT('',#91531);
#9626=VERTEX_POINT('',#91532);
#9627=VERTEX_POINT('',#91579);
#9628=VERTEX_POINT('',#91580);
#9629=VERTEX_POINT('',#91627);
#9630=VERTEX_POINT('',#91628);
#9631=VERTEX_POINT('',#91681);
#9632=VERTEX_POINT('',#91682);
#9633=VERTEX_POINT('',#91729);
#9634=VERTEX_POINT('',#91730);
#9635=VERTEX_POINT('',#91777);
#9636=VERTEX_POINT('',#91778);
#9637=VERTEX_POINT('',#91825);
#9638=VERTEX_POINT('',#91826);
#9639=VERTEX_POINT('',#91879);
#9640=VERTEX_POINT('',#91880);
#9641=VERTEX_POINT('',#91927);
#9642=VERTEX_POINT('',#91928);
#9643=VERTEX_POINT('',#91975);
#9644=VERTEX_POINT('',#91976);
#9645=VERTEX_POINT('',#92029);
#9646=VERTEX_POINT('',#92030);
#9647=VERTEX_POINT('',#92077);
#9648=VERTEX_POINT('',#92078);
#9649=VERTEX_POINT('',#92125);
#9650=VERTEX_POINT('',#92126);
#9651=VERTEX_POINT('',#92173);
#9652=VERTEX_POINT('',#92174);
#9653=VERTEX_POINT('',#92227);
#9654=VERTEX_POINT('',#92228);
#9655=VERTEX_POINT('',#92275);
#9656=VERTEX_POINT('',#92276);
#9657=VERTEX_POINT('',#92323);
#9658=VERTEX_POINT('',#92324);
#9659=VERTEX_POINT('',#92377);
#9660=VERTEX_POINT('',#92378);
#9661=VERTEX_POINT('',#92425);
#9662=VERTEX_POINT('',#92426);
#9663=VERTEX_POINT('',#92473);
#9664=VERTEX_POINT('',#92474);
#9665=VERTEX_POINT('',#92521);
#9666=VERTEX_POINT('',#92522);
#9667=VERTEX_POINT('',#92575);
#9668=VERTEX_POINT('',#92576);
#9669=VERTEX_POINT('',#92623);
#9670=VERTEX_POINT('',#92624);
#9671=VERTEX_POINT('',#92671);
#9672=VERTEX_POINT('',#92672);
#9673=VERTEX_POINT('',#92725);
#9674=VERTEX_POINT('',#92726);
#9675=VERTEX_POINT('',#92773);
#9676=VERTEX_POINT('',#92774);
#9677=VERTEX_POINT('',#92821);
#9678=VERTEX_POINT('',#92822);
#9679=VERTEX_POINT('',#92869);
#9680=VERTEX_POINT('',#92870);
#9681=VERTEX_POINT('',#92920);
#9682=VERTEX_POINT('',#92921);
#9683=VERTEX_POINT('',#92968);
#9684=VERTEX_POINT('',#92969);
#9685=VERTEX_POINT('',#93016);
#9686=VERTEX_POINT('',#93017);
#9687=VERTEX_POINT('',#93019);
#9688=VERTEX_POINT('',#93030);
#9689=VERTEX_POINT('',#93041);
#9690=VERTEX_POINT('',#93042);
#9691=VERTEX_POINT('',#93066);
#9692=VERTEX_POINT('',#93067);
#9693=VERTEX_POINT('',#93090);
#9694=VERTEX_POINT('',#93091);
#9695=VERTEX_POINT('',#93115);
#9696=VERTEX_POINT('',#93116);
#9697=VERTEX_POINT('',#93140);
#9698=VERTEX_POINT('',#93141);
#9699=VERTEX_POINT('',#93164);
#9700=VERTEX_POINT('',#93165);
#9701=VERTEX_POINT('',#93188);
#9702=VERTEX_POINT('',#93189);
#9703=VERTEX_POINT('',#93213);
#9704=VERTEX_POINT('',#93214);
#9705=VERTEX_POINT('',#93238);
#9706=VERTEX_POINT('',#93239);
#9707=VERTEX_POINT('',#93262);
#9708=VERTEX_POINT('',#93263);
#9709=VERTEX_POINT('',#93287);
#9710=VERTEX_POINT('',#93288);
#9711=VERTEX_POINT('',#93312);
#9712=VERTEX_POINT('',#93313);
#9713=VERTEX_POINT('',#93336);
#9714=VERTEX_POINT('',#93337);
#9715=VERTEX_POINT('',#93360);
#9716=VERTEX_POINT('',#93361);
#9717=VERTEX_POINT('',#93385);
#9718=VERTEX_POINT('',#93386);
#9719=VERTEX_POINT('',#93410);
#9720=VERTEX_POINT('',#93411);
#9721=VERTEX_POINT('',#93434);
#9722=VERTEX_POINT('',#93435);
#9723=VERTEX_POINT('',#93459);
#9724=VERTEX_POINT('',#93460);
#9725=VERTEX_POINT('',#93484);
#9726=VERTEX_POINT('',#93485);
#9727=VERTEX_POINT('',#93508);
#9728=VERTEX_POINT('',#93509);
#9729=VERTEX_POINT('',#93532);
#9730=VERTEX_POINT('',#93533);
#9731=VERTEX_POINT('',#93557);
#9732=VERTEX_POINT('',#93558);
#9733=VERTEX_POINT('',#93582);
#9734=VERTEX_POINT('',#93583);
#9735=VERTEX_POINT('',#93606);
#9736=VERTEX_POINT('',#93607);
#9737=VERTEX_POINT('',#93631);
#9738=VERTEX_POINT('',#93632);
#9739=VERTEX_POINT('',#93656);
#9740=VERTEX_POINT('',#93657);
#9741=VERTEX_POINT('',#93680);
#9742=VERTEX_POINT('',#93681);
#9743=VERTEX_POINT('',#93704);
#9744=VERTEX_POINT('',#93705);
#9745=VERTEX_POINT('',#93729);
#9746=VERTEX_POINT('',#93730);
#9747=VERTEX_POINT('',#93754);
#9748=VERTEX_POINT('',#93755);
#9749=VERTEX_POINT('',#93778);
#9750=VERTEX_POINT('',#93779);
#9751=VERTEX_POINT('',#93803);
#9752=VERTEX_POINT('',#93804);
#9753=VERTEX_POINT('',#93828);
#9754=VERTEX_POINT('',#93829);
#9755=VERTEX_POINT('',#93852);
#9756=VERTEX_POINT('',#93853);
#9757=VERTEX_POINT('',#93876);
#9758=VERTEX_POINT('',#93877);
#9759=VERTEX_POINT('',#93901);
#9760=VERTEX_POINT('',#93902);
#9761=VERTEX_POINT('',#93926);
#9762=VERTEX_POINT('',#93927);
#9763=VERTEX_POINT('',#93950);
#9764=VERTEX_POINT('',#93951);
#9765=VERTEX_POINT('',#93975);
#9766=VERTEX_POINT('',#93976);
#9767=VERTEX_POINT('',#94000);
#9768=VERTEX_POINT('',#94001);
#9769=VERTEX_POINT('',#94024);
#9770=VERTEX_POINT('',#94025);
#9771=VERTEX_POINT('',#94048);
#9772=VERTEX_POINT('',#94049);
#9773=VERTEX_POINT('',#94073);
#9774=VERTEX_POINT('',#94074);
#9775=VERTEX_POINT('',#94098);
#9776=VERTEX_POINT('',#94099);
#9777=VERTEX_POINT('',#94122);
#9778=VERTEX_POINT('',#94123);
#9779=VERTEX_POINT('',#94147);
#9780=VERTEX_POINT('',#94148);
#9781=VERTEX_POINT('',#94172);
#9782=VERTEX_POINT('',#94173);
#9783=VERTEX_POINT('',#94196);
#9784=VERTEX_POINT('',#94197);
#9785=VERTEX_POINT('',#94220);
#9786=VERTEX_POINT('',#94441);
#9787=VERTEX_POINT('',#94506);
#9788=VERTEX_POINT('',#94539);
#9789=VERTEX_POINT('',#95802);
#9790=VERTEX_POINT('',#95925);
#9791=VERTEX_POINT('',#97316);
#9792=VERTEX_POINT('',#97317);
#9793=VERTEX_POINT('',#97319);
#9794=VERTEX_POINT('',#97321);
#9795=VERTEX_POINT('',#97325);
#9796=VERTEX_POINT('',#97327);
#9797=VERTEX_POINT('',#97331);
#9798=VERTEX_POINT('',#97333);
#9799=VERTEX_POINT('',#97337);
#9800=VERTEX_POINT('',#97339);
#9801=VERTEX_POINT('',#97343);
#9802=VERTEX_POINT('',#97345);
#9803=VERTEX_POINT('',#97353);
#9804=VERTEX_POINT('',#97356);
#12770=EDGE_CURVE('',#9585,#9586,#6028,.T.);
#12771=EDGE_CURVE('',#9585,#9587,#2007,.T.);
#12772=EDGE_CURVE('',#9587,#9588,#7598,.F.);
#12773=EDGE_CURVE('',#9588,#9586,#2008,.T.);
#12774=EDGE_CURVE('',#9589,#9590,#6029,.T.);
#12775=EDGE_CURVE('',#9589,#9585,#2009,.T.);
#12776=EDGE_CURVE('',#9586,#9590,#2010,.T.);
#12777=EDGE_CURVE('',#9591,#9592,#6030,.T.);
#12778=EDGE_CURVE('',#9591,#9589,#2011,.T.);
#12779=EDGE_CURVE('',#9590,#9592,#2012,.T.);
#12780=EDGE_CURVE('',#9593,#9594,#6031,.T.);
#12781=EDGE_CURVE('',#9593,#9591,#2013,.T.);
#12782=EDGE_CURVE('',#9592,#9594,#2014,.T.);
#12783=EDGE_CURVE('',#9595,#9596,#6032,.T.);
#12784=EDGE_CURVE('',#9595,#9593,#2015,.T.);
#12785=EDGE_CURVE('',#9594,#9596,#2016,.T.);
#12786=EDGE_CURVE('',#9597,#9598,#6033,.T.);
#12787=EDGE_CURVE('',#9597,#9595,#2017,.T.);
#12788=EDGE_CURVE('',#9596,#9598,#2018,.T.);
#12789=EDGE_CURVE('',#9599,#9600,#6034,.T.);
#12790=EDGE_CURVE('',#9599,#9597,#2019,.T.);
#12791=EDGE_CURVE('',#9598,#9600,#2020,.T.);
#12792=EDGE_CURVE('',#9601,#9602,#6035,.T.);
#12793=EDGE_CURVE('',#9601,#9599,#2021,.T.);
#12794=EDGE_CURVE('',#9600,#9602,#2022,.T.);
#12795=EDGE_CURVE('',#9603,#9604,#6036,.T.);
#12796=EDGE_CURVE('',#9603,#9601,#2023,.T.);
#12797=EDGE_CURVE('',#9602,#9604,#2024,.T.);
#12798=EDGE_CURVE('',#9605,#9606,#6037,.T.);
#12799=EDGE_CURVE('',#9605,#9603,#2025,.T.);
#12800=EDGE_CURVE('',#9604,#9606,#2026,.T.);
#12801=EDGE_CURVE('',#9607,#9608,#6038,.T.);
#12802=EDGE_CURVE('',#9607,#9605,#2027,.T.);
#12803=EDGE_CURVE('',#9606,#9608,#2028,.T.);
#12804=EDGE_CURVE('',#9609,#9610,#6039,.T.);
#12805=EDGE_CURVE('',#9609,#9607,#2029,.T.);
#12806=EDGE_CURVE('',#9608,#9610,#2030,.T.);
#12807=EDGE_CURVE('',#9611,#9612,#6040,.T.);
#12808=EDGE_CURVE('',#9611,#9609,#2031,.T.);
#12809=EDGE_CURVE('',#9610,#9612,#2032,.T.);
#12810=EDGE_CURVE('',#9613,#9614,#6041,.T.);
#12811=EDGE_CURVE('',#9613,#9611,#2033,.T.);
#12812=EDGE_CURVE('',#9612,#9614,#2034,.T.);
#12813=EDGE_CURVE('',#9615,#9616,#6042,.T.);
#12814=EDGE_CURVE('',#9615,#9613,#2035,.T.);
#12815=EDGE_CURVE('',#9614,#9616,#2036,.T.);
#12816=EDGE_CURVE('',#9617,#9618,#6043,.T.);
#12817=EDGE_CURVE('',#9617,#9615,#2037,.T.);
#12818=EDGE_CURVE('',#9616,#9618,#2038,.T.);
#12819=EDGE_CURVE('',#9619,#9620,#6044,.T.);
#12820=EDGE_CURVE('',#9619,#9617,#2039,.T.);
#12821=EDGE_CURVE('',#9618,#9620,#2040,.T.);
#12822=EDGE_CURVE('',#9621,#9622,#6045,.T.);
#12823=EDGE_CURVE('',#9621,#9619,#2041,.T.);
#12824=EDGE_CURVE('',#9620,#9622,#2042,.T.);
#12825=EDGE_CURVE('',#9623,#9624,#6046,.T.);
#12826=EDGE_CURVE('',#9623,#9621,#2043,.T.);
#12827=EDGE_CURVE('',#9622,#9624,#2044,.T.);
#12828=EDGE_CURVE('',#9625,#9626,#6047,.T.);
#12829=EDGE_CURVE('',#9625,#9623,#2045,.T.);
#12830=EDGE_CURVE('',#9624,#9626,#2046,.T.);
#12831=EDGE_CURVE('',#9627,#9628,#6048,.T.);
#12832=EDGE_CURVE('',#9627,#9625,#2047,.T.);
#12833=EDGE_CURVE('',#9626,#9628,#2048,.T.);
#12834=EDGE_CURVE('',#9629,#9630,#6049,.T.);
#12835=EDGE_CURVE('',#9629,#9627,#2049,.T.);
#12836=EDGE_CURVE('',#9628,#9630,#2050,.T.);
#12837=EDGE_CURVE('',#9631,#9632,#6050,.T.);
#12838=EDGE_CURVE('',#9631,#9629,#2051,.T.);
#12839=EDGE_CURVE('',#9630,#9632,#2052,.T.);
#12840=EDGE_CURVE('',#9633,#9634,#6051,.T.);
#12841=EDGE_CURVE('',#9633,#9631,#2053,.T.);
#12842=EDGE_CURVE('',#9632,#9634,#2054,.T.);
#12843=EDGE_CURVE('',#9635,#9636,#6052,.T.);
#12844=EDGE_CURVE('',#9635,#9633,#2055,.T.);
#12845=EDGE_CURVE('',#9634,#9636,#2056,.T.);
#12846=EDGE_CURVE('',#9637,#9638,#6053,.T.);
#12847=EDGE_CURVE('',#9637,#9635,#2057,.T.);
#12848=EDGE_CURVE('',#9636,#9638,#2058,.T.);
#12849=EDGE_CURVE('',#9639,#9640,#6054,.T.);
#12850=EDGE_CURVE('',#9639,#9637,#2059,.T.);
#12851=EDGE_CURVE('',#9638,#9640,#2060,.T.);
#12852=EDGE_CURVE('',#9641,#9642,#6055,.T.);
#12853=EDGE_CURVE('',#9641,#9639,#2061,.T.);
#12854=EDGE_CURVE('',#9640,#9642,#2062,.T.);
#12855=EDGE_CURVE('',#9643,#9644,#6056,.T.);
#12856=EDGE_CURVE('',#9643,#9641,#2063,.T.);
#12857=EDGE_CURVE('',#9642,#9644,#2064,.T.);
#12858=EDGE_CURVE('',#9645,#9646,#6057,.T.);
#12859=EDGE_CURVE('',#9645,#9643,#2065,.T.);
#12860=EDGE_CURVE('',#9644,#9646,#2066,.T.);
#12861=EDGE_CURVE('',#9647,#9648,#6058,.T.);
#12862=EDGE_CURVE('',#9647,#9645,#2067,.T.);
#12863=EDGE_CURVE('',#9646,#9648,#2068,.T.);
#12864=EDGE_CURVE('',#9649,#9650,#6059,.T.);
#12865=EDGE_CURVE('',#9649,#9647,#2069,.T.);
#12866=EDGE_CURVE('',#9648,#9650,#2070,.T.);
#12867=EDGE_CURVE('',#9651,#9652,#6060,.T.);
#12868=EDGE_CURVE('',#9651,#9649,#2071,.T.);
#12869=EDGE_CURVE('',#9650,#9652,#2072,.T.);
#12870=EDGE_CURVE('',#9653,#9654,#6061,.T.);
#12871=EDGE_CURVE('',#9653,#9651,#2073,.T.);
#12872=EDGE_CURVE('',#9652,#9654,#2074,.T.);
#12873=EDGE_CURVE('',#9655,#9656,#6062,.T.);
#12874=EDGE_CURVE('',#9655,#9653,#2075,.T.);
#12875=EDGE_CURVE('',#9654,#9656,#2076,.T.);
#12876=EDGE_CURVE('',#9657,#9658,#6063,.T.);
#12877=EDGE_CURVE('',#9657,#9655,#2077,.T.);
#12878=EDGE_CURVE('',#9656,#9658,#2078,.T.);
#12879=EDGE_CURVE('',#9659,#9660,#6064,.T.);
#12880=EDGE_CURVE('',#9659,#9657,#2079,.T.);
#12881=EDGE_CURVE('',#9658,#9660,#2080,.T.);
#12882=EDGE_CURVE('',#9661,#9662,#6065,.T.);
#12883=EDGE_CURVE('',#9661,#9659,#2081,.T.);
#12884=EDGE_CURVE('',#9660,#9662,#2082,.T.);
#12885=EDGE_CURVE('',#9663,#9664,#6066,.T.);
#12886=EDGE_CURVE('',#9663,#9661,#2083,.T.);
#12887=EDGE_CURVE('',#9662,#9664,#2084,.T.);
#12888=EDGE_CURVE('',#9665,#9666,#6067,.T.);
#12889=EDGE_CURVE('',#9665,#9663,#2085,.T.);
#12890=EDGE_CURVE('',#9664,#9666,#2086,.T.);
#12891=EDGE_CURVE('',#9667,#9668,#6068,.T.);
#12892=EDGE_CURVE('',#9667,#9665,#2087,.T.);
#12893=EDGE_CURVE('',#9666,#9668,#2088,.T.);
#12894=EDGE_CURVE('',#9669,#9670,#6069,.T.);
#12895=EDGE_CURVE('',#9669,#9667,#2089,.T.);
#12896=EDGE_CURVE('',#9668,#9670,#2090,.T.);
#12897=EDGE_CURVE('',#9671,#9672,#6070,.T.);
#12898=EDGE_CURVE('',#9671,#9669,#2091,.T.);
#12899=EDGE_CURVE('',#9670,#9672,#2092,.T.);
#12900=EDGE_CURVE('',#9673,#9674,#6071,.T.);
#12901=EDGE_CURVE('',#9673,#9671,#2093,.T.);
#12902=EDGE_CURVE('',#9672,#9674,#2094,.T.);
#12903=EDGE_CURVE('',#9675,#9676,#6072,.T.);
#12904=EDGE_CURVE('',#9675,#9673,#2095,.T.);
#12905=EDGE_CURVE('',#9674,#9676,#2096,.T.);
#12906=EDGE_CURVE('',#9677,#9678,#6073,.T.);
#12907=EDGE_CURVE('',#9677,#9675,#2097,.T.);
#12908=EDGE_CURVE('',#9676,#9678,#2098,.T.);
#12909=EDGE_CURVE('',#9679,#9680,#6074,.T.);
#12910=EDGE_CURVE('',#9679,#9677,#2099,.T.);
#12911=EDGE_CURVE('',#9678,#9680,#2100,.T.);
#12912=EDGE_CURVE('',#9681,#9682,#6075,.T.);
#12913=EDGE_CURVE('',#9681,#9679,#2101,.T.);
#12914=EDGE_CURVE('',#9680,#9682,#2102,.T.);
#12915=EDGE_CURVE('',#9683,#9684,#6076,.T.);
#12916=EDGE_CURVE('',#9683,#9681,#2103,.T.);
#12917=EDGE_CURVE('',#9682,#9684,#2104,.T.);
#12918=EDGE_CURVE('',#9685,#9686,#6077,.T.);
#12919=EDGE_CURVE('',#9685,#9687,#2105,.T.);
#12920=EDGE_CURVE('',#9687,#9688,#7599,.T.);
#12921=EDGE_CURVE('',#9686,#9688,#2106,.T.);
#12922=EDGE_CURVE('',#9689,#9690,#6078,.T.);
#12923=EDGE_CURVE('',#9689,#9685,#2107,.T.);
#12924=EDGE_CURVE('',#9690,#9686,#2108,.T.);
#12925=EDGE_CURVE('',#9691,#9692,#6079,.T.);
#12926=EDGE_CURVE('',#9691,#9689,#2109,.T.);
#12927=EDGE_CURVE('',#9692,#9690,#2110,.T.);
#12928=EDGE_CURVE('',#9693,#9694,#6080,.T.);
#12929=EDGE_CURVE('',#9693,#9691,#2111,.T.);
#12930=EDGE_CURVE('',#9694,#9692,#2112,.T.);
#12931=EDGE_CURVE('',#9695,#9696,#6081,.T.);
#12932=EDGE_CURVE('',#9695,#9693,#2113,.T.);
#12933=EDGE_CURVE('',#9696,#9694,#2114,.T.);
#12934=EDGE_CURVE('',#9697,#9698,#6082,.T.);
#12935=EDGE_CURVE('',#9697,#9695,#2115,.T.);
#12936=EDGE_CURVE('',#9698,#9696,#2116,.T.);
#12937=EDGE_CURVE('',#9699,#9700,#6083,.T.);
#12938=EDGE_CURVE('',#9699,#9697,#2117,.T.);
#12939=EDGE_CURVE('',#9700,#9698,#2118,.T.);
#12940=EDGE_CURVE('',#9701,#9702,#6084,.T.);
#12941=EDGE_CURVE('',#9701,#9699,#2119,.T.);
#12942=EDGE_CURVE('',#9702,#9700,#2120,.T.);
#12943=EDGE_CURVE('',#9703,#9704,#6085,.T.);
#12944=EDGE_CURVE('',#9703,#9701,#2121,.T.);
#12945=EDGE_CURVE('',#9704,#9702,#2122,.T.);
#12946=EDGE_CURVE('',#9705,#9706,#6086,.T.);
#12947=EDGE_CURVE('',#9705,#9703,#2123,.T.);
#12948=EDGE_CURVE('',#9706,#9704,#2124,.T.);
#12949=EDGE_CURVE('',#9707,#9708,#6087,.T.);
#12950=EDGE_CURVE('',#9707,#9705,#2125,.T.);
#12951=EDGE_CURVE('',#9708,#9706,#2126,.T.);
#12952=EDGE_CURVE('',#9709,#9710,#6088,.T.);
#12953=EDGE_CURVE('',#9709,#9707,#2127,.T.);
#12954=EDGE_CURVE('',#9710,#9708,#2128,.T.);
#12955=EDGE_CURVE('',#9711,#9712,#6089,.T.);
#12956=EDGE_CURVE('',#9711,#9709,#2129,.T.);
#12957=EDGE_CURVE('',#9712,#9710,#2130,.T.);
#12958=EDGE_CURVE('',#9713,#9714,#6090,.T.);
#12959=EDGE_CURVE('',#9713,#9711,#2131,.T.);
#12960=EDGE_CURVE('',#9714,#9712,#2132,.T.);
#12961=EDGE_CURVE('',#9715,#9716,#6091,.T.);
#12962=EDGE_CURVE('',#9715,#9713,#2133,.T.);
#12963=EDGE_CURVE('',#9716,#9714,#2134,.T.);
#12964=EDGE_CURVE('',#9717,#9718,#6092,.T.);
#12965=EDGE_CURVE('',#9717,#9715,#2135,.T.);
#12966=EDGE_CURVE('',#9718,#9716,#2136,.T.);
#12967=EDGE_CURVE('',#9719,#9720,#6093,.T.);
#12968=EDGE_CURVE('',#9719,#9717,#2137,.T.);
#12969=EDGE_CURVE('',#9720,#9718,#2138,.T.);
#12970=EDGE_CURVE('',#9721,#9722,#6094,.T.);
#12971=EDGE_CURVE('',#9721,#9719,#2139,.T.);
#12972=EDGE_CURVE('',#9722,#9720,#2140,.T.);
#12973=EDGE_CURVE('',#9723,#9724,#6095,.T.);
#12974=EDGE_CURVE('',#9723,#9721,#2141,.T.);
#12975=EDGE_CURVE('',#9724,#9722,#2142,.T.);
#12976=EDGE_CURVE('',#9725,#9726,#6096,.T.);
#12977=EDGE_CURVE('',#9725,#9723,#2143,.T.);
#12978=EDGE_CURVE('',#9726,#9724,#2144,.T.);
#12979=EDGE_CURVE('',#9727,#9728,#6097,.T.);
#12980=EDGE_CURVE('',#9727,#9725,#2145,.T.);
#12981=EDGE_CURVE('',#9728,#9726,#2146,.T.);
#12982=EDGE_CURVE('',#9729,#9730,#6098,.T.);
#12983=EDGE_CURVE('',#9729,#9727,#2147,.T.);
#12984=EDGE_CURVE('',#9730,#9728,#2148,.T.);
#12985=EDGE_CURVE('',#9731,#9732,#6099,.T.);
#12986=EDGE_CURVE('',#9731,#9729,#2149,.T.);
#12987=EDGE_CURVE('',#9732,#9730,#2150,.T.);
#12988=EDGE_CURVE('',#9733,#9734,#6100,.T.);
#12989=EDGE_CURVE('',#9733,#9731,#2151,.T.);
#12990=EDGE_CURVE('',#9734,#9732,#2152,.T.);
#12991=EDGE_CURVE('',#9735,#9736,#6101,.T.);
#12992=EDGE_CURVE('',#9735,#9733,#2153,.T.);
#12993=EDGE_CURVE('',#9736,#9734,#2154,.T.);
#12994=EDGE_CURVE('',#9737,#9738,#6102,.T.);
#12995=EDGE_CURVE('',#9737,#9735,#2155,.T.);
#12996=EDGE_CURVE('',#9738,#9736,#2156,.T.);
#12997=EDGE_CURVE('',#9739,#9740,#6103,.T.);
#12998=EDGE_CURVE('',#9739,#9737,#2157,.T.);
#12999=EDGE_CURVE('',#9740,#9738,#2158,.T.);
#13000=EDGE_CURVE('',#9741,#9742,#6104,.T.);
#13001=EDGE_CURVE('',#9741,#9739,#2159,.T.);
#13002=EDGE_CURVE('',#9742,#9740,#2160,.T.);
#13003=EDGE_CURVE('',#9743,#9744,#6105,.T.);
#13004=EDGE_CURVE('',#9743,#9741,#2161,.T.);
#13005=EDGE_CURVE('',#9744,#9742,#2162,.T.);
#13006=EDGE_CURVE('',#9745,#9746,#6106,.T.);
#13007=EDGE_CURVE('',#9745,#9743,#2163,.T.);
#13008=EDGE_CURVE('',#9746,#9744,#2164,.T.);
#13009=EDGE_CURVE('',#9747,#9748,#6107,.T.);
#13010=EDGE_CURVE('',#9747,#9745,#2165,.T.);
#13011=EDGE_CURVE('',#9748,#9746,#2166,.T.);
#13012=EDGE_CURVE('',#9749,#9750,#6108,.T.);
#13013=EDGE_CURVE('',#9749,#9747,#2167,.T.);
#13014=EDGE_CURVE('',#9750,#9748,#2168,.T.);
#13015=EDGE_CURVE('',#9751,#9752,#6109,.T.);
#13016=EDGE_CURVE('',#9751,#9749,#2169,.T.);
#13017=EDGE_CURVE('',#9752,#9750,#2170,.T.);
#13018=EDGE_CURVE('',#9753,#9754,#6110,.T.);
#13019=EDGE_CURVE('',#9753,#9751,#2171,.T.);
#13020=EDGE_CURVE('',#9754,#9752,#2172,.T.);
#13021=EDGE_CURVE('',#9755,#9756,#6111,.T.);
#13022=EDGE_CURVE('',#9755,#9753,#2173,.T.);
#13023=EDGE_CURVE('',#9756,#9754,#2174,.T.);
#13024=EDGE_CURVE('',#9757,#9758,#6112,.T.);
#13025=EDGE_CURVE('',#9757,#9755,#2175,.T.);
#13026=EDGE_CURVE('',#9758,#9756,#2176,.T.);
#13027=EDGE_CURVE('',#9759,#9760,#6113,.T.);
#13028=EDGE_CURVE('',#9759,#9757,#2177,.T.);
#13029=EDGE_CURVE('',#9760,#9758,#2178,.T.);
#13030=EDGE_CURVE('',#9761,#9762,#6114,.T.);
#13031=EDGE_CURVE('',#9761,#9759,#2179,.T.);
#13032=EDGE_CURVE('',#9762,#9760,#2180,.T.);
#13033=EDGE_CURVE('',#9763,#9764,#6115,.T.);
#13034=EDGE_CURVE('',#9763,#9761,#2181,.T.);
#13035=EDGE_CURVE('',#9764,#9762,#2182,.T.);
#13036=EDGE_CURVE('',#9765,#9766,#6116,.T.);
#13037=EDGE_CURVE('',#9765,#9763,#2183,.T.);
#13038=EDGE_CURVE('',#9766,#9764,#2184,.T.);
#13039=EDGE_CURVE('',#9767,#9768,#6117,.T.);
#13040=EDGE_CURVE('',#9767,#9765,#2185,.T.);
#13041=EDGE_CURVE('',#9768,#9766,#2186,.T.);
#13042=EDGE_CURVE('',#9769,#9770,#6118,.T.);
#13043=EDGE_CURVE('',#9769,#9767,#2187,.T.);
#13044=EDGE_CURVE('',#9770,#9768,#2188,.T.);
#13045=EDGE_CURVE('',#9771,#9772,#6119,.T.);
#13046=EDGE_CURVE('',#9771,#9769,#2189,.T.);
#13047=EDGE_CURVE('',#9772,#9770,#2190,.T.);
#13048=EDGE_CURVE('',#9773,#9774,#6120,.T.);
#13049=EDGE_CURVE('',#9773,#9771,#2191,.T.);
#13050=EDGE_CURVE('',#9774,#9772,#2192,.T.);
#13051=EDGE_CURVE('',#9775,#9776,#6121,.T.);
#13052=EDGE_CURVE('',#9775,#9773,#2193,.T.);
#13053=EDGE_CURVE('',#9776,#9774,#2194,.T.);
#13054=EDGE_CURVE('',#9777,#9778,#6122,.T.);
#13055=EDGE_CURVE('',#9777,#9775,#2195,.T.);
#13056=EDGE_CURVE('',#9778,#9776,#2196,.T.);
#13057=EDGE_CURVE('',#9779,#9780,#6123,.T.);
#13058=EDGE_CURVE('',#9779,#9777,#2197,.T.);
#13059=EDGE_CURVE('',#9780,#9778,#2198,.T.);
#13060=EDGE_CURVE('',#9781,#9782,#6124,.T.);
#13061=EDGE_CURVE('',#9781,#9779,#2199,.T.);
#13062=EDGE_CURVE('',#9782,#9780,#2200,.T.);
#13063=EDGE_CURVE('',#9783,#9784,#6125,.T.);
#13064=EDGE_CURVE('',#9783,#9781,#2201,.T.);
#13065=EDGE_CURVE('',#9784,#9782,#2202,.T.);
#13066=EDGE_CURVE('',#9688,#9785,#2203,.T.);
#13067=EDGE_CURVE('',#9786,#9687,#2204,.T.);
#13068=EDGE_CURVE('',#9787,#9786,#7600,.T.);
#13069=EDGE_CURVE('',#9785,#9787,#2205,.T.);
#13070=EDGE_CURVE('',#9785,#9788,#6126,.T.);
#13071=EDGE_CURVE('',#9788,#9788,#7601,.T.);
#13072=EDGE_CURVE('',#9789,#9783,#2206,.T.);
#13073=EDGE_CURVE('',#9587,#9789,#2207,.T.);
#13074=EDGE_CURVE('',#9786,#9683,#2208,.T.);
#13075=EDGE_CURVE('',#9790,#9784,#2209,.T.);
#13076=EDGE_CURVE('',#9789,#9790,#7602,.T.);
#13077=EDGE_CURVE('',#9684,#9787,#2210,.T.);
#13078=EDGE_CURVE('',#9790,#9588,#2211,.T.);
#13079=EDGE_CURVE('',#9791,#9792,#6127,.T.);
#13080=EDGE_CURVE('',#9791,#9793,#6128,.T.);
#13081=EDGE_CURVE('',#9793,#9794,#6129,.T.);
#13082=EDGE_CURVE('',#9792,#9794,#6130,.T.);
#13083=EDGE_CURVE('',#9795,#9791,#6131,.T.);
#13084=EDGE_CURVE('',#9795,#9796,#6132,.T.);
#13085=EDGE_CURVE('',#9796,#9793,#6133,.T.);
#13086=EDGE_CURVE('',#9797,#9795,#6134,.T.);
#13087=EDGE_CURVE('',#9797,#9798,#6135,.T.);
#13088=EDGE_CURVE('',#9798,#9796,#6136,.T.);
#13089=EDGE_CURVE('',#9799,#9797,#6137,.T.);
#13090=EDGE_CURVE('',#9799,#9800,#6138,.T.);
#13091=EDGE_CURVE('',#9800,#9798,#6139,.T.);
#13092=EDGE_CURVE('',#9801,#9799,#6140,.T.);
#13093=EDGE_CURVE('',#9801,#9802,#6141,.T.);
#13094=EDGE_CURVE('',#9802,#9800,#6142,.T.);
#13095=EDGE_CURVE('',#9792,#9801,#6143,.T.);
#13096=EDGE_CURVE('',#9794,#9802,#6144,.T.);
#13097=EDGE_CURVE('',#9803,#9803,#7603,.T.);
#13098=EDGE_CURVE('',#9803,#9804,#6145,.T.);
#13099=EDGE_CURVE('',#9804,#9804,#7604,.T.);
#19026=ORIENTED_EDGE('',*,*,#12770,.F.);
#19027=ORIENTED_EDGE('',*,*,#12771,.T.);
#19028=ORIENTED_EDGE('',*,*,#12772,.T.);
#19029=ORIENTED_EDGE('',*,*,#12773,.T.);
#19030=ORIENTED_EDGE('',*,*,#12774,.F.);
#19031=ORIENTED_EDGE('',*,*,#12775,.T.);
#19032=ORIENTED_EDGE('',*,*,#12770,.T.);
#19033=ORIENTED_EDGE('',*,*,#12776,.T.);
#19034=ORIENTED_EDGE('',*,*,#12777,.F.);
#19035=ORIENTED_EDGE('',*,*,#12778,.T.);
#19036=ORIENTED_EDGE('',*,*,#12774,.T.);
#19037=ORIENTED_EDGE('',*,*,#12779,.T.);
#19038=ORIENTED_EDGE('',*,*,#12780,.F.);
#19039=ORIENTED_EDGE('',*,*,#12781,.T.);
#19040=ORIENTED_EDGE('',*,*,#12777,.T.);
#19041=ORIENTED_EDGE('',*,*,#12782,.T.);
#19042=ORIENTED_EDGE('',*,*,#12783,.F.);
#19043=ORIENTED_EDGE('',*,*,#12784,.T.);
#19044=ORIENTED_EDGE('',*,*,#12780,.T.);
#19045=ORIENTED_EDGE('',*,*,#12785,.T.);
#19046=ORIENTED_EDGE('',*,*,#12786,.F.);
#19047=ORIENTED_EDGE('',*,*,#12787,.T.);
#19048=ORIENTED_EDGE('',*,*,#12783,.T.);
#19049=ORIENTED_EDGE('',*,*,#12788,.T.);
#19050=ORIENTED_EDGE('',*,*,#12789,.F.);
#19051=ORIENTED_EDGE('',*,*,#12790,.T.);
#19052=ORIENTED_EDGE('',*,*,#12786,.T.);
#19053=ORIENTED_EDGE('',*,*,#12791,.T.);
#19054=ORIENTED_EDGE('',*,*,#12792,.F.);
#19055=ORIENTED_EDGE('',*,*,#12793,.T.);
#19056=ORIENTED_EDGE('',*,*,#12789,.T.);
#19057=ORIENTED_EDGE('',*,*,#12794,.T.);
#19058=ORIENTED_EDGE('',*,*,#12795,.F.);
#19059=ORIENTED_EDGE('',*,*,#12796,.T.);
#19060=ORIENTED_EDGE('',*,*,#12792,.T.);
#19061=ORIENTED_EDGE('',*,*,#12797,.T.);
#19062=ORIENTED_EDGE('',*,*,#12798,.F.);
#19063=ORIENTED_EDGE('',*,*,#12799,.T.);
#19064=ORIENTED_EDGE('',*,*,#12795,.T.);
#19065=ORIENTED_EDGE('',*,*,#12800,.T.);
#19066=ORIENTED_EDGE('',*,*,#12801,.F.);
#19067=ORIENTED_EDGE('',*,*,#12802,.T.);
#19068=ORIENTED_EDGE('',*,*,#12798,.T.);
#19069=ORIENTED_EDGE('',*,*,#12803,.T.);
#19070=ORIENTED_EDGE('',*,*,#12804,.F.);
#19071=ORIENTED_EDGE('',*,*,#12805,.T.);
#19072=ORIENTED_EDGE('',*,*,#12801,.T.);
#19073=ORIENTED_EDGE('',*,*,#12806,.T.);
#19074=ORIENTED_EDGE('',*,*,#12807,.F.);
#19075=ORIENTED_EDGE('',*,*,#12808,.T.);
#19076=ORIENTED_EDGE('',*,*,#12804,.T.);
#19077=ORIENTED_EDGE('',*,*,#12809,.T.);
#19078=ORIENTED_EDGE('',*,*,#12810,.F.);
#19079=ORIENTED_EDGE('',*,*,#12811,.T.);
#19080=ORIENTED_EDGE('',*,*,#12807,.T.);
#19081=ORIENTED_EDGE('',*,*,#12812,.T.);
#19082=ORIENTED_EDGE('',*,*,#12813,.F.);
#19083=ORIENTED_EDGE('',*,*,#12814,.T.);
#19084=ORIENTED_EDGE('',*,*,#12810,.T.);
#19085=ORIENTED_EDGE('',*,*,#12815,.T.);
#19086=ORIENTED_EDGE('',*,*,#12816,.F.);
#19087=ORIENTED_EDGE('',*,*,#12817,.T.);
#19088=ORIENTED_EDGE('',*,*,#12813,.T.);
#19089=ORIENTED_EDGE('',*,*,#12818,.T.);
#19090=ORIENTED_EDGE('',*,*,#12819,.F.);
#19091=ORIENTED_EDGE('',*,*,#12820,.T.);
#19092=ORIENTED_EDGE('',*,*,#12816,.T.);
#19093=ORIENTED_EDGE('',*,*,#12821,.T.);
#19094=ORIENTED_EDGE('',*,*,#12822,.F.);
#19095=ORIENTED_EDGE('',*,*,#12823,.T.);
#19096=ORIENTED_EDGE('',*,*,#12819,.T.);
#19097=ORIENTED_EDGE('',*,*,#12824,.T.);
#19098=ORIENTED_EDGE('',*,*,#12825,.F.);
#19099=ORIENTED_EDGE('',*,*,#12826,.T.);
#19100=ORIENTED_EDGE('',*,*,#12822,.T.);
#19101=ORIENTED_EDGE('',*,*,#12827,.T.);
#19102=ORIENTED_EDGE('',*,*,#12828,.F.);
#19103=ORIENTED_EDGE('',*,*,#12829,.T.);
#19104=ORIENTED_EDGE('',*,*,#12825,.T.);
#19105=ORIENTED_EDGE('',*,*,#12830,.T.);
#19106=ORIENTED_EDGE('',*,*,#12831,.F.);
#19107=ORIENTED_EDGE('',*,*,#12832,.T.);
#19108=ORIENTED_EDGE('',*,*,#12828,.T.);
#19109=ORIENTED_EDGE('',*,*,#12833,.T.);
#19110=ORIENTED_EDGE('',*,*,#12834,.F.);
#19111=ORIENTED_EDGE('',*,*,#12835,.T.);
#19112=ORIENTED_EDGE('',*,*,#12831,.T.);
#19113=ORIENTED_EDGE('',*,*,#12836,.T.);
#19114=ORIENTED_EDGE('',*,*,#12837,.F.);
#19115=ORIENTED_EDGE('',*,*,#12838,.T.);
#19116=ORIENTED_EDGE('',*,*,#12834,.T.);
#19117=ORIENTED_EDGE('',*,*,#12839,.T.);
#19118=ORIENTED_EDGE('',*,*,#12840,.F.);
#19119=ORIENTED_EDGE('',*,*,#12841,.T.);
#19120=ORIENTED_EDGE('',*,*,#12837,.T.);
#19121=ORIENTED_EDGE('',*,*,#12842,.T.);
#19122=ORIENTED_EDGE('',*,*,#12843,.F.);
#19123=ORIENTED_EDGE('',*,*,#12844,.T.);
#19124=ORIENTED_EDGE('',*,*,#12840,.T.);
#19125=ORIENTED_EDGE('',*,*,#12845,.T.);
#19126=ORIENTED_EDGE('',*,*,#12846,.F.);
#19127=ORIENTED_EDGE('',*,*,#12847,.T.);
#19128=ORIENTED_EDGE('',*,*,#12843,.T.);
#19129=ORIENTED_EDGE('',*,*,#12848,.T.);
#19130=ORIENTED_EDGE('',*,*,#12849,.F.);
#19131=ORIENTED_EDGE('',*,*,#12850,.T.);
#19132=ORIENTED_EDGE('',*,*,#12846,.T.);
#19133=ORIENTED_EDGE('',*,*,#12851,.T.);
#19134=ORIENTED_EDGE('',*,*,#12852,.F.);
#19135=ORIENTED_EDGE('',*,*,#12853,.T.);
#19136=ORIENTED_EDGE('',*,*,#12849,.T.);
#19137=ORIENTED_EDGE('',*,*,#12854,.T.);
#19138=ORIENTED_EDGE('',*,*,#12855,.F.);
#19139=ORIENTED_EDGE('',*,*,#12856,.T.);
#19140=ORIENTED_EDGE('',*,*,#12852,.T.);
#19141=ORIENTED_EDGE('',*,*,#12857,.T.);
#19142=ORIENTED_EDGE('',*,*,#12858,.F.);
#19143=ORIENTED_EDGE('',*,*,#12859,.T.);
#19144=ORIENTED_EDGE('',*,*,#12855,.T.);
#19145=ORIENTED_EDGE('',*,*,#12860,.T.);
#19146=ORIENTED_EDGE('',*,*,#12861,.F.);
#19147=ORIENTED_EDGE('',*,*,#12862,.T.);
#19148=ORIENTED_EDGE('',*,*,#12858,.T.);
#19149=ORIENTED_EDGE('',*,*,#12863,.T.);
#19150=ORIENTED_EDGE('',*,*,#12864,.F.);
#19151=ORIENTED_EDGE('',*,*,#12865,.T.);
#19152=ORIENTED_EDGE('',*,*,#12861,.T.);
#19153=ORIENTED_EDGE('',*,*,#12866,.T.);
#19154=ORIENTED_EDGE('',*,*,#12867,.F.);
#19155=ORIENTED_EDGE('',*,*,#12868,.T.);
#19156=ORIENTED_EDGE('',*,*,#12864,.T.);
#19157=ORIENTED_EDGE('',*,*,#12869,.T.);
#19158=ORIENTED_EDGE('',*,*,#12870,.F.);
#19159=ORIENTED_EDGE('',*,*,#12871,.T.);
#19160=ORIENTED_EDGE('',*,*,#12867,.T.);
#19161=ORIENTED_EDGE('',*,*,#12872,.T.);
#19162=ORIENTED_EDGE('',*,*,#12873,.F.);
#19163=ORIENTED_EDGE('',*,*,#12874,.T.);
#19164=ORIENTED_EDGE('',*,*,#12870,.T.);
#19165=ORIENTED_EDGE('',*,*,#12875,.T.);
#19166=ORIENTED_EDGE('',*,*,#12876,.F.);
#19167=ORIENTED_EDGE('',*,*,#12877,.T.);
#19168=ORIENTED_EDGE('',*,*,#12873,.T.);
#19169=ORIENTED_EDGE('',*,*,#12878,.T.);
#19170=ORIENTED_EDGE('',*,*,#12879,.F.);
#19171=ORIENTED_EDGE('',*,*,#12880,.T.);
#19172=ORIENTED_EDGE('',*,*,#12876,.T.);
#19173=ORIENTED_EDGE('',*,*,#12881,.T.);
#19174=ORIENTED_EDGE('',*,*,#12882,.F.);
#19175=ORIENTED_EDGE('',*,*,#12883,.T.);
#19176=ORIENTED_EDGE('',*,*,#12879,.T.);
#19177=ORIENTED_EDGE('',*,*,#12884,.T.);
#19178=ORIENTED_EDGE('',*,*,#12885,.F.);
#19179=ORIENTED_EDGE('',*,*,#12886,.T.);
#19180=ORIENTED_EDGE('',*,*,#12882,.T.);
#19181=ORIENTED_EDGE('',*,*,#12887,.T.);
#19182=ORIENTED_EDGE('',*,*,#12888,.F.);
#19183=ORIENTED_EDGE('',*,*,#12889,.T.);
#19184=ORIENTED_EDGE('',*,*,#12885,.T.);
#19185=ORIENTED_EDGE('',*,*,#12890,.T.);
#19186=ORIENTED_EDGE('',*,*,#12891,.F.);
#19187=ORIENTED_EDGE('',*,*,#12892,.T.);
#19188=ORIENTED_EDGE('',*,*,#12888,.T.);
#19189=ORIENTED_EDGE('',*,*,#12893,.T.);
#19190=ORIENTED_EDGE('',*,*,#12894,.F.);
#19191=ORIENTED_EDGE('',*,*,#12895,.T.);
#19192=ORIENTED_EDGE('',*,*,#12891,.T.);
#19193=ORIENTED_EDGE('',*,*,#12896,.T.);
#19194=ORIENTED_EDGE('',*,*,#12897,.F.);
#19195=ORIENTED_EDGE('',*,*,#12898,.T.);
#19196=ORIENTED_EDGE('',*,*,#12894,.T.);
#19197=ORIENTED_EDGE('',*,*,#12899,.T.);
#19198=ORIENTED_EDGE('',*,*,#12900,.F.);
#19199=ORIENTED_EDGE('',*,*,#12901,.T.);
#19200=ORIENTED_EDGE('',*,*,#12897,.T.);
#19201=ORIENTED_EDGE('',*,*,#12902,.T.);
#19202=ORIENTED_EDGE('',*,*,#12903,.F.);
#19203=ORIENTED_EDGE('',*,*,#12904,.T.);
#19204=ORIENTED_EDGE('',*,*,#12900,.T.);
#19205=ORIENTED_EDGE('',*,*,#12905,.T.);
#19206=ORIENTED_EDGE('',*,*,#12906,.F.);
#19207=ORIENTED_EDGE('',*,*,#12907,.T.);
#19208=ORIENTED_EDGE('',*,*,#12903,.T.);
#19209=ORIENTED_EDGE('',*,*,#12908,.T.);
#19210=ORIENTED_EDGE('',*,*,#12909,.F.);
#19211=ORIENTED_EDGE('',*,*,#12910,.T.);
#19212=ORIENTED_EDGE('',*,*,#12906,.T.);
#19213=ORIENTED_EDGE('',*,*,#12911,.T.);
#19214=ORIENTED_EDGE('',*,*,#12912,.F.);
#19215=ORIENTED_EDGE('',*,*,#12913,.T.);
#19216=ORIENTED_EDGE('',*,*,#12909,.T.);
#19217=ORIENTED_EDGE('',*,*,#12914,.T.);
#19218=ORIENTED_EDGE('',*,*,#12915,.F.);
#19219=ORIENTED_EDGE('',*,*,#12916,.T.);
#19220=ORIENTED_EDGE('',*,*,#12912,.T.);
#19221=ORIENTED_EDGE('',*,*,#12917,.T.);
#19222=ORIENTED_EDGE('',*,*,#12918,.F.);
#19223=ORIENTED_EDGE('',*,*,#12919,.T.);
#19224=ORIENTED_EDGE('',*,*,#12920,.T.);
#19225=ORIENTED_EDGE('',*,*,#12921,.F.);
#19226=ORIENTED_EDGE('',*,*,#12922,.F.);
#19227=ORIENTED_EDGE('',*,*,#12923,.T.);
#19228=ORIENTED_EDGE('',*,*,#12918,.T.);
#19229=ORIENTED_EDGE('',*,*,#12924,.F.);
#19230=ORIENTED_EDGE('',*,*,#12925,.F.);
#19231=ORIENTED_EDGE('',*,*,#12926,.T.);
#19232=ORIENTED_EDGE('',*,*,#12922,.T.);
#19233=ORIENTED_EDGE('',*,*,#12927,.F.);
#19234=ORIENTED_EDGE('',*,*,#12928,.F.);
#19235=ORIENTED_EDGE('',*,*,#12929,.T.);
#19236=ORIENTED_EDGE('',*,*,#12925,.T.);
#19237=ORIENTED_EDGE('',*,*,#12930,.F.);
#19238=ORIENTED_EDGE('',*,*,#12931,.F.);
#19239=ORIENTED_EDGE('',*,*,#12932,.T.);
#19240=ORIENTED_EDGE('',*,*,#12928,.T.);
#19241=ORIENTED_EDGE('',*,*,#12933,.F.);
#19242=ORIENTED_EDGE('',*,*,#12934,.F.);
#19243=ORIENTED_EDGE('',*,*,#12935,.T.);
#19244=ORIENTED_EDGE('',*,*,#12931,.T.);
#19245=ORIENTED_EDGE('',*,*,#12936,.F.);
#19246=ORIENTED_EDGE('',*,*,#12937,.F.);
#19247=ORIENTED_EDGE('',*,*,#12938,.T.);
#19248=ORIENTED_EDGE('',*,*,#12934,.T.);
#19249=ORIENTED_EDGE('',*,*,#12939,.F.);
#19250=ORIENTED_EDGE('',*,*,#12940,.F.);
#19251=ORIENTED_EDGE('',*,*,#12941,.T.);
#19252=ORIENTED_EDGE('',*,*,#12937,.T.);
#19253=ORIENTED_EDGE('',*,*,#12942,.F.);
#19254=ORIENTED_EDGE('',*,*,#12943,.F.);
#19255=ORIENTED_EDGE('',*,*,#12944,.T.);
#19256=ORIENTED_EDGE('',*,*,#12940,.T.);
#19257=ORIENTED_EDGE('',*,*,#12945,.F.);
#19258=ORIENTED_EDGE('',*,*,#12946,.F.);
#19259=ORIENTED_EDGE('',*,*,#12947,.T.);
#19260=ORIENTED_EDGE('',*,*,#12943,.T.);
#19261=ORIENTED_EDGE('',*,*,#12948,.F.);
#19262=ORIENTED_EDGE('',*,*,#12949,.F.);
#19263=ORIENTED_EDGE('',*,*,#12950,.T.);
#19264=ORIENTED_EDGE('',*,*,#12946,.T.);
#19265=ORIENTED_EDGE('',*,*,#12951,.F.);
#19266=ORIENTED_EDGE('',*,*,#12952,.F.);
#19267=ORIENTED_EDGE('',*,*,#12953,.T.);
#19268=ORIENTED_EDGE('',*,*,#12949,.T.);
#19269=ORIENTED_EDGE('',*,*,#12954,.F.);
#19270=ORIENTED_EDGE('',*,*,#12955,.F.);
#19271=ORIENTED_EDGE('',*,*,#12956,.T.);
#19272=ORIENTED_EDGE('',*,*,#12952,.T.);
#19273=ORIENTED_EDGE('',*,*,#12957,.F.);
#19274=ORIENTED_EDGE('',*,*,#12958,.F.);
#19275=ORIENTED_EDGE('',*,*,#12959,.T.);
#19276=ORIENTED_EDGE('',*,*,#12955,.T.);
#19277=ORIENTED_EDGE('',*,*,#12960,.F.);
#19278=ORIENTED_EDGE('',*,*,#12961,.F.);
#19279=ORIENTED_EDGE('',*,*,#12962,.T.);
#19280=ORIENTED_EDGE('',*,*,#12958,.T.);
#19281=ORIENTED_EDGE('',*,*,#12963,.F.);
#19282=ORIENTED_EDGE('',*,*,#12964,.F.);
#19283=ORIENTED_EDGE('',*,*,#12965,.T.);
#19284=ORIENTED_EDGE('',*,*,#12961,.T.);
#19285=ORIENTED_EDGE('',*,*,#12966,.F.);
#19286=ORIENTED_EDGE('',*,*,#12967,.F.);
#19287=ORIENTED_EDGE('',*,*,#12968,.T.);
#19288=ORIENTED_EDGE('',*,*,#12964,.T.);
#19289=ORIENTED_EDGE('',*,*,#12969,.F.);
#19290=ORIENTED_EDGE('',*,*,#12970,.F.);
#19291=ORIENTED_EDGE('',*,*,#12971,.T.);
#19292=ORIENTED_EDGE('',*,*,#12967,.T.);
#19293=ORIENTED_EDGE('',*,*,#12972,.F.);
#19294=ORIENTED_EDGE('',*,*,#12973,.F.);
#19295=ORIENTED_EDGE('',*,*,#12974,.T.);
#19296=ORIENTED_EDGE('',*,*,#12970,.T.);
#19297=ORIENTED_EDGE('',*,*,#12975,.F.);
#19298=ORIENTED_EDGE('',*,*,#12976,.F.);
#19299=ORIENTED_EDGE('',*,*,#12977,.T.);
#19300=ORIENTED_EDGE('',*,*,#12973,.T.);
#19301=ORIENTED_EDGE('',*,*,#12978,.F.);
#19302=ORIENTED_EDGE('',*,*,#12979,.F.);
#19303=ORIENTED_EDGE('',*,*,#12980,.T.);
#19304=ORIENTED_EDGE('',*,*,#12976,.T.);
#19305=ORIENTED_EDGE('',*,*,#12981,.F.);
#19306=ORIENTED_EDGE('',*,*,#12982,.F.);
#19307=ORIENTED_EDGE('',*,*,#12983,.T.);
#19308=ORIENTED_EDGE('',*,*,#12979,.T.);
#19309=ORIENTED_EDGE('',*,*,#12984,.F.);
#19310=ORIENTED_EDGE('',*,*,#12985,.F.);
#19311=ORIENTED_EDGE('',*,*,#12986,.T.);
#19312=ORIENTED_EDGE('',*,*,#12982,.T.);
#19313=ORIENTED_EDGE('',*,*,#12987,.F.);
#19314=ORIENTED_EDGE('',*,*,#12988,.F.);
#19315=ORIENTED_EDGE('',*,*,#12989,.T.);
#19316=ORIENTED_EDGE('',*,*,#12985,.T.);
#19317=ORIENTED_EDGE('',*,*,#12990,.F.);
#19318=ORIENTED_EDGE('',*,*,#12991,.F.);
#19319=ORIENTED_EDGE('',*,*,#12992,.T.);
#19320=ORIENTED_EDGE('',*,*,#12988,.T.);
#19321=ORIENTED_EDGE('',*,*,#12993,.F.);
#19322=ORIENTED_EDGE('',*,*,#12994,.F.);
#19323=ORIENTED_EDGE('',*,*,#12995,.T.);
#19324=ORIENTED_EDGE('',*,*,#12991,.T.);
#19325=ORIENTED_EDGE('',*,*,#12996,.F.);
#19326=ORIENTED_EDGE('',*,*,#12997,.F.);
#19327=ORIENTED_EDGE('',*,*,#12998,.T.);
#19328=ORIENTED_EDGE('',*,*,#12994,.T.);
#19329=ORIENTED_EDGE('',*,*,#12999,.F.);
#19330=ORIENTED_EDGE('',*,*,#13000,.F.);
#19331=ORIENTED_EDGE('',*,*,#13001,.T.);
#19332=ORIENTED_EDGE('',*,*,#12997,.T.);
#19333=ORIENTED_EDGE('',*,*,#13002,.F.);
#19334=ORIENTED_EDGE('',*,*,#13003,.F.);
#19335=ORIENTED_EDGE('',*,*,#13004,.T.);
#19336=ORIENTED_EDGE('',*,*,#13000,.T.);
#19337=ORIENTED_EDGE('',*,*,#13005,.F.);
#19338=ORIENTED_EDGE('',*,*,#13006,.F.);
#19339=ORIENTED_EDGE('',*,*,#13007,.T.);
#19340=ORIENTED_EDGE('',*,*,#13003,.T.);
#19341=ORIENTED_EDGE('',*,*,#13008,.F.);
#19342=ORIENTED_EDGE('',*,*,#13009,.F.);
#19343=ORIENTED_EDGE('',*,*,#13010,.T.);
#19344=ORIENTED_EDGE('',*,*,#13006,.T.);
#19345=ORIENTED_EDGE('',*,*,#13011,.F.);
#19346=ORIENTED_EDGE('',*,*,#13012,.F.);
#19347=ORIENTED_EDGE('',*,*,#13013,.T.);
#19348=ORIENTED_EDGE('',*,*,#13009,.T.);
#19349=ORIENTED_EDGE('',*,*,#13014,.F.);
#19350=ORIENTED_EDGE('',*,*,#13015,.F.);
#19351=ORIENTED_EDGE('',*,*,#13016,.T.);
#19352=ORIENTED_EDGE('',*,*,#13012,.T.);
#19353=ORIENTED_EDGE('',*,*,#13017,.F.);
#19354=ORIENTED_EDGE('',*,*,#13018,.F.);
#19355=ORIENTED_EDGE('',*,*,#13019,.T.);
#19356=ORIENTED_EDGE('',*,*,#13015,.T.);
#19357=ORIENTED_EDGE('',*,*,#13020,.F.);
#19358=ORIENTED_EDGE('',*,*,#13021,.F.);
#19359=ORIENTED_EDGE('',*,*,#13022,.T.);
#19360=ORIENTED_EDGE('',*,*,#13018,.T.);
#19361=ORIENTED_EDGE('',*,*,#13023,.F.);
#19362=ORIENTED_EDGE('',*,*,#13024,.F.);
#19363=ORIENTED_EDGE('',*,*,#13025,.T.);
#19364=ORIENTED_EDGE('',*,*,#13021,.T.);
#19365=ORIENTED_EDGE('',*,*,#13026,.F.);
#19366=ORIENTED_EDGE('',*,*,#13027,.F.);
#19367=ORIENTED_EDGE('',*,*,#13028,.T.);
#19368=ORIENTED_EDGE('',*,*,#13024,.T.);
#19369=ORIENTED_EDGE('',*,*,#13029,.F.);
#19370=ORIENTED_EDGE('',*,*,#13030,.F.);
#19371=ORIENTED_EDGE('',*,*,#13031,.T.);
#19372=ORIENTED_EDGE('',*,*,#13027,.T.);
#19373=ORIENTED_EDGE('',*,*,#13032,.F.);
#19374=ORIENTED_EDGE('',*,*,#13033,.F.);
#19375=ORIENTED_EDGE('',*,*,#13034,.T.);
#19376=ORIENTED_EDGE('',*,*,#13030,.T.);
#19377=ORIENTED_EDGE('',*,*,#13035,.F.);
#19378=ORIENTED_EDGE('',*,*,#13036,.F.);
#19379=ORIENTED_EDGE('',*,*,#13037,.T.);
#19380=ORIENTED_EDGE('',*,*,#13033,.T.);
#19381=ORIENTED_EDGE('',*,*,#13038,.F.);
#19382=ORIENTED_EDGE('',*,*,#13039,.F.);
#19383=ORIENTED_EDGE('',*,*,#13040,.T.);
#19384=ORIENTED_EDGE('',*,*,#13036,.T.);
#19385=ORIENTED_EDGE('',*,*,#13041,.F.);
#19386=ORIENTED_EDGE('',*,*,#13042,.F.);
#19387=ORIENTED_EDGE('',*,*,#13043,.T.);
#19388=ORIENTED_EDGE('',*,*,#13039,.T.);
#19389=ORIENTED_EDGE('',*,*,#13044,.F.);
#19390=ORIENTED_EDGE('',*,*,#13045,.F.);
#19391=ORIENTED_EDGE('',*,*,#13046,.T.);
#19392=ORIENTED_EDGE('',*,*,#13042,.T.);
#19393=ORIENTED_EDGE('',*,*,#13047,.F.);
#19394=ORIENTED_EDGE('',*,*,#13048,.F.);
#19395=ORIENTED_EDGE('',*,*,#13049,.T.);
#19396=ORIENTED_EDGE('',*,*,#13045,.T.);
#19397=ORIENTED_EDGE('',*,*,#13050,.F.);
#19398=ORIENTED_EDGE('',*,*,#13051,.F.);
#19399=ORIENTED_EDGE('',*,*,#13052,.T.);
#19400=ORIENTED_EDGE('',*,*,#13048,.T.);
#19401=ORIENTED_EDGE('',*,*,#13053,.F.);
#19402=ORIENTED_EDGE('',*,*,#13054,.F.);
#19403=ORIENTED_EDGE('',*,*,#13055,.T.);
#19404=ORIENTED_EDGE('',*,*,#13051,.T.);
#19405=ORIENTED_EDGE('',*,*,#13056,.F.);
#19406=ORIENTED_EDGE('',*,*,#13057,.F.);
#19407=ORIENTED_EDGE('',*,*,#13058,.T.);
#19408=ORIENTED_EDGE('',*,*,#13054,.T.);
#19409=ORIENTED_EDGE('',*,*,#13059,.F.);
#19410=ORIENTED_EDGE('',*,*,#13060,.F.);
#19411=ORIENTED_EDGE('',*,*,#13061,.T.);
#19412=ORIENTED_EDGE('',*,*,#13057,.T.);
#19413=ORIENTED_EDGE('',*,*,#13062,.F.);
#19414=ORIENTED_EDGE('',*,*,#13063,.F.);
#19415=ORIENTED_EDGE('',*,*,#13064,.T.);
#19416=ORIENTED_EDGE('',*,*,#13060,.T.);
#19417=ORIENTED_EDGE('',*,*,#13065,.F.);
#19418=ORIENTED_EDGE('',*,*,#13066,.F.);
#19419=ORIENTED_EDGE('',*,*,#12920,.F.);
#19420=ORIENTED_EDGE('',*,*,#13067,.F.);
#19421=ORIENTED_EDGE('',*,*,#13068,.F.);
#19422=ORIENTED_EDGE('',*,*,#13069,.F.);
#19423=ORIENTED_EDGE('',*,*,#13070,.T.);
#19424=ORIENTED_EDGE('',*,*,#13071,.F.);
#19425=ORIENTED_EDGE('',*,*,#13070,.F.);
#19426=ORIENTED_EDGE('',*,*,#13067,.T.);
#19427=ORIENTED_EDGE('',*,*,#12919,.F.);
#19428=ORIENTED_EDGE('',*,*,#12923,.F.);
#19429=ORIENTED_EDGE('',*,*,#12926,.F.);
#19430=ORIENTED_EDGE('',*,*,#12929,.F.);
#19431=ORIENTED_EDGE('',*,*,#12932,.F.);
#19432=ORIENTED_EDGE('',*,*,#12935,.F.);
#19433=ORIENTED_EDGE('',*,*,#12938,.F.);
#19434=ORIENTED_EDGE('',*,*,#12941,.F.);
#19435=ORIENTED_EDGE('',*,*,#12944,.F.);
#19436=ORIENTED_EDGE('',*,*,#12947,.F.);
#19437=ORIENTED_EDGE('',*,*,#12950,.F.);
#19438=ORIENTED_EDGE('',*,*,#12953,.F.);
#19439=ORIENTED_EDGE('',*,*,#12956,.F.);
#19440=ORIENTED_EDGE('',*,*,#12959,.F.);
#19441=ORIENTED_EDGE('',*,*,#12962,.F.);
#19442=ORIENTED_EDGE('',*,*,#12965,.F.);
#19443=ORIENTED_EDGE('',*,*,#12968,.F.);
#19444=ORIENTED_EDGE('',*,*,#12971,.F.);
#19445=ORIENTED_EDGE('',*,*,#12974,.F.);
#19446=ORIENTED_EDGE('',*,*,#12977,.F.);
#19447=ORIENTED_EDGE('',*,*,#12980,.F.);
#19448=ORIENTED_EDGE('',*,*,#12983,.F.);
#19449=ORIENTED_EDGE('',*,*,#12986,.F.);
#19450=ORIENTED_EDGE('',*,*,#12989,.F.);
#19451=ORIENTED_EDGE('',*,*,#12992,.F.);
#19452=ORIENTED_EDGE('',*,*,#12995,.F.);
#19453=ORIENTED_EDGE('',*,*,#12998,.F.);
#19454=ORIENTED_EDGE('',*,*,#13001,.F.);
#19455=ORIENTED_EDGE('',*,*,#13004,.F.);
#19456=ORIENTED_EDGE('',*,*,#13007,.F.);
#19457=ORIENTED_EDGE('',*,*,#13010,.F.);
#19458=ORIENTED_EDGE('',*,*,#13013,.F.);
#19459=ORIENTED_EDGE('',*,*,#13016,.F.);
#19460=ORIENTED_EDGE('',*,*,#13019,.F.);
#19461=ORIENTED_EDGE('',*,*,#13022,.F.);
#19462=ORIENTED_EDGE('',*,*,#13025,.F.);
#19463=ORIENTED_EDGE('',*,*,#13028,.F.);
#19464=ORIENTED_EDGE('',*,*,#13031,.F.);
#19465=ORIENTED_EDGE('',*,*,#13034,.F.);
#19466=ORIENTED_EDGE('',*,*,#13037,.F.);
#19467=ORIENTED_EDGE('',*,*,#13040,.F.);
#19468=ORIENTED_EDGE('',*,*,#13043,.F.);
#19469=ORIENTED_EDGE('',*,*,#13046,.F.);
#19470=ORIENTED_EDGE('',*,*,#13049,.F.);
#19471=ORIENTED_EDGE('',*,*,#13052,.F.);
#19472=ORIENTED_EDGE('',*,*,#13055,.F.);
#19473=ORIENTED_EDGE('',*,*,#13058,.F.);
#19474=ORIENTED_EDGE('',*,*,#13061,.F.);
#19475=ORIENTED_EDGE('',*,*,#13064,.F.);
#19476=ORIENTED_EDGE('',*,*,#13072,.F.);
#19477=ORIENTED_EDGE('',*,*,#13073,.F.);
#19478=ORIENTED_EDGE('',*,*,#12771,.F.);
#19479=ORIENTED_EDGE('',*,*,#12775,.F.);
#19480=ORIENTED_EDGE('',*,*,#12778,.F.);
#19481=ORIENTED_EDGE('',*,*,#12781,.F.);
#19482=ORIENTED_EDGE('',*,*,#12784,.F.);
#19483=ORIENTED_EDGE('',*,*,#12787,.F.);
#19484=ORIENTED_EDGE('',*,*,#12790,.F.);
#19485=ORIENTED_EDGE('',*,*,#12793,.F.);
#19486=ORIENTED_EDGE('',*,*,#12796,.F.);
#19487=ORIENTED_EDGE('',*,*,#12799,.F.);
#19488=ORIENTED_EDGE('',*,*,#12802,.F.);
#19489=ORIENTED_EDGE('',*,*,#12805,.F.);
#19490=ORIENTED_EDGE('',*,*,#12808,.F.);
#19491=ORIENTED_EDGE('',*,*,#12811,.F.);
#19492=ORIENTED_EDGE('',*,*,#12814,.F.);
#19493=ORIENTED_EDGE('',*,*,#12817,.F.);
#19494=ORIENTED_EDGE('',*,*,#12820,.F.);
#19495=ORIENTED_EDGE('',*,*,#12823,.F.);
#19496=ORIENTED_EDGE('',*,*,#12826,.F.);
#19497=ORIENTED_EDGE('',*,*,#12829,.F.);
#19498=ORIENTED_EDGE('',*,*,#12832,.F.);
#19499=ORIENTED_EDGE('',*,*,#12835,.F.);
#19500=ORIENTED_EDGE('',*,*,#12838,.F.);
#19501=ORIENTED_EDGE('',*,*,#12841,.F.);
#19502=ORIENTED_EDGE('',*,*,#12844,.F.);
#19503=ORIENTED_EDGE('',*,*,#12847,.F.);
#19504=ORIENTED_EDGE('',*,*,#12850,.F.);
#19505=ORIENTED_EDGE('',*,*,#12853,.F.);
#19506=ORIENTED_EDGE('',*,*,#12856,.F.);
#19507=ORIENTED_EDGE('',*,*,#12859,.F.);
#19508=ORIENTED_EDGE('',*,*,#12862,.F.);
#19509=ORIENTED_EDGE('',*,*,#12865,.F.);
#19510=ORIENTED_EDGE('',*,*,#12868,.F.);
#19511=ORIENTED_EDGE('',*,*,#12871,.F.);
#19512=ORIENTED_EDGE('',*,*,#12874,.F.);
#19513=ORIENTED_EDGE('',*,*,#12877,.F.);
#19514=ORIENTED_EDGE('',*,*,#12880,.F.);
#19515=ORIENTED_EDGE('',*,*,#12883,.F.);
#19516=ORIENTED_EDGE('',*,*,#12886,.F.);
#19517=ORIENTED_EDGE('',*,*,#12889,.F.);
#19518=ORIENTED_EDGE('',*,*,#12892,.F.);
#19519=ORIENTED_EDGE('',*,*,#12895,.F.);
#19520=ORIENTED_EDGE('',*,*,#12898,.F.);
#19521=ORIENTED_EDGE('',*,*,#12901,.F.);
#19522=ORIENTED_EDGE('',*,*,#12904,.F.);
#19523=ORIENTED_EDGE('',*,*,#12907,.F.);
#19524=ORIENTED_EDGE('',*,*,#12910,.F.);
#19525=ORIENTED_EDGE('',*,*,#12913,.F.);
#19526=ORIENTED_EDGE('',*,*,#12916,.F.);
#19527=ORIENTED_EDGE('',*,*,#13074,.F.);
#19528=ORIENTED_EDGE('',*,*,#13063,.T.);
#19529=ORIENTED_EDGE('',*,*,#13075,.F.);
#19530=ORIENTED_EDGE('',*,*,#13076,.F.);
#19531=ORIENTED_EDGE('',*,*,#13072,.T.);
#19532=ORIENTED_EDGE('',*,*,#13066,.T.);
#19533=ORIENTED_EDGE('',*,*,#13069,.T.);
#19534=ORIENTED_EDGE('',*,*,#13077,.F.);
#19535=ORIENTED_EDGE('',*,*,#12917,.F.);
#19536=ORIENTED_EDGE('',*,*,#12914,.F.);
#19537=ORIENTED_EDGE('',*,*,#12911,.F.);
#19538=ORIENTED_EDGE('',*,*,#12908,.F.);
#19539=ORIENTED_EDGE('',*,*,#12905,.F.);
#19540=ORIENTED_EDGE('',*,*,#12902,.F.);
#19541=ORIENTED_EDGE('',*,*,#12899,.F.);
#19542=ORIENTED_EDGE('',*,*,#12896,.F.);
#19543=ORIENTED_EDGE('',*,*,#12893,.F.);
#19544=ORIENTED_EDGE('',*,*,#12890,.F.);
#19545=ORIENTED_EDGE('',*,*,#12887,.F.);
#19546=ORIENTED_EDGE('',*,*,#12884,.F.);
#19547=ORIENTED_EDGE('',*,*,#12881,.F.);
#19548=ORIENTED_EDGE('',*,*,#12878,.F.);
#19549=ORIENTED_EDGE('',*,*,#12875,.F.);
#19550=ORIENTED_EDGE('',*,*,#12872,.F.);
#19551=ORIENTED_EDGE('',*,*,#12869,.F.);
#19552=ORIENTED_EDGE('',*,*,#12866,.F.);
#19553=ORIENTED_EDGE('',*,*,#12863,.F.);
#19554=ORIENTED_EDGE('',*,*,#12860,.F.);
#19555=ORIENTED_EDGE('',*,*,#12857,.F.);
#19556=ORIENTED_EDGE('',*,*,#12854,.F.);
#19557=ORIENTED_EDGE('',*,*,#12851,.F.);
#19558=ORIENTED_EDGE('',*,*,#12848,.F.);
#19559=ORIENTED_EDGE('',*,*,#12845,.F.);
#19560=ORIENTED_EDGE('',*,*,#12842,.F.);
#19561=ORIENTED_EDGE('',*,*,#12839,.F.);
#19562=ORIENTED_EDGE('',*,*,#12836,.F.);
#19563=ORIENTED_EDGE('',*,*,#12833,.F.);
#19564=ORIENTED_EDGE('',*,*,#12830,.F.);
#19565=ORIENTED_EDGE('',*,*,#12827,.F.);
#19566=ORIENTED_EDGE('',*,*,#12824,.F.);
#19567=ORIENTED_EDGE('',*,*,#12821,.F.);
#19568=ORIENTED_EDGE('',*,*,#12818,.F.);
#19569=ORIENTED_EDGE('',*,*,#12815,.F.);
#19570=ORIENTED_EDGE('',*,*,#12812,.F.);
#19571=ORIENTED_EDGE('',*,*,#12809,.F.);
#19572=ORIENTED_EDGE('',*,*,#12806,.F.);
#19573=ORIENTED_EDGE('',*,*,#12803,.F.);
#19574=ORIENTED_EDGE('',*,*,#12800,.F.);
#19575=ORIENTED_EDGE('',*,*,#12797,.F.);
#19576=ORIENTED_EDGE('',*,*,#12794,.F.);
#19577=ORIENTED_EDGE('',*,*,#12791,.F.);
#19578=ORIENTED_EDGE('',*,*,#12788,.F.);
#19579=ORIENTED_EDGE('',*,*,#12785,.F.);
#19580=ORIENTED_EDGE('',*,*,#12782,.F.);
#19581=ORIENTED_EDGE('',*,*,#12779,.F.);
#19582=ORIENTED_EDGE('',*,*,#12776,.F.);
#19583=ORIENTED_EDGE('',*,*,#12773,.F.);
#19584=ORIENTED_EDGE('',*,*,#13078,.F.);
#19585=ORIENTED_EDGE('',*,*,#13075,.T.);
#19586=ORIENTED_EDGE('',*,*,#13065,.T.);
#19587=ORIENTED_EDGE('',*,*,#13062,.T.);
#19588=ORIENTED_EDGE('',*,*,#13059,.T.);
#19589=ORIENTED_EDGE('',*,*,#13056,.T.);
#19590=ORIENTED_EDGE('',*,*,#13053,.T.);
#19591=ORIENTED_EDGE('',*,*,#13050,.T.);
#19592=ORIENTED_EDGE('',*,*,#13047,.T.);
#19593=ORIENTED_EDGE('',*,*,#13044,.T.);
#19594=ORIENTED_EDGE('',*,*,#13041,.T.);
#19595=ORIENTED_EDGE('',*,*,#13038,.T.);
#19596=ORIENTED_EDGE('',*,*,#13035,.T.);
#19597=ORIENTED_EDGE('',*,*,#13032,.T.);
#19598=ORIENTED_EDGE('',*,*,#13029,.T.);
#19599=ORIENTED_EDGE('',*,*,#13026,.T.);
#19600=ORIENTED_EDGE('',*,*,#13023,.T.);
#19601=ORIENTED_EDGE('',*,*,#13020,.T.);
#19602=ORIENTED_EDGE('',*,*,#13017,.T.);
#19603=ORIENTED_EDGE('',*,*,#13014,.T.);
#19604=ORIENTED_EDGE('',*,*,#13011,.T.);
#19605=ORIENTED_EDGE('',*,*,#13008,.T.);
#19606=ORIENTED_EDGE('',*,*,#13005,.T.);
#19607=ORIENTED_EDGE('',*,*,#13002,.T.);
#19608=ORIENTED_EDGE('',*,*,#12999,.T.);
#19609=ORIENTED_EDGE('',*,*,#12996,.T.);
#19610=ORIENTED_EDGE('',*,*,#12993,.T.);
#19611=ORIENTED_EDGE('',*,*,#12990,.T.);
#19612=ORIENTED_EDGE('',*,*,#12987,.T.);
#19613=ORIENTED_EDGE('',*,*,#12984,.T.);
#19614=ORIENTED_EDGE('',*,*,#12981,.T.);
#19615=ORIENTED_EDGE('',*,*,#12978,.T.);
#19616=ORIENTED_EDGE('',*,*,#12975,.T.);
#19617=ORIENTED_EDGE('',*,*,#12972,.T.);
#19618=ORIENTED_EDGE('',*,*,#12969,.T.);
#19619=ORIENTED_EDGE('',*,*,#12966,.T.);
#19620=ORIENTED_EDGE('',*,*,#12963,.T.);
#19621=ORIENTED_EDGE('',*,*,#12960,.T.);
#19622=ORIENTED_EDGE('',*,*,#12957,.T.);
#19623=ORIENTED_EDGE('',*,*,#12954,.T.);
#19624=ORIENTED_EDGE('',*,*,#12951,.T.);
#19625=ORIENTED_EDGE('',*,*,#12948,.T.);
#19626=ORIENTED_EDGE('',*,*,#12945,.T.);
#19627=ORIENTED_EDGE('',*,*,#12942,.T.);
#19628=ORIENTED_EDGE('',*,*,#12939,.T.);
#19629=ORIENTED_EDGE('',*,*,#12936,.T.);
#19630=ORIENTED_EDGE('',*,*,#12933,.T.);
#19631=ORIENTED_EDGE('',*,*,#12930,.T.);
#19632=ORIENTED_EDGE('',*,*,#12927,.T.);
#19633=ORIENTED_EDGE('',*,*,#12924,.T.);
#19634=ORIENTED_EDGE('',*,*,#12921,.T.);
#19635=ORIENTED_EDGE('',*,*,#12915,.T.);
#19636=ORIENTED_EDGE('',*,*,#13077,.T.);
#19637=ORIENTED_EDGE('',*,*,#13068,.T.);
#19638=ORIENTED_EDGE('',*,*,#13074,.T.);
#19639=ORIENTED_EDGE('',*,*,#13079,.F.);
#19640=ORIENTED_EDGE('',*,*,#13080,.T.);
#19641=ORIENTED_EDGE('',*,*,#13081,.T.);
#19642=ORIENTED_EDGE('',*,*,#13082,.F.);
#19643=ORIENTED_EDGE('',*,*,#13083,.F.);
#19644=ORIENTED_EDGE('',*,*,#13084,.T.);
#19645=ORIENTED_EDGE('',*,*,#13085,.T.);
#19646=ORIENTED_EDGE('',*,*,#13080,.F.);
#19647=ORIENTED_EDGE('',*,*,#13086,.F.);
#19648=ORIENTED_EDGE('',*,*,#13087,.T.);
#19649=ORIENTED_EDGE('',*,*,#13088,.T.);
#19650=ORIENTED_EDGE('',*,*,#13084,.F.);
#19651=ORIENTED_EDGE('',*,*,#13089,.F.);
#19652=ORIENTED_EDGE('',*,*,#13090,.T.);
#19653=ORIENTED_EDGE('',*,*,#13091,.T.);
#19654=ORIENTED_EDGE('',*,*,#13087,.F.);
#19655=ORIENTED_EDGE('',*,*,#13092,.F.);
#19656=ORIENTED_EDGE('',*,*,#13093,.T.);
#19657=ORIENTED_EDGE('',*,*,#13094,.T.);
#19658=ORIENTED_EDGE('',*,*,#13090,.F.);
#19659=ORIENTED_EDGE('',*,*,#13095,.F.);
#19660=ORIENTED_EDGE('',*,*,#13082,.T.);
#19661=ORIENTED_EDGE('',*,*,#13096,.T.);
#19662=ORIENTED_EDGE('',*,*,#13093,.F.);
#19663=ORIENTED_EDGE('',*,*,#13096,.F.);
#19664=ORIENTED_EDGE('',*,*,#13081,.F.);
#19665=ORIENTED_EDGE('',*,*,#13085,.F.);
#19666=ORIENTED_EDGE('',*,*,#13088,.F.);
#19667=ORIENTED_EDGE('',*,*,#13091,.F.);
#19668=ORIENTED_EDGE('',*,*,#13094,.F.);
#19669=ORIENTED_EDGE('',*,*,#13097,.T.);
#19670=ORIENTED_EDGE('',*,*,#13073,.T.);
#19671=ORIENTED_EDGE('',*,*,#13076,.T.);
#19672=ORIENTED_EDGE('',*,*,#13078,.T.);
#19673=ORIENTED_EDGE('',*,*,#12772,.F.);
#19674=ORIENTED_EDGE('',*,*,#13097,.F.);
#19675=ORIENTED_EDGE('',*,*,#13098,.T.);
#19676=ORIENTED_EDGE('',*,*,#13099,.T.);
#19677=ORIENTED_EDGE('',*,*,#13098,.F.);
#19678=ORIENTED_EDGE('',*,*,#13099,.F.);
#19679=ORIENTED_EDGE('',*,*,#13079,.T.);
#19680=ORIENTED_EDGE('',*,*,#13095,.T.);
#19681=ORIENTED_EDGE('',*,*,#13092,.T.);
#19682=ORIENTED_EDGE('',*,*,#13089,.T.);
#19683=ORIENTED_EDGE('',*,*,#13086,.T.);
#19684=ORIENTED_EDGE('',*,*,#13083,.T.);
#19685=ORIENTED_EDGE('',*,*,#13071,.T.);
#20552=CYLINDRICAL_SURFACE('',#23326,2.942);
#20553=CYLINDRICAL_SURFACE('',#23328,2.942);
#20554=CYLINDRICAL_SURFACE('',#23329,2.942);
#20555=CYLINDRICAL_SURFACE('',#23330,2.942);
#20556=CYLINDRICAL_SURFACE('',#23331,2.942);
#20557=CYLINDRICAL_SURFACE('',#23332,2.942);
#20558=CYLINDRICAL_SURFACE('',#23333,2.942);
#20559=CYLINDRICAL_SURFACE('',#23334,2.942);
#20560=CYLINDRICAL_SURFACE('',#23335,2.942);
#20561=CYLINDRICAL_SURFACE('',#23336,2.942);
#20562=CYLINDRICAL_SURFACE('',#23337,2.942);
#20563=CYLINDRICAL_SURFACE('',#23338,2.942);
#20564=CYLINDRICAL_SURFACE('',#23339,2.942);
#20565=CYLINDRICAL_SURFACE('',#23340,2.942);
#20566=CYLINDRICAL_SURFACE('',#23341,2.942);
#20567=CYLINDRICAL_SURFACE('',#23342,2.942);
#20568=CYLINDRICAL_SURFACE('',#23343,2.942);
#20569=CYLINDRICAL_SURFACE('',#23344,2.942);
#20570=CYLINDRICAL_SURFACE('',#23345,2.942);
#20571=CYLINDRICAL_SURFACE('',#23346,2.942);
#20572=CYLINDRICAL_SURFACE('',#23347,2.942);
#20573=CYLINDRICAL_SURFACE('',#23348,2.942);
#20574=CYLINDRICAL_SURFACE('',#23349,2.942);
#20575=CYLINDRICAL_SURFACE('',#23350,2.942);
#20576=CYLINDRICAL_SURFACE('',#23351,2.942);
#20577=CYLINDRICAL_SURFACE('',#23352,2.942);
#20578=CYLINDRICAL_SURFACE('',#23353,2.942);
#20579=CYLINDRICAL_SURFACE('',#23354,2.942);
#20580=CYLINDRICAL_SURFACE('',#23355,2.942);
#20581=CYLINDRICAL_SURFACE('',#23356,2.942);
#20582=CYLINDRICAL_SURFACE('',#23357,2.942);
#20583=CYLINDRICAL_SURFACE('',#23358,2.942);
#20584=CYLINDRICAL_SURFACE('',#23359,2.942);
#20585=CYLINDRICAL_SURFACE('',#23360,2.942);
#20586=CYLINDRICAL_SURFACE('',#23361,2.942);
#20587=CYLINDRICAL_SURFACE('',#23362,2.942);
#20588=CYLINDRICAL_SURFACE('',#23363,2.942);
#20589=CYLINDRICAL_SURFACE('',#23364,2.942);
#20590=CYLINDRICAL_SURFACE('',#23365,2.942);
#20591=CYLINDRICAL_SURFACE('',#23366,2.942);
#20592=CYLINDRICAL_SURFACE('',#23367,2.942);
#20593=CYLINDRICAL_SURFACE('',#23368,2.942);
#20594=CYLINDRICAL_SURFACE('',#23369,2.942);
#20595=CYLINDRICAL_SURFACE('',#23370,2.942);
#20596=CYLINDRICAL_SURFACE('',#23371,2.942);
#20597=CYLINDRICAL_SURFACE('',#23372,2.942);
#20598=CYLINDRICAL_SURFACE('',#23373,2.942);
#20599=CYLINDRICAL_SURFACE('',#23374,2.942);
#20600=CYLINDRICAL_SURFACE('',#23375,2.942);
#20601=CYLINDRICAL_SURFACE('',#23376,2.37175);
#20602=CYLINDRICAL_SURFACE('',#23378,2.37175);
#20603=CYLINDRICAL_SURFACE('',#23379,2.37175);
#20604=CYLINDRICAL_SURFACE('',#23380,2.37175);
#20605=CYLINDRICAL_SURFACE('',#23381,2.37175);
#20606=CYLINDRICAL_SURFACE('',#23382,2.37175);
#20607=CYLINDRICAL_SURFACE('',#23383,2.37175);
#20608=CYLINDRICAL_SURFACE('',#23384,2.37175);
#20609=CYLINDRICAL_SURFACE('',#23385,2.37175);
#20610=CYLINDRICAL_SURFACE('',#23386,2.37175);
#20611=CYLINDRICAL_SURFACE('',#23387,2.37175);
#20612=CYLINDRICAL_SURFACE('',#23388,2.37175);
#20613=CYLINDRICAL_SURFACE('',#23389,2.37175);
#20614=CYLINDRICAL_SURFACE('',#23390,2.37175);
#20615=CYLINDRICAL_SURFACE('',#23391,2.37175);
#20616=CYLINDRICAL_SURFACE('',#23392,2.37175);
#20617=CYLINDRICAL_SURFACE('',#23393,2.37175);
#20618=CYLINDRICAL_SURFACE('',#23394,2.37175);
#20619=CYLINDRICAL_SURFACE('',#23395,2.37175);
#20620=CYLINDRICAL_SURFACE('',#23396,2.37175);
#20621=CYLINDRICAL_SURFACE('',#23397,2.37175);
#20622=CYLINDRICAL_SURFACE('',#23398,2.37175);
#20623=CYLINDRICAL_SURFACE('',#23399,2.37175);
#20624=CYLINDRICAL_SURFACE('',#23400,2.37175);
#20625=CYLINDRICAL_SURFACE('',#23401,2.37175);
#20626=CYLINDRICAL_SURFACE('',#23402,2.37175);
#20627=CYLINDRICAL_SURFACE('',#23403,2.37175);
#20628=CYLINDRICAL_SURFACE('',#23404,2.37175);
#20629=CYLINDRICAL_SURFACE('',#23405,2.37175);
#20630=CYLINDRICAL_SURFACE('',#23406,2.37175);
#20631=CYLINDRICAL_SURFACE('',#23407,2.37175);
#20632=CYLINDRICAL_SURFACE('',#23408,2.37175);
#20633=CYLINDRICAL_SURFACE('',#23409,2.37175);
#20634=CYLINDRICAL_SURFACE('',#23410,2.37175);
#20635=CYLINDRICAL_SURFACE('',#23411,2.37175);
#20636=CYLINDRICAL_SURFACE('',#23412,2.37175);
#20637=CYLINDRICAL_SURFACE('',#23413,2.37175);
#20638=CYLINDRICAL_SURFACE('',#23414,2.37175);
#20639=CYLINDRICAL_SURFACE('',#23415,2.37175);
#20640=CYLINDRICAL_SURFACE('',#23416,2.37175);
#20641=CYLINDRICAL_SURFACE('',#23417,2.37175);
#20642=CYLINDRICAL_SURFACE('',#23418,2.37175);
#20643=CYLINDRICAL_SURFACE('',#23419,2.37175);
#20644=CYLINDRICAL_SURFACE('',#23420,2.37175);
#20645=CYLINDRICAL_SURFACE('',#23421,2.37175);
#20646=CYLINDRICAL_SURFACE('',#23422,2.37175);
#20647=CYLINDRICAL_SURFACE('',#23423,2.37175);
#20648=CYLINDRICAL_SURFACE('',#23424,2.37175);
#20649=CYLINDRICAL_SURFACE('',#23425,2.37175);
#20650=CYLINDRICAL_SURFACE('',#23429,2.37175);
#20651=CYLINDRICAL_SURFACE('',#23431,2.942);
#20652=CYLINDRICAL_SURFACE('',#23441,5.);
#21689=ADVANCED_FACE('',(#3569),#20552,.T.);
#21690=ADVANCED_FACE('',(#3570),#20553,.T.);
#21691=ADVANCED_FACE('',(#3571),#20554,.T.);
#21692=ADVANCED_FACE('',(#3572),#20555,.T.);
#21693=ADVANCED_FACE('',(#3573),#20556,.T.);
#21694=ADVANCED_FACE('',(#3574),#20557,.T.);
#21695=ADVANCED_FACE('',(#3575),#20558,.T.);
#21696=ADVANCED_FACE('',(#3576),#20559,.T.);
#21697=ADVANCED_FACE('',(#3577),#20560,.T.);
#21698=ADVANCED_FACE('',(#3578),#20561,.T.);
#21699=ADVANCED_FACE('',(#3579),#20562,.T.);
#21700=ADVANCED_FACE('',(#3580),#20563,.T.);
#21701=ADVANCED_FACE('',(#3581),#20564,.T.);
#21702=ADVANCED_FACE('',(#3582),#20565,.T.);
#21703=ADVANCED_FACE('',(#3583),#20566,.T.);
#21704=ADVANCED_FACE('',(#3584),#20567,.T.);
#21705=ADVANCED_FACE('',(#3585),#20568,.T.);
#21706=ADVANCED_FACE('',(#3586),#20569,.T.);
#21707=ADVANCED_FACE('',(#3587),#20570,.T.);
#21708=ADVANCED_FACE('',(#3588),#20571,.T.);
#21709=ADVANCED_FACE('',(#3589),#20572,.T.);
#21710=ADVANCED_FACE('',(#3590),#20573,.T.);
#21711=ADVANCED_FACE('',(#3591),#20574,.T.);
#21712=ADVANCED_FACE('',(#3592),#20575,.T.);
#21713=ADVANCED_FACE('',(#3593),#20576,.T.);
#21714=ADVANCED_FACE('',(#3594),#20577,.T.);
#21715=ADVANCED_FACE('',(#3595),#20578,.T.);
#21716=ADVANCED_FACE('',(#3596),#20579,.T.);
#21717=ADVANCED_FACE('',(#3597),#20580,.T.);
#21718=ADVANCED_FACE('',(#3598),#20581,.T.);
#21719=ADVANCED_FACE('',(#3599),#20582,.T.);
#21720=ADVANCED_FACE('',(#3600),#20583,.T.);
#21721=ADVANCED_FACE('',(#3601),#20584,.T.);
#21722=ADVANCED_FACE('',(#3602),#20585,.T.);
#21723=ADVANCED_FACE('',(#3603),#20586,.T.);
#21724=ADVANCED_FACE('',(#3604),#20587,.T.);
#21725=ADVANCED_FACE('',(#3605),#20588,.T.);
#21726=ADVANCED_FACE('',(#3606),#20589,.T.);
#21727=ADVANCED_FACE('',(#3607),#20590,.T.);
#21728=ADVANCED_FACE('',(#3608),#20591,.T.);
#21729=ADVANCED_FACE('',(#3609),#20592,.T.);
#21730=ADVANCED_FACE('',(#3610),#20593,.T.);
#21731=ADVANCED_FACE('',(#3611),#20594,.T.);
#21732=ADVANCED_FACE('',(#3612),#20595,.T.);
#21733=ADVANCED_FACE('',(#3613),#20596,.T.);
#21734=ADVANCED_FACE('',(#3614),#20597,.T.);
#21735=ADVANCED_FACE('',(#3615),#20598,.T.);
#21736=ADVANCED_FACE('',(#3616),#20599,.T.);
#21737=ADVANCED_FACE('',(#3617),#20600,.T.);
#21738=ADVANCED_FACE('',(#3618),#20601,.T.);
#21739=ADVANCED_FACE('',(#3619),#20602,.T.);
#21740=ADVANCED_FACE('',(#3620),#20603,.T.);
#21741=ADVANCED_FACE('',(#3621),#20604,.T.);
#21742=ADVANCED_FACE('',(#3622),#20605,.T.);
#21743=ADVANCED_FACE('',(#3623),#20606,.T.);
#21744=ADVANCED_FACE('',(#3624),#20607,.T.);
#21745=ADVANCED_FACE('',(#3625),#20608,.T.);
#21746=ADVANCED_FACE('',(#3626),#20609,.T.);
#21747=ADVANCED_FACE('',(#3627),#20610,.T.);
#21748=ADVANCED_FACE('',(#3628),#20611,.T.);
#21749=ADVANCED_FACE('',(#3629),#20612,.T.);
#21750=ADVANCED_FACE('',(#3630),#20613,.T.);
#21751=ADVANCED_FACE('',(#3631),#20614,.T.);
#21752=ADVANCED_FACE('',(#3632),#20615,.T.);
#21753=ADVANCED_FACE('',(#3633),#20616,.T.);
#21754=ADVANCED_FACE('',(#3634),#20617,.T.);
#21755=ADVANCED_FACE('',(#3635),#20618,.T.);
#21756=ADVANCED_FACE('',(#3636),#20619,.T.);
#21757=ADVANCED_FACE('',(#3637),#20620,.T.);
#21758=ADVANCED_FACE('',(#3638),#20621,.T.);
#21759=ADVANCED_FACE('',(#3639),#20622,.T.);
#21760=ADVANCED_FACE('',(#3640),#20623,.T.);
#21761=ADVANCED_FACE('',(#3641),#20624,.T.);
#21762=ADVANCED_FACE('',(#3642),#20625,.T.);
#21763=ADVANCED_FACE('',(#3643),#20626,.T.);
#21764=ADVANCED_FACE('',(#3644),#20627,.T.);
#21765=ADVANCED_FACE('',(#3645),#20628,.T.);
#21766=ADVANCED_FACE('',(#3646),#20629,.T.);
#21767=ADVANCED_FACE('',(#3647),#20630,.T.);
#21768=ADVANCED_FACE('',(#3648),#20631,.T.);
#21769=ADVANCED_FACE('',(#3649),#20632,.T.);
#21770=ADVANCED_FACE('',(#3650),#20633,.T.);
#21771=ADVANCED_FACE('',(#3651),#20634,.T.);
#21772=ADVANCED_FACE('',(#3652),#20635,.T.);
#21773=ADVANCED_FACE('',(#3653),#20636,.T.);
#21774=ADVANCED_FACE('',(#3654),#20637,.T.);
#21775=ADVANCED_FACE('',(#3655),#20638,.T.);
#21776=ADVANCED_FACE('',(#3656),#20639,.T.);
#21777=ADVANCED_FACE('',(#3657),#20640,.T.);
#21778=ADVANCED_FACE('',(#3658),#20641,.T.);
#21779=ADVANCED_FACE('',(#3659),#20642,.T.);
#21780=ADVANCED_FACE('',(#3660),#20643,.T.);
#21781=ADVANCED_FACE('',(#3661),#20644,.T.);
#21782=ADVANCED_FACE('',(#3662),#20645,.T.);
#21783=ADVANCED_FACE('',(#3663),#20646,.T.);
#21784=ADVANCED_FACE('',(#3664),#20647,.T.);
#21785=ADVANCED_FACE('',(#3665),#20648,.T.);
#21786=ADVANCED_FACE('',(#3666),#20649,.T.);
#21787=ADVANCED_FACE('',(#3667),#333,.T.);
#21788=ADVANCED_FACE('',(#3668),#374,.F.);
#21789=ADVANCED_FACE('',(#3669),#20650,.T.);
#21790=ADVANCED_FACE('',(#3670),#375,.F.);
#21791=ADVANCED_FACE('',(#3671),#20651,.T.);
#21792=ADVANCED_FACE('',(#3672),#2523,.F.);
#21793=ADVANCED_FACE('',(#3673),#2524,.F.);
#21794=ADVANCED_FACE('',(#3674),#2525,.F.);
#21795=ADVANCED_FACE('',(#3675),#2526,.F.);
#21796=ADVANCED_FACE('',(#3676),#2527,.F.);
#21797=ADVANCED_FACE('',(#3677),#2528,.F.);
#21798=ADVANCED_FACE('',(#3678),#2529,.F.);
#21799=ADVANCED_FACE('',(#3679,#2373),#2530,.T.);
#21800=ADVANCED_FACE('',(#3680),#20652,.T.);
#21801=ADVANCED_FACE('',(#3681,#2374),#2531,.F.);
#21802=ADVANCED_FACE('',(#3682),#2532,.T.);
#21827=CLOSED_SHELL('',(#21689,#21690,#21691,#21692,#21693,#21694,#21695,
#21696,#21697,#21698,#21699,#21700,#21701,#21702,#21703,#21704,#21705,#21706,
#21707,#21708,#21709,#21710,#21711,#21712,#21713,#21714,#21715,#21716,#21717,
#21718,#21719,#21720,#21721,#21722,#21723,#21724,#21725,#21726,#21727,#21728,
#21729,#21730,#21731,#21732,#21733,#21734,#21735,#21736,#21737,#21738,#21739,
#21740,#21741,#21742,#21743,#21744,#21745,#21746,#21747,#21748,#21749,#21750,
#21751,#21752,#21753,#21754,#21755,#21756,#21757,#21758,#21759,#21760,#21761,
#21762,#21763,#21764,#21765,#21766,#21767,#21768,#21769,#21770,#21771,#21772,
#21773,#21774,#21775,#21776,#21777,#21778,#21779,#21780,#21781,#21782,#21783,
#21784,#21785,#21786,#21787,#21788,#21789,#21790,#21791,#21792,#21793,#21794,
#21795,#21796,#21797,#21798,#21799,#21800,#21801,#21802));
#23325=AXIS2_PLACEMENT_3D('',#90611,#27164,#27165);
#23326=AXIS2_PLACEMENT_3D('',#90612,#27166,#27167);
#23327=AXIS2_PLACEMENT_3D('',#90628,#27169,#27170);
#23328=AXIS2_PLACEMENT_3D('',#90636,#27171,#27172);
#23329=AXIS2_PLACEMENT_3D('',#90684,#27174,#27175);
#23330=AXIS2_PLACEMENT_3D('',#90732,#27177,#27178);
#23331=AXIS2_PLACEMENT_3D('',#90780,#27180,#27181);
#23332=AXIS2_PLACEMENT_3D('',#90834,#27183,#27184);
#23333=AXIS2_PLACEMENT_3D('',#90882,#27186,#27187);
#23334=AXIS2_PLACEMENT_3D('',#90930,#27189,#27190);
#23335=AXIS2_PLACEMENT_3D('',#90984,#27192,#27193);
#23336=AXIS2_PLACEMENT_3D('',#91032,#27195,#27196);
#23337=AXIS2_PLACEMENT_3D('',#91080,#27198,#27199);
#23338=AXIS2_PLACEMENT_3D('',#91128,#27201,#27202);
#23339=AXIS2_PLACEMENT_3D('',#91182,#27204,#27205);
#23340=AXIS2_PLACEMENT_3D('',#91230,#27207,#27208);
#23341=AXIS2_PLACEMENT_3D('',#91278,#27210,#27211);
#23342=AXIS2_PLACEMENT_3D('',#91332,#27213,#27214);
#23343=AXIS2_PLACEMENT_3D('',#91380,#27216,#27217);
#23344=AXIS2_PLACEMENT_3D('',#91428,#27219,#27220);
#23345=AXIS2_PLACEMENT_3D('',#91476,#27222,#27223);
#23346=AXIS2_PLACEMENT_3D('',#91530,#27225,#27226);
#23347=AXIS2_PLACEMENT_3D('',#91578,#27228,#27229);
#23348=AXIS2_PLACEMENT_3D('',#91626,#27231,#27232);
#23349=AXIS2_PLACEMENT_3D('',#91680,#27234,#27235);
#23350=AXIS2_PLACEMENT_3D('',#91728,#27237,#27238);
#23351=AXIS2_PLACEMENT_3D('',#91776,#27240,#27241);
#23352=AXIS2_PLACEMENT_3D('',#91824,#27243,#27244);
#23353=AXIS2_PLACEMENT_3D('',#91878,#27246,#27247);
#23354=AXIS2_PLACEMENT_3D('',#91926,#27249,#27250);
#23355=AXIS2_PLACEMENT_3D('',#91974,#27252,#27253);
#23356=AXIS2_PLACEMENT_3D('',#92028,#27255,#27256);
#23357=AXIS2_PLACEMENT_3D('',#92076,#27258,#27259);
#23358=AXIS2_PLACEMENT_3D('',#92124,#27261,#27262);
#23359=AXIS2_PLACEMENT_3D('',#92172,#27264,#27265);
#23360=AXIS2_PLACEMENT_3D('',#92226,#27267,#27268);
#23361=AXIS2_PLACEMENT_3D('',#92274,#27270,#27271);
#23362=AXIS2_PLACEMENT_3D('',#92322,#27273,#27274);
#23363=AXIS2_PLACEMENT_3D('',#92376,#27276,#27277);
#23364=AXIS2_PLACEMENT_3D('',#92424,#27279,#27280);
#23365=AXIS2_PLACEMENT_3D('',#92472,#27282,#27283);
#23366=AXIS2_PLACEMENT_3D('',#92520,#27285,#27286);
#23367=AXIS2_PLACEMENT_3D('',#92574,#27288,#27289);
#23368=AXIS2_PLACEMENT_3D('',#92622,#27291,#27292);
#23369=AXIS2_PLACEMENT_3D('',#92670,#27294,#27295);
#23370=AXIS2_PLACEMENT_3D('',#92724,#27297,#27298);
#23371=AXIS2_PLACEMENT_3D('',#92772,#27300,#27301);
#23372=AXIS2_PLACEMENT_3D('',#92820,#27303,#27304);
#23373=AXIS2_PLACEMENT_3D('',#92868,#27306,#27307);
#23374=AXIS2_PLACEMENT_3D('',#92919,#27309,#27310);
#23375=AXIS2_PLACEMENT_3D('',#92967,#27312,#27313);
#23376=AXIS2_PLACEMENT_3D('',#93015,#27315,#27316);
#23377=AXIS2_PLACEMENT_3D('',#93031,#27318,#27319);
#23378=AXIS2_PLACEMENT_3D('',#93040,#27320,#27321);
#23379=AXIS2_PLACEMENT_3D('',#93065,#27323,#27324);
#23380=AXIS2_PLACEMENT_3D('',#93089,#27326,#27327);
#23381=AXIS2_PLACEMENT_3D('',#93114,#27329,#27330);
#23382=AXIS2_PLACEMENT_3D('',#93139,#27332,#27333);
#23383=AXIS2_PLACEMENT_3D('',#93163,#27335,#27336);
#23384=AXIS2_PLACEMENT_3D('',#93187,#27338,#27339);
#23385=AXIS2_PLACEMENT_3D('',#93212,#27341,#27342);
#23386=AXIS2_PLACEMENT_3D('',#93237,#27344,#27345);
#23387=AXIS2_PLACEMENT_3D('',#93261,#27347,#27348);
#23388=AXIS2_PLACEMENT_3D('',#93286,#27350,#27351);
#23389=AXIS2_PLACEMENT_3D('',#93311,#27353,#27354);
#23390=AXIS2_PLACEMENT_3D('',#93335,#27356,#27357);
#23391=AXIS2_PLACEMENT_3D('',#93359,#27359,#27360);
#23392=AXIS2_PLACEMENT_3D('',#93384,#27362,#27363);
#23393=AXIS2_PLACEMENT_3D('',#93409,#27365,#27366);
#23394=AXIS2_PLACEMENT_3D('',#93433,#27368,#27369);
#23395=AXIS2_PLACEMENT_3D('',#93458,#27371,#27372);
#23396=AXIS2_PLACEMENT_3D('',#93483,#27374,#27375);
#23397=AXIS2_PLACEMENT_3D('',#93507,#27377,#27378);
#23398=AXIS2_PLACEMENT_3D('',#93531,#27380,#27381);
#23399=AXIS2_PLACEMENT_3D('',#93556,#27383,#27384);
#23400=AXIS2_PLACEMENT_3D('',#93581,#27386,#27387);
#23401=AXIS2_PLACEMENT_3D('',#93605,#27389,#27390);
#23402=AXIS2_PLACEMENT_3D('',#93630,#27392,#27393);
#23403=AXIS2_PLACEMENT_3D('',#93655,#27395,#27396);
#23404=AXIS2_PLACEMENT_3D('',#93679,#27398,#27399);
#23405=AXIS2_PLACEMENT_3D('',#93703,#27401,#27402);
#23406=AXIS2_PLACEMENT_3D('',#93728,#27404,#27405);
#23407=AXIS2_PLACEMENT_3D('',#93753,#27407,#27408);
#23408=AXIS2_PLACEMENT_3D('',#93777,#27410,#27411);
#23409=AXIS2_PLACEMENT_3D('',#93802,#27413,#27414);
#23410=AXIS2_PLACEMENT_3D('',#93827,#27416,#27417);
#23411=AXIS2_PLACEMENT_3D('',#93851,#27419,#27420);
#23412=AXIS2_PLACEMENT_3D('',#93875,#27422,#27423);
#23413=AXIS2_PLACEMENT_3D('',#93900,#27425,#27426);
#23414=AXIS2_PLACEMENT_3D('',#93925,#27428,#27429);
#23415=AXIS2_PLACEMENT_3D('',#93949,#27431,#27432);
#23416=AXIS2_PLACEMENT_3D('',#93974,#27434,#27435);
#23417=AXIS2_PLACEMENT_3D('',#93999,#27437,#27438);
#23418=AXIS2_PLACEMENT_3D('',#94023,#27440,#27441);
#23419=AXIS2_PLACEMENT_3D('',#94047,#27443,#27444);
#23420=AXIS2_PLACEMENT_3D('',#94072,#27446,#27447);
#23421=AXIS2_PLACEMENT_3D('',#94097,#27449,#27450);
#23422=AXIS2_PLACEMENT_3D('',#94121,#27452,#27453);
#23423=AXIS2_PLACEMENT_3D('',#94146,#27455,#27456);
#23424=AXIS2_PLACEMENT_3D('',#94171,#27458,#27459);
#23425=AXIS2_PLACEMENT_3D('',#94195,#27461,#27462);
#23426=AXIS2_PLACEMENT_3D('',#94219,#27464,#27465);
#23427=AXIS2_PLACEMENT_3D('',#94507,#27466,#27467);
#23428=AXIS2_PLACEMENT_3D('',#94541,#27469,#27470);
#23429=AXIS2_PLACEMENT_3D('',#95924,#27471,#27472);
#23430=AXIS2_PLACEMENT_3D('',#95935,#27473,#27474);
#23431=AXIS2_PLACEMENT_3D('',#97314,#27475,#27476);
#23432=AXIS2_PLACEMENT_3D('',#97315,#27477,#27478);
#23433=AXIS2_PLACEMENT_3D('',#97324,#27483,#27484);
#23434=AXIS2_PLACEMENT_3D('',#97330,#27488,#27489);
#23435=AXIS2_PLACEMENT_3D('',#97336,#27493,#27494);
#23436=AXIS2_PLACEMENT_3D('',#97342,#27498,#27499);
#23437=AXIS2_PLACEMENT_3D('',#97348,#27503,#27504);
#23438=AXIS2_PLACEMENT_3D('',#97351,#27507,#27508);
#23439=AXIS2_PLACEMENT_3D('',#97352,#27509,#27510);
#23440=AXIS2_PLACEMENT_3D('',#97354,#27511,#27512);
#23441=AXIS2_PLACEMENT_3D('',#97355,#27513,#27514);
#23442=AXIS2_PLACEMENT_3D('',#97358,#27516,#27517);
#23443=AXIS2_PLACEMENT_3D('',#97359,#27518,#27519);
#23444=AXIS2_PLACEMENT_3D('',#97360,#27520,#27521);
#27164=DIRECTION('axis',(0.,0.,1.));
#27165=DIRECTION('refdir',(1.,0.,0.));
#27166=DIRECTION('center_axis',(0.,0.,1.));
#27167=DIRECTION('ref_axis',(1.,0.,0.));
#27168=DIRECTION('',(0.,0.,-1.));
#27169=DIRECTION('center_axis',(0.,0.,-1.));
#27170=DIRECTION('ref_axis',(1.,0.,0.));
#27171=DIRECTION('center_axis',(0.,0.,1.));
#27172=DIRECTION('ref_axis',(1.,0.,0.));
#27173=DIRECTION('',(0.,0.,-1.));
#27174=DIRECTION('center_axis',(0.,0.,1.));
#27175=DIRECTION('ref_axis',(1.,0.,0.));
#27176=DIRECTION('',(0.,0.,-1.));
#27177=DIRECTION('center_axis',(0.,0.,1.));
#27178=DIRECTION('ref_axis',(1.,0.,0.));
#27179=DIRECTION('',(0.,0.,-1.));
#27180=DIRECTION('center_axis',(0.,0.,1.));
#27181=DIRECTION('ref_axis',(1.,0.,0.));
#27182=DIRECTION('',(0.,0.,-1.));
#27183=DIRECTION('center_axis',(0.,0.,1.));
#27184=DIRECTION('ref_axis',(1.,0.,0.));
#27185=DIRECTION('',(0.,0.,-1.));
#27186=DIRECTION('center_axis',(0.,0.,1.));
#27187=DIRECTION('ref_axis',(1.,0.,0.));
#27188=DIRECTION('',(0.,0.,-1.));
#27189=DIRECTION('center_axis',(0.,0.,1.));
#27190=DIRECTION('ref_axis',(1.,0.,0.));
#27191=DIRECTION('',(0.,0.,-1.));
#27192=DIRECTION('center_axis',(0.,0.,1.));
#27193=DIRECTION('ref_axis',(1.,0.,0.));
#27194=DIRECTION('',(0.,0.,-1.));
#27195=DIRECTION('center_axis',(0.,0.,1.));
#27196=DIRECTION('ref_axis',(1.,0.,0.));
#27197=DIRECTION('',(0.,0.,-1.));
#27198=DIRECTION('center_axis',(0.,0.,1.));
#27199=DIRECTION('ref_axis',(1.,0.,0.));
#27200=DIRECTION('',(0.,0.,-1.));
#27201=DIRECTION('center_axis',(0.,0.,1.));
#27202=DIRECTION('ref_axis',(1.,0.,0.));
#27203=DIRECTION('',(0.,0.,-1.));
#27204=DIRECTION('center_axis',(0.,0.,1.));
#27205=DIRECTION('ref_axis',(1.,0.,0.));
#27206=DIRECTION('',(0.,0.,-1.));
#27207=DIRECTION('center_axis',(0.,0.,1.));
#27208=DIRECTION('ref_axis',(1.,0.,0.));
#27209=DIRECTION('',(0.,0.,-1.));
#27210=DIRECTION('center_axis',(0.,0.,1.));
#27211=DIRECTION('ref_axis',(1.,0.,0.));
#27212=DIRECTION('',(0.,0.,-1.));
#27213=DIRECTION('center_axis',(0.,0.,1.));
#27214=DIRECTION('ref_axis',(1.,0.,0.));
#27215=DIRECTION('',(0.,0.,-1.));
#27216=DIRECTION('center_axis',(0.,0.,1.));
#27217=DIRECTION('ref_axis',(1.,0.,0.));
#27218=DIRECTION('',(0.,0.,-1.));
#27219=DIRECTION('center_axis',(0.,0.,1.));
#27220=DIRECTION('ref_axis',(1.,0.,0.));
#27221=DIRECTION('',(0.,0.,-1.));
#27222=DIRECTION('center_axis',(0.,0.,1.));
#27223=DIRECTION('ref_axis',(1.,0.,0.));
#27224=DIRECTION('',(0.,0.,-1.));
#27225=DIRECTION('center_axis',(0.,0.,1.));
#27226=DIRECTION('ref_axis',(1.,0.,0.));
#27227=DIRECTION('',(0.,0.,-1.));
#27228=DIRECTION('center_axis',(0.,0.,1.));
#27229=DIRECTION('ref_axis',(1.,0.,0.));
#27230=DIRECTION('',(0.,0.,-1.));
#27231=DIRECTION('center_axis',(0.,0.,1.));
#27232=DIRECTION('ref_axis',(1.,0.,0.));
#27233=DIRECTION('',(0.,0.,-1.));
#27234=DIRECTION('center_axis',(0.,0.,1.));
#27235=DIRECTION('ref_axis',(1.,0.,0.));
#27236=DIRECTION('',(0.,0.,-1.));
#27237=DIRECTION('center_axis',(0.,0.,1.));
#27238=DIRECTION('ref_axis',(1.,0.,0.));
#27239=DIRECTION('',(0.,0.,-1.));
#27240=DIRECTION('center_axis',(0.,0.,1.));
#27241=DIRECTION('ref_axis',(1.,0.,0.));
#27242=DIRECTION('',(0.,0.,-1.));
#27243=DIRECTION('center_axis',(0.,0.,1.));
#27244=DIRECTION('ref_axis',(1.,0.,0.));
#27245=DIRECTION('',(0.,0.,-1.));
#27246=DIRECTION('center_axis',(0.,0.,1.));
#27247=DIRECTION('ref_axis',(1.,0.,0.));
#27248=DIRECTION('',(0.,0.,-1.));
#27249=DIRECTION('center_axis',(0.,0.,1.));
#27250=DIRECTION('ref_axis',(1.,0.,0.));
#27251=DIRECTION('',(0.,0.,-1.));
#27252=DIRECTION('center_axis',(0.,0.,1.));
#27253=DIRECTION('ref_axis',(1.,0.,0.));
#27254=DIRECTION('',(0.,0.,-1.));
#27255=DIRECTION('center_axis',(0.,0.,1.));
#27256=DIRECTION('ref_axis',(1.,0.,0.));
#27257=DIRECTION('',(0.,0.,-1.));
#27258=DIRECTION('center_axis',(0.,0.,1.));
#27259=DIRECTION('ref_axis',(1.,0.,0.));
#27260=DIRECTION('',(0.,0.,-1.));
#27261=DIRECTION('center_axis',(0.,0.,1.));
#27262=DIRECTION('ref_axis',(1.,0.,0.));
#27263=DIRECTION('',(0.,0.,-1.));
#27264=DIRECTION('center_axis',(0.,0.,1.));
#27265=DIRECTION('ref_axis',(1.,0.,0.));
#27266=DIRECTION('',(0.,0.,-1.));
#27267=DIRECTION('center_axis',(0.,0.,1.));
#27268=DIRECTION('ref_axis',(1.,0.,0.));
#27269=DIRECTION('',(0.,0.,-1.));
#27270=DIRECTION('center_axis',(0.,0.,1.));
#27271=DIRECTION('ref_axis',(1.,0.,0.));
#27272=DIRECTION('',(0.,0.,-1.));
#27273=DIRECTION('center_axis',(0.,0.,1.));
#27274=DIRECTION('ref_axis',(1.,0.,0.));
#27275=DIRECTION('',(0.,0.,-1.));
#27276=DIRECTION('center_axis',(0.,0.,1.));
#27277=DIRECTION('ref_axis',(1.,0.,0.));
#27278=DIRECTION('',(0.,0.,-1.));
#27279=DIRECTION('center_axis',(0.,0.,1.));
#27280=DIRECTION('ref_axis',(1.,0.,0.));
#27281=DIRECTION('',(0.,0.,-1.));
#27282=DIRECTION('center_axis',(0.,0.,1.));
#27283=DIRECTION('ref_axis',(1.,0.,0.));
#27284=DIRECTION('',(0.,0.,-1.));
#27285=DIRECTION('center_axis',(0.,0.,1.));
#27286=DIRECTION('ref_axis',(1.,0.,0.));
#27287=DIRECTION('',(0.,0.,-1.));
#27288=DIRECTION('center_axis',(0.,0.,1.));
#27289=DIRECTION('ref_axis',(1.,0.,0.));
#27290=DIRECTION('',(0.,0.,-1.));
#27291=DIRECTION('center_axis',(0.,0.,1.));
#27292=DIRECTION('ref_axis',(1.,0.,0.));
#27293=DIRECTION('',(0.,0.,-1.));
#27294=DIRECTION('center_axis',(0.,0.,1.));
#27295=DIRECTION('ref_axis',(1.,0.,0.));
#27296=DIRECTION('',(0.,0.,-1.));
#27297=DIRECTION('center_axis',(0.,0.,1.));
#27298=DIRECTION('ref_axis',(1.,0.,0.));
#27299=DIRECTION('',(0.,0.,-1.));
#27300=DIRECTION('center_axis',(0.,0.,1.));
#27301=DIRECTION('ref_axis',(1.,0.,0.));
#27302=DIRECTION('',(0.,0.,-1.));
#27303=DIRECTION('center_axis',(0.,0.,1.));
#27304=DIRECTION('ref_axis',(1.,0.,0.));
#27305=DIRECTION('',(0.,0.,-1.));
#27306=DIRECTION('center_axis',(0.,0.,1.));
#27307=DIRECTION('ref_axis',(1.,0.,0.));
#27308=DIRECTION('',(0.,0.,-1.));
#27309=DIRECTION('center_axis',(0.,0.,1.));
#27310=DIRECTION('ref_axis',(1.,0.,0.));
#27311=DIRECTION('',(0.,0.,-1.));
#27312=DIRECTION('center_axis',(0.,0.,1.));
#27313=DIRECTION('ref_axis',(1.,0.,0.));
#27314=DIRECTION('',(0.,0.,-1.));
#27315=DIRECTION('center_axis',(0.,0.,1.));
#27316=DIRECTION('ref_axis',(0.997333003469248,-0.0729854793161552,0.));
#27317=DIRECTION('',(0.,0.,1.));
#27318=DIRECTION('center_axis',(0.,0.,-1.));
#27319=DIRECTION('ref_axis',(1.,-7.35649788641118E-13,0.));
#27320=DIRECTION('center_axis',(0.,0.,1.));
#27321=DIRECTION('ref_axis',(1.,-7.35649788641118E-13,0.));
#27322=DIRECTION('',(0.,0.,1.));
#27323=DIRECTION('center_axis',(0.,0.,1.));
#27324=DIRECTION('ref_axis',(1.,-7.35649788641118E-13,0.));
#27325=DIRECTION('',(0.,0.,1.));
#27326=DIRECTION('center_axis',(0.,0.,1.));
#27327=DIRECTION('ref_axis',(1.,-7.35649788641118E-13,0.));
#27328=DIRECTION('',(0.,0.,1.));
#27329=DIRECTION('center_axis',(0.,0.,1.));
#27330=DIRECTION('ref_axis',(1.,-7.35649788641118E-13,0.));
#27331=DIRECTION('',(0.,0.,1.));
#27332=DIRECTION('center_axis',(0.,0.,1.));
#27333=DIRECTION('ref_axis',(1.,-7.35649788641118E-13,0.));
#27334=DIRECTION('',(0.,0.,1.));
#27335=DIRECTION('center_axis',(0.,0.,1.));
#27336=DIRECTION('ref_axis',(1.,-7.35649788641118E-13,0.));
#27337=DIRECTION('',(0.,0.,1.));
#27338=DIRECTION('center_axis',(0.,0.,1.));
#27339=DIRECTION('ref_axis',(1.,-7.35649788641118E-13,0.));
#27340=DIRECTION('',(0.,0.,1.));
#27341=DIRECTION('center_axis',(0.,0.,1.));
#27342=DIRECTION('ref_axis',(1.,-7.35649788641118E-13,0.));
#27343=DIRECTION('',(0.,0.,1.));
#27344=DIRECTION('center_axis',(0.,0.,1.));
#27345=DIRECTION('ref_axis',(1.,-7.35649788641118E-13,0.));
#27346=DIRECTION('',(0.,0.,1.));
#27347=DIRECTION('center_axis',(0.,0.,1.));
#27348=DIRECTION('ref_axis',(1.,-7.35649788641118E-13,0.));
#27349=DIRECTION('',(0.,0.,1.));
#27350=DIRECTION('center_axis',(0.,0.,1.));
#27351=DIRECTION('ref_axis',(1.,-7.35649788641118E-13,0.));
#27352=DIRECTION('',(0.,0.,1.));
#27353=DIRECTION('center_axis',(0.,0.,1.));
#27354=DIRECTION('ref_axis',(1.,-7.35649788641118E-13,0.));
#27355=DIRECTION('',(0.,0.,1.));
#27356=DIRECTION('center_axis',(0.,0.,1.));
#27357=DIRECTION('ref_axis',(1.,-7.35649788641118E-13,0.));
#27358=DIRECTION('',(0.,0.,1.));
#27359=DIRECTION('center_axis',(0.,0.,1.));
#27360=DIRECTION('ref_axis',(1.,-7.35649788641118E-13,0.));
#27361=DIRECTION('',(0.,0.,1.));
#27362=DIRECTION('center_axis',(0.,0.,1.));
#27363=DIRECTION('ref_axis',(1.,-7.35649788641118E-13,0.));
#27364=DIRECTION('',(0.,0.,1.));
#27365=DIRECTION('center_axis',(0.,0.,1.));
#27366=DIRECTION('ref_axis',(1.,-7.35649788641118E-13,0.));
#27367=DIRECTION('',(0.,0.,1.));
#27368=DIRECTION('center_axis',(0.,0.,1.));
#27369=DIRECTION('ref_axis',(1.,-7.35649788641118E-13,0.));
#27370=DIRECTION('',(0.,0.,1.));
#27371=DIRECTION('center_axis',(0.,0.,1.));
#27372=DIRECTION('ref_axis',(1.,-7.35649788641118E-13,0.));
#27373=DIRECTION('',(0.,0.,1.));
#27374=DIRECTION('center_axis',(0.,0.,1.));
#27375=DIRECTION('ref_axis',(1.,-7.35649788641118E-13,0.));
#27376=DIRECTION('',(0.,0.,1.));
#27377=DIRECTION('center_axis',(0.,0.,1.));
#27378=DIRECTION('ref_axis',(1.,-7.35649788641118E-13,0.));
#27379=DIRECTION('',(0.,0.,1.));
#27380=DIRECTION('center_axis',(0.,0.,1.));
#27381=DIRECTION('ref_axis',(1.,-7.35649788641118E-13,0.));
#27382=DIRECTION('',(0.,0.,1.));
#27383=DIRECTION('center_axis',(0.,0.,1.));
#27384=DIRECTION('ref_axis',(1.,-7.35649788641118E-13,0.));
#27385=DIRECTION('',(0.,0.,1.));
#27386=DIRECTION('center_axis',(0.,0.,1.));
#27387=DIRECTION('ref_axis',(1.,-7.35649788641118E-13,0.));
#27388=DIRECTION('',(0.,0.,1.));
#27389=DIRECTION('center_axis',(0.,0.,1.));
#27390=DIRECTION('ref_axis',(1.,-7.35649788641118E-13,0.));
#27391=DIRECTION('',(0.,0.,1.));
#27392=DIRECTION('center_axis',(0.,0.,1.));
#27393=DIRECTION('ref_axis',(1.,-7.35649788641118E-13,0.));
#27394=DIRECTION('',(0.,0.,1.));
#27395=DIRECTION('center_axis',(0.,0.,1.));
#27396=DIRECTION('ref_axis',(1.,-7.35649788641118E-13,0.));
#27397=DIRECTION('',(0.,0.,1.));
#27398=DIRECTION('center_axis',(0.,0.,1.));
#27399=DIRECTION('ref_axis',(1.,-7.35649788641118E-13,0.));
#27400=DIRECTION('',(0.,0.,1.));
#27401=DIRECTION('center_axis',(0.,0.,1.));
#27402=DIRECTION('ref_axis',(1.,-7.35649788641118E-13,0.));
#27403=DIRECTION('',(0.,0.,1.));
#27404=DIRECTION('center_axis',(0.,0.,1.));
#27405=DIRECTION('ref_axis',(1.,-7.35649788641118E-13,0.));
#27406=DIRECTION('',(0.,0.,1.));
#27407=DIRECTION('center_axis',(0.,0.,1.));
#27408=DIRECTION('ref_axis',(1.,-7.35649788641118E-13,0.));
#27409=DIRECTION('',(0.,0.,1.));
#27410=DIRECTION('center_axis',(0.,0.,1.));
#27411=DIRECTION('ref_axis',(1.,-7.35649788641118E-13,0.));
#27412=DIRECTION('',(0.,0.,1.));
#27413=DIRECTION('center_axis',(0.,0.,1.));
#27414=DIRECTION('ref_axis',(1.,-7.35649788641118E-13,0.));
#27415=DIRECTION('',(0.,0.,1.));
#27416=DIRECTION('center_axis',(0.,0.,1.));
#27417=DIRECTION('ref_axis',(1.,-7.35649788641118E-13,0.));
#27418=DIRECTION('',(0.,0.,1.));
#27419=DIRECTION('center_axis',(0.,0.,1.));
#27420=DIRECTION('ref_axis',(1.,-7.35649788641118E-13,0.));
#27421=DIRECTION('',(0.,0.,1.));
#27422=DIRECTION('center_axis',(0.,0.,1.));
#27423=DIRECTION('ref_axis',(1.,-7.35649788641118E-13,0.));
#27424=DIRECTION('',(0.,0.,1.));
#27425=DIRECTION('center_axis',(0.,0.,1.));
#27426=DIRECTION('ref_axis',(1.,-7.35649788641118E-13,0.));
#27427=DIRECTION('',(0.,0.,1.));
#27428=DIRECTION('center_axis',(0.,0.,1.));
#27429=DIRECTION('ref_axis',(1.,-7.35649788641118E-13,0.));
#27430=DIRECTION('',(0.,0.,1.));
#27431=DIRECTION('center_axis',(0.,0.,1.));
#27432=DIRECTION('ref_axis',(1.,-7.35649788641118E-13,0.));
#27433=DIRECTION('',(0.,0.,1.));
#27434=DIRECTION('center_axis',(0.,0.,1.));
#27435=DIRECTION('ref_axis',(1.,-7.35649788641118E-13,0.));
#27436=DIRECTION('',(0.,0.,1.));
#27437=DIRECTION('center_axis',(0.,0.,1.));
#27438=DIRECTION('ref_axis',(1.,-7.35649788641118E-13,0.));
#27439=DIRECTION('',(0.,0.,1.));
#27440=DIRECTION('center_axis',(0.,0.,1.));
#27441=DIRECTION('ref_axis',(1.,-7.35649788641118E-13,0.));
#27442=DIRECTION('',(0.,0.,1.));
#27443=DIRECTION('center_axis',(0.,0.,1.));
#27444=DIRECTION('ref_axis',(1.,-7.35649788641118E-13,0.));
#27445=DIRECTION('',(0.,0.,1.));
#27446=DIRECTION('center_axis',(0.,0.,1.));
#27447=DIRECTION('ref_axis',(1.,-7.35649788641118E-13,0.));
#27448=DIRECTION('',(0.,0.,1.));
#27449=DIRECTION('center_axis',(0.,0.,1.));
#27450=DIRECTION('ref_axis',(1.,-7.35649788641118E-13,0.));
#27451=DIRECTION('',(0.,0.,1.));
#27452=DIRECTION('center_axis',(0.,0.,1.));
#27453=DIRECTION('ref_axis',(1.,-7.35649788641118E-13,0.));
#27454=DIRECTION('',(0.,0.,1.));
#27455=DIRECTION('center_axis',(0.,0.,1.));
#27456=DIRECTION('ref_axis',(1.,-7.35649788641118E-13,0.));
#27457=DIRECTION('',(0.,0.,1.));
#27458=DIRECTION('center_axis',(0.,0.,1.));
#27459=DIRECTION('ref_axis',(1.,-7.35649788641118E-13,0.));
#27460=DIRECTION('',(0.,0.,1.));
#27461=DIRECTION('center_axis',(0.,0.,1.));
#27462=DIRECTION('ref_axis',(1.,-7.35649788641118E-13,0.));
#27463=DIRECTION('',(0.,0.,1.));
#27464=DIRECTION('center_axis',(0.,0.,-1.));
#27465=DIRECTION('ref_axis',(1.,0.,0.));
#27466=DIRECTION('center_axis',(0.,0.,-1.));
#27467=DIRECTION('ref_axis',(1.,0.,0.));
#27468=DIRECTION('',(0.707106781186549,8.65956056235495E-17,0.707106781186546));
#27469=DIRECTION('center_axis',(0.,0.,1.));
#27470=DIRECTION('ref_axis',(1.,0.,0.));
#27471=DIRECTION('center_axis',(0.,0.,1.));
#27472=DIRECTION('ref_axis',(1.,-7.35649788641118E-13,0.));
#27473=DIRECTION('center_axis',(0.,0.,-1.));
#27474=DIRECTION('ref_axis',(1.,-7.35649788641118E-13,0.));
#27475=DIRECTION('center_axis',(0.,0.,1.));
#27476=DIRECTION('ref_axis',(1.,0.,0.));
#27477=DIRECTION('center_axis',(-1.92296268638356E-16,-1.,0.));
#27478=DIRECTION('ref_axis',(1.,-1.92296268638356E-16,0.));
#27479=DIRECTION('',(1.,-1.92296268638356E-16,0.));
#27480=DIRECTION('',(0.,0.,1.));
#27481=DIRECTION('',(1.,-1.92296268638356E-16,0.));
#27482=DIRECTION('',(0.,0.,1.));
#27483=DIRECTION('center_axis',(-0.866025403784439,-0.5,0.));
#27484=DIRECTION('ref_axis',(0.5,-0.866025403784439,0.));
#27485=DIRECTION('',(0.5,-0.866025403784439,0.));
#27486=DIRECTION('',(0.,0.,1.));
#27487=DIRECTION('',(0.5,-0.866025403784439,0.));
#27488=DIRECTION('center_axis',(-0.866025403784439,0.5,0.));
#27489=DIRECTION('ref_axis',(-0.5,-0.866025403784438,0.));
#27490=DIRECTION('',(-0.5,-0.866025403784438,0.));
#27491=DIRECTION('',(0.,0.,1.));
#27492=DIRECTION('',(-0.5,-0.866025403784439,0.));
#27493=DIRECTION('center_axis',(1.92296268638356E-16,1.,0.));
#27494=DIRECTION('ref_axis',(-1.,1.92296268638356E-16,0.));
#27495=DIRECTION('',(-1.,1.92296268638356E-16,0.));
#27496=DIRECTION('',(0.,0.,1.));
#27497=DIRECTION('',(-1.,1.92296268638356E-16,0.));
#27498=DIRECTION('center_axis',(0.866025403784439,0.5,0.));
#27499=DIRECTION('ref_axis',(-0.5,0.866025403784439,0.));
#27500=DIRECTION('',(-0.5,0.866025403784439,0.));
#27501=DIRECTION('',(0.,0.,1.));
#27502=DIRECTION('',(-0.5,0.866025403784439,0.));
#27503=DIRECTION('center_axis',(0.866025403784439,-0.5,0.));
#27504=DIRECTION('ref_axis',(0.5,0.866025403784439,0.));
#27505=DIRECTION('',(0.5,0.866025403784439,0.));
#27506=DIRECTION('',(0.5,0.866025403784439,0.));
#27507=DIRECTION('center_axis',(0.,0.,1.));
#27508=DIRECTION('ref_axis',(1.,0.,0.));
#27509=DIRECTION('center_axis',(0.,0.,1.));
#27510=DIRECTION('ref_axis',(1.,0.,0.));
#27511=DIRECTION('center_axis',(0.,0.,1.));
#27512=DIRECTION('ref_axis',(1.,0.,0.));
#27513=DIRECTION('center_axis',(0.,0.,1.));
#27514=DIRECTION('ref_axis',(1.,0.,0.));
#27515=DIRECTION('',(0.,0.,-1.));
#27516=DIRECTION('center_axis',(0.,0.,1.));
#27517=DIRECTION('ref_axis',(1.,0.,0.));
#27518=DIRECTION('center_axis',(0.,0.,1.));
#27519=DIRECTION('ref_axis',(1.,0.,0.));
#27520=DIRECTION('center_axis',(0.,0.,1.));
#27521=DIRECTION('ref_axis',(1.,0.,0.));
#90611=CARTESIAN_POINT('',(0.,0.,0.));
#90612=CARTESIAN_POINT('Origin',(0.,0.,0.));
#90613=CARTESIAN_POINT('',(-2.94572833338121,0.00181828527978219,0.322176117089595));
#90614=CARTESIAN_POINT('',(-2.94480724771071,0.00314787458853884,0.177823882910503));
#90615=CARTESIAN_POINT('',(-2.942,-3.60291088309151E-16,0.));
#90616=CARTESIAN_POINT('',(1.28892185405323,2.64462557919718,0.));
#90617=CARTESIAN_POINT('Ctrl Pts',(-2.94572833338121,0.00181828527978219,
0.322176117089595));
#90618=CARTESIAN_POINT('Ctrl Pts',(-2.94634360469406,0.0948282274037363,
0.317125952852808));
#90619=CARTESIAN_POINT('Ctrl Pts',(-2.9423230955825,0.187780597515525,0.31207578861602));
#90620=CARTESIAN_POINT('Ctrl Pts',(-2.93349332836829,0.280269293446551,
0.307025624379232));
#90621=CARTESIAN_POINT('Ctrl Pts',(-2.84078967180988,1.2513073848389,0.254003989763848));
#90622=CARTESIAN_POINT('Ctrl Pts',(-2.21796709303351,2.17123521104683,0.200982355148463));
#90623=CARTESIAN_POINT('Ctrl Pts',(-1.35083655151447,2.61872799079034,0.147960720533078));
#90624=CARTESIAN_POINT('Ctrl Pts',(-0.544239642849529,3.03498168675485,
0.0986404803553854));
#90625=CARTESIAN_POINT('Ctrl Pts',(0.473745963287759,3.04245857499168,0.0493202401776924));
#90626=CARTESIAN_POINT('Ctrl Pts',(1.29201570592007,2.64858957748139,-3.98986399474666E-16));
#90627=CARTESIAN_POINT('',(-1.28892185405285,2.64462557919736,0.));
#90628=CARTESIAN_POINT('Origin',(0.,0.,0.));
#90629=CARTESIAN_POINT('Ctrl Pts',(-1.28892185405285,2.64462557919736,-2.24820162486594E-14));
#90630=CARTESIAN_POINT('Ctrl Pts',(-2.17016087157859,2.21513255860965,0.0530334224957372));
#90631=CARTESIAN_POINT('Ctrl Pts',(-2.81210852573283,1.31417567340568,0.106066844991497));
#90632=CARTESIAN_POINT('Ctrl Pts',(-2.92616511686446,0.346700093493863,
0.159100267487257));
#90633=CARTESIAN_POINT('Ctrl Pts',(-2.93958779542159,0.232843335263716,
0.165341472628339));
#90634=CARTESIAN_POINT('Ctrl Pts',(-2.9456993876071,0.118065318924837,0.171582677769421));
#90635=CARTESIAN_POINT('Ctrl Pts',(-2.94480724771071,0.00314787458853884,
0.177823882910503));
#90636=CARTESIAN_POINT('Origin',(0.,0.,0.));
#90637=CARTESIAN_POINT('',(-2.93822341007844,0.00177250923968975,1.3221761170896));
#90638=CARTESIAN_POINT('',(-2.93786545338865,0.00151834006811738,1.17782388291051));
#90639=CARTESIAN_POINT('',(-2.942,-3.60291088309151E-16,0.));
#90640=CARTESIAN_POINT('Ctrl Pts',(-2.93822341007844,0.00177250923968975,
1.3221761170896));
#90641=CARTESIAN_POINT('Ctrl Pts',(-2.94027489500473,0.377271029867399,
1.30192242721178));
#90642=CARTESIAN_POINT('Ctrl Pts',(-2.87355216442792,0.752067251550473,
1.28166873733397));
#90643=CARTESIAN_POINT('Ctrl Pts',(-2.73470753731878,1.09790711585681,1.26141504745616));
#90644=CARTESIAN_POINT('Ctrl Pts',(-2.37122961644105,2.00327275694782,1.20839341284077));
#90645=CARTESIAN_POINT('Ctrl Pts',(-1.51348078456157,2.71019263013704,1.15537177822539));
#90646=CARTESIAN_POINT('Ctrl Pts',(-0.555353735968972,2.89405691690588,
1.10235014361));
#90647=CARTESIAN_POINT('Ctrl Pts',(0.402773312623631,3.07792120367472,1.04932850899462));
#90648=CARTESIAN_POINT('Ctrl Pts',(1.46127857792935,2.73872990402317,0.996306874379233));
#90649=CARTESIAN_POINT('Ctrl Pts',(2.13406540677062,2.03220287366626,0.943285239763848));
#90650=CARTESIAN_POINT('Ctrl Pts',(2.80685223561189,1.32567584330935,0.890263605148464));
#90651=CARTESIAN_POINT('Ctrl Pts',(3.09392062798872,0.251813082247085,0.837241970533078));
#90652=CARTESIAN_POINT('Ctrl Pts',(2.86345785963421,-0.696160052250375,
0.784220335917694));
#90653=CARTESIAN_POINT('Ctrl Pts',(2.63299509127969,-1.64413318674784,0.731198701302309));
#90654=CARTESIAN_POINT('Ctrl Pts',(1.88500116219385,-2.46621669468049,0.678177066686924));
#90655=CARTESIAN_POINT('Ctrl Pts',(0.962941916531661,-2.78505266672784,
0.62515543207154));
#90656=CARTESIAN_POINT('Ctrl Pts',(0.0408826708694723,-3.1038886387752,
0.572133797456155));
#90657=CARTESIAN_POINT('Ctrl Pts',(-1.05524189136906,-2.91947707493725,
0.51911216284077));
#90658=CARTESIAN_POINT('Ctrl Pts',(-1.8220118053181,-2.3161971147299,0.466090528225386));
#90659=CARTESIAN_POINT('Ctrl Pts',(-2.51574900299274,-1.77037790430724,
0.418119057846789));
#90660=CARTESIAN_POINT('Ctrl Pts',(-2.93988387601795,-0.881682423669888,
0.370147587468192));
#90661=CARTESIAN_POINT('Ctrl Pts',(-2.94572833338121,0.00181828527978219,
0.322176117089595));
#90662=CARTESIAN_POINT('Ctrl Pts',(-2.94480724771071,0.00314787458853884,
0.177823882910503));
#90663=CARTESIAN_POINT('Ctrl Pts',(-2.93811860296998,-0.85842323414381,
0.22461610026518));
#90664=CARTESIAN_POINT('Ctrl Pts',(-2.53775312306778,-1.72783153197978,
0.271408317619858));
#90665=CARTESIAN_POINT('Ctrl Pts',(-1.87323616063333,-2.27559789904567,
0.318200534974535));
#90666=CARTESIAN_POINT('Ctrl Pts',(-1.12008508516153,-2.89642603705373,
0.371233957470294));
#90667=CARTESIAN_POINT('Ctrl Pts',(-0.0276174061089035,-3.10408803845018,
0.424267379966054));
#90668=CARTESIAN_POINT('Ctrl Pts',(0.901529172781748,-2.8053109028385,0.477300802461814));
#90669=CARTESIAN_POINT('Ctrl Pts',(1.8306757516724,-2.50653376722683,0.530334224957574));
#90670=CARTESIAN_POINT('Ctrl Pts',(2.59650123040107,-1.70131749460704,0.583367647453334));
#90671=CARTESIAN_POINT('Ctrl Pts',(2.8475652442623,-0.758507527336255,0.636401069949093));
#90672=CARTESIAN_POINT('Ctrl Pts',(3.09862925812353,0.184302439934527,0.689434492444853));
#90673=CARTESIAN_POINT('Ctrl Pts',(2.83493180711731,1.2647061018563,0.742467914940612));
#90674=CARTESIAN_POINT('Ctrl Pts',(2.17741585189684,1.98579598787704,0.795501337436372));
#90675=CARTESIAN_POINT('Ctrl Pts',(1.51989989667636,2.70688587389778,0.848534759932131));
#90676=CARTESIAN_POINT('Ctrl Pts',(0.468565437241616,3.06866198401749,0.901568182427891));
#90677=CARTESIAN_POINT('Ctrl Pts',(-0.493489605026679,2.90521466357553,
0.954601604923651));
#90678=CARTESIAN_POINT('Ctrl Pts',(-1.45554464729497,2.74176734313358,1.00763502741941));
#90679=CARTESIAN_POINT('Ctrl Pts',(-2.32832027239682,2.05309659212996,1.06066844991517));
#90680=CARTESIAN_POINT('Ctrl Pts',(-2.71091124967939,1.15542995337685,1.11370187241093));
#90681=CARTESIAN_POINT('Ctrl Pts',(-2.86510648171644,0.793644328850147,
1.13507587591079));
#90682=CARTESIAN_POINT('Ctrl Pts',(-2.93967988512601,0.397911017809249,
1.15644987941065));
#90683=CARTESIAN_POINT('Ctrl Pts',(-2.93786545338865,0.00151834006811738,
1.17782388291051));
#90684=CARTESIAN_POINT('Origin',(0.,0.,0.));
#90685=CARTESIAN_POINT('',(-2.93928862718909,-0.00231022146983534,2.3221761170896));
#90686=CARTESIAN_POINT('',(-2.93977341269383,-0.00246746851037129,2.1778238829105));
#90687=CARTESIAN_POINT('',(-2.942,-3.60291088309151E-16,0.));
#90688=CARTESIAN_POINT('Ctrl Pts',(-2.93928862718909,-0.00231022146983534,
2.3221761170896));
#90689=CARTESIAN_POINT('Ctrl Pts',(-2.93448895843968,0.654458709996738,
2.28671890157076));
#90690=CARTESIAN_POINT('Ctrl Pts',(-2.71712890865226,1.31410884872896,2.25126168605192));
#90691=CARTESIAN_POINT('Ctrl Pts',(-2.31282889140208,1.82615547188083,2.21580447053308));
#90692=CARTESIAN_POINT('Ctrl Pts',(-1.70825102266775,2.59185431657369,2.16278283591769));
#90693=CARTESIAN_POINT('Ctrl Pts',(-0.685651158909644,3.02749257073117,
2.10976120130231));
#90694=CARTESIAN_POINT('Ctrl Pts',(0.28537070618245,2.93301616105637,2.05673956668693));
#90695=CARTESIAN_POINT('Ctrl Pts',(1.25639257127454,2.83853975138157,2.00371793207154));
#90696=CARTESIAN_POINT('Ctrl Pts',(2.17583643770061,2.21394867787448,1.95069629745616));
#90697=CARTESIAN_POINT('Ctrl Pts',(2.621473533489,1.34606781880211,1.89767466284077));
#90698=CARTESIAN_POINT('Ctrl Pts',(3.0671106292774,0.478186959729728,1.84465302822539));
#90699=CARTESIAN_POINT('Ctrl Pts',(3.03894095442811,-0.632983684907954,
1.79163139361));
#90700=CARTESIAN_POINT('Ctrl Pts',(2.54990095382167,-1.47716865811546,1.73860975899462));
#90701=CARTESIAN_POINT('Ctrl Pts',(2.06086095321523,-2.32135363132295,1.68558812437923));
#90702=CARTESIAN_POINT('Ctrl Pts',(1.11095062685165,-2.89855293310027,1.63256648976385));
#90703=CARTESIAN_POINT('Ctrl Pts',(0.136388833930434,-2.9437074353793,1.57954485514846));
#90704=CARTESIAN_POINT('Ctrl Pts',(-0.838172958990785,-2.98886193765833,
1.52652322053308));
#90705=CARTESIAN_POINT('Ctrl Pts',(-1.83738621846964,-2.50197164043906,
1.47350158591769));
#90706=CARTESIAN_POINT('Ctrl Pts',(-2.40238934327107,-1.70662078733303,
1.42047995130231));
#90707=CARTESIAN_POINT('Ctrl Pts',(-2.75156739680238,-1.21508534164919,
1.38771200656474));
#90708=CARTESIAN_POINT('Ctrl Pts',(-2.93490436327265,-0.605737275258753,
1.35494406182717));
#90709=CARTESIAN_POINT('Ctrl Pts',(-2.93822341007844,0.00177250923968975,
1.3221761170896));
#90710=CARTESIAN_POINT('Ctrl Pts',(-2.93786545338865,0.00151834006811738,
1.17782388291051));
#90711=CARTESIAN_POINT('Ctrl Pts',(-2.9351778963003,-0.585623038082895,
1.20948330190641));
#90712=CARTESIAN_POINT('Ctrl Pts',(-2.76489639151172,-1.17421105846512,
1.24114272090231));
#90713=CARTESIAN_POINT('Ctrl Pts',(-2.43753063936175,-1.65606669470434,
1.27280213989821));
#90714=CARTESIAN_POINT('Ctrl Pts',(-1.88915272229826,-2.46323417752985,
1.32583556239397));
#90715=CARTESIAN_POINT('Ctrl Pts',(-0.899990558707984,-2.97090661667828,
1.37886898488973));
#90716=CARTESIAN_POINT('Ctrl Pts',(0.07551096328437,-2.94589715015884,1.43190240738549));
#90717=CARTESIAN_POINT('Ctrl Pts',(1.05101248527673,-2.92088768363939,1.48493582988125));
#90718=CARTESIAN_POINT('Ctrl Pts',(2.01285336567117,-2.36319631145207,1.53796925237701));
#90719=CARTESIAN_POINT('Ctrl Pts',(2.51916357038756,-1.52900912719568,1.59100267487277));
#90720=CARTESIAN_POINT('Ctrl Pts',(3.02547377510396,-0.694821942939303,
1.64403609736853));
#90721=CARTESIAN_POINT('Ctrl Pts',(3.0762533041423,0.415861053386139,1.69706951986429));
#90722=CARTESIAN_POINT('Ctrl Pts',(2.6481694163222,1.29277087678848,1.75010294236005));
#90723=CARTESIAN_POINT('Ctrl Pts',(2.22008552850209,2.16968070019081,1.80313636485581));
#90724=CARTESIAN_POINT('Ctrl Pts',(1.31313822382353,2.81281735067005,1.85616978735156));
#90725=CARTESIAN_POINT('Ctrl Pts',(0.343989133332744,2.92672437389905,1.90920320984732));
#90726=CARTESIAN_POINT('Ctrl Pts',(-0.625159957158049,3.04063139712806,
1.96223663234308));
#90727=CARTESIAN_POINT('Ctrl Pts',(-1.65651083346107,2.62530879310683,2.01527005483884));
#90728=CARTESIAN_POINT('Ctrl Pts',(-2.27625313257342,1.8715561682732,2.0683034773346));
#90729=CARTESIAN_POINT('Ctrl Pts',(-2.70286729874226,1.35269284717742,2.10481027919324));
#90730=CARTESIAN_POINT('Ctrl Pts',(-2.9344374252303,0.673461734771185,2.14131708105187));
#90731=CARTESIAN_POINT('Ctrl Pts',(-2.93977341269383,-0.00246746851037129,
2.1778238829105));
#90732=CARTESIAN_POINT('Origin',(0.,0.,0.));
#90733=CARTESIAN_POINT('',(-2.94660142545168,-0.00080359277598141,3.32217611708959));
#90734=CARTESIAN_POINT('',(-2.94677574562124,-0.00048046415745224,3.1778238829105));
#90735=CARTESIAN_POINT('',(-2.942,-3.60291088309151E-16,0.));
#90736=CARTESIAN_POINT('Ctrl Pts',(-2.94660142545168,-0.00080359277598141,
3.32217611708959));
#90737=CARTESIAN_POINT('Ctrl Pts',(-2.9432210210648,0.931587450945792,3.27151537592973));
#90738=CARTESIAN_POINT('Ctrl Pts',(-2.4632020008259,1.86697373967705,3.22085463476987));
#90739=CARTESIAN_POINT('Ctrl Pts',(-1.70229822738816,2.40545252134969,3.17019389361));
#90740=CARTESIAN_POINT('Ctrl Pts',(-0.905934792329565,2.96902550816978,
3.11717225899462));
#90741=CARTESIAN_POINT('Ctrl Pts',(0.198103007440144,3.09783561201883,3.06415062437924));
#90742=CARTESIAN_POINT('Ctrl Pts',(1.10281702258816,2.73273044381862,3.01112898976385));
#90743=CARTESIAN_POINT('Ctrl Pts',(2.00753103773617,2.36762527561841,2.95810735514846));
#90744=CARTESIAN_POINT('Ctrl Pts',(2.71292126826249,1.50860483536893,2.90508572053308));
#90745=CARTESIAN_POINT('Ctrl Pts',(2.89505718696188,0.550149958862014,2.85206408591769));
#90746=CARTESIAN_POINT('Ctrl Pts',(3.07719310566127,-0.40830491764491,2.79904245130231));
#90747=CARTESIAN_POINT('Ctrl Pts',(2.73607471253372,-1.46619423040927,2.74602081668693));
#90748=CARTESIAN_POINT('Ctrl Pts',(2.02835099365646,-2.13771218014694,2.69299918207154));
#90749=CARTESIAN_POINT('Ctrl Pts',(1.3206272747792,-2.8092301298846,2.63997754745616));
#90750=CARTESIAN_POINT('Ctrl Pts',(0.246298230152233,-3.09437671659557,
2.58695591284077));
#90751=CARTESIAN_POINT('Ctrl Pts',(-0.70128090767504,-2.86220649994471,
2.53393427822538));
#90752=CARTESIAN_POINT('Ctrl Pts',(-1.64886004550232,-2.63003628329385,
2.48091264361));
#90753=CARTESIAN_POINT('Ctrl Pts',(-2.4696892765299,-1.88054926328115,2.42789100899462));
#90754=CARTESIAN_POINT('Ctrl Pts',(-2.78682595518842,-0.957926035660687,
2.37486937437924));
#90755=CARTESIAN_POINT('Ctrl Pts',(-2.89188347699535,-0.65228964486123,
2.35730495528269));
#90756=CARTESIAN_POINT('Ctrl Pts',(-2.94166623615261,-0.327653444085288,
2.33974053618614));
#90757=CARTESIAN_POINT('Ctrl Pts',(-2.93928862718909,-0.00231022146983534,
2.3221761170896));
#90758=CARTESIAN_POINT('Ctrl Pts',(-2.93977341269383,-0.00246746851037129,
2.1778238829105));
#90759=CARTESIAN_POINT('Ctrl Pts',(-2.94218901296677,-0.308460460266985,
2.19435050354763));
#90760=CARTESIAN_POINT('Ctrl Pts',(-2.89824084993499,-0.613776768417091,
2.21087712418476));
#90761=CARTESIAN_POINT('Ctrl Pts',(-2.80503526316264,-0.903231941911796,
2.22740374482188));
#90762=CARTESIAN_POINT('Ctrl Pts',(-2.50594137271785,-1.83208478161718,
2.28043716731764));
#90763=CARTESIAN_POINT('Ctrl Pts',(-1.69961986990659,-2.59760781538194,
2.3334705898134));
#90764=CARTESIAN_POINT('Ctrl Pts',(-0.75650214363239,-2.84811401666259,
2.38650401230916));
#90765=CARTESIAN_POINT('Ctrl Pts',(0.186615582641814,-3.09862021794324,
2.43953743480492));
#90766=CARTESIAN_POINT('Ctrl Pts',(1.26652953237896,-2.83410958673978,2.49257085730068));
#90767=CARTESIAN_POINT('Ctrl Pts',(1.98711806191723,-2.17610013539117,2.54560427979644));
#90768=CARTESIAN_POINT('Ctrl Pts',(2.7077065914555,-1.51809068404256,2.5986377022922));
#90769=CARTESIAN_POINT('Ctrl Pts',(3.06896970079488,-0.466582412548801,
2.65167112478796));
#90770=CARTESIAN_POINT('Ctrl Pts',(2.90493990584006,0.495352443093267,2.70470454728372));
#90771=CARTESIAN_POINT('Ctrl Pts',(2.74091011088523,1.45728729873534,2.75773796977948));
#90772=CARTESIAN_POINT('Ctrl Pts',(2.0515874116362,2.32964873852571,2.81077139227524));
#90773=CARTESIAN_POINT('Ctrl Pts',(1.15365266405868,2.71166649769722,2.863804814771));
#90774=CARTESIAN_POINT('Ctrl Pts',(0.255717916481151,3.09368425686873,2.91683823726676));
#90775=CARTESIAN_POINT('Ctrl Pts',(-0.85082887942487,2.98535833542137,2.96987165976252));
#90776=CARTESIAN_POINT('Ctrl Pts',(-1.65763057826024,2.4364545324485,3.02290508225827));
#90777=CARTESIAN_POINT('Ctrl Pts',(-2.44322794727629,1.90197699716214,3.07454468247568));
#90778=CARTESIAN_POINT('Ctrl Pts',(-2.9446289500562,0.949775755309008,3.12618428269309));
#90779=CARTESIAN_POINT('Ctrl Pts',(-2.94677574562124,-0.00048046415745224,
3.1778238829105));
#90780=CARTESIAN_POINT('Origin',(0.,0.,0.));
#90781=CARTESIAN_POINT('',(-2.94172250344281,0.00271694754677573,4.3221761170896));
#90782=CARTESIAN_POINT('',(-2.94122604762498,0.00270348896235926,4.17782388291051));
#90783=CARTESIAN_POINT('',(-2.942,-3.60291088309151E-16,0.));
#90784=CARTESIAN_POINT('Ctrl Pts',(-2.94172250344281,0.00271694754677573,
4.3221761170896));
#90785=CARTESIAN_POINT('Ctrl Pts',(-2.9438999436428,0.240100699663681,4.30933348490409));
#90786=CARTESIAN_POINT('Ctrl Pts',(-2.91758898170167,0.477007792036415,
4.29649085271859));
#90787=CARTESIAN_POINT('Ctrl Pts',(-2.86094144805788,0.706424172715316,
4.28364822053308));
#90788=CARTESIAN_POINT('Ctrl Pts',(-2.62706845478522,1.65358448498141,4.2306265859177));
#90789=CARTESIAN_POINT('Ctrl Pts',(-1.87610725072441,2.47306528404282,4.17760495130231));
#90790=CARTESIAN_POINT('Ctrl Pts',(-0.952915541058148,2.78854317750225,
4.12458331668693));
#90791=CARTESIAN_POINT('Ctrl Pts',(-0.0297238313918914,3.10402107096167,
4.07156168207154));
#90792=CARTESIAN_POINT('Ctrl Pts',(1.06569838387982,2.91549605881912,4.01854004745616));
#90793=CARTESIAN_POINT('Ctrl Pts',(1.8303094172875,2.30954292397576,3.96551841284077));
#90794=CARTESIAN_POINT('Ctrl Pts',(2.5949204506952,1.7035897891324,3.91249677822539));
#90795=CARTESIAN_POINT('Ctrl Pts',(3.02872030223887,0.680208531588234,3.85947514361001));
#90796=CARTESIAN_POINT('Ctrl Pts',(2.93249865246612,-0.290641934962542,
3.80645350899462));
#90797=CARTESIAN_POINT('Ctrl Pts',(2.83627700269337,-1.26149240151332,3.75343187437924));
#90798=CARTESIAN_POINT('Ctrl Pts',(2.21003385160419,-2.1798120770707,3.70041023976385));
#90799=CARTESIAN_POINT('Ctrl Pts',(1.3413536641399,-2.6238886084906,3.64738860514846));
#90800=CARTESIAN_POINT('Ctrl Pts',(0.472673476675607,-3.06796513991049,
3.59436697053308));
#90801=CARTESIAN_POINT('Ctrl Pts',(-0.638443747163792,-3.03779852719289,
3.5413453359177));
#90802=CARTESIAN_POINT('Ctrl Pts',(-1.48174883110658,-2.54724193593031,
3.48832370130231));
#90803=CARTESIAN_POINT('Ctrl Pts',(-2.32505391504936,-2.05668534466774,
3.43530206668693));
#90804=CARTESIAN_POINT('Ctrl Pts',(-2.90054685909553,-1.10573877486018,
3.38228043207154));
#90805=CARTESIAN_POINT('Ctrl Pts',(-2.94394879594488,-0.131097555060847,
3.32925879745616));
#90806=CARTESIAN_POINT('Ctrl Pts',(-2.94588135327563,-0.0876997214407355,
3.32689790400064));
#90807=CARTESIAN_POINT('Ctrl Pts',(-2.94675895916341,-0.0442549095690453,
3.32453701054511));
#90808=CARTESIAN_POINT('Ctrl Pts',(-2.94660142545168,-0.00080359277598141,
3.32217611708959));
#90809=CARTESIAN_POINT('Ctrl Pts',(-2.94677574562124,-0.00048046415745224,
3.1778238829105));
#90810=CARTESIAN_POINT('Ctrl Pts',(-2.94683369052153,-0.0261291578587509,
3.17921770518885));
#90811=CARTESIAN_POINT('Ctrl Pts',(-2.9465279123969,-0.0517764345476016,
3.1806115274672));
#90812=CARTESIAN_POINT('Ctrl Pts',(-2.94585418233316,-0.0774140418253259,
3.18200534974556));
#90813=CARTESIAN_POINT('Ctrl Pts',(-2.92021948580598,-1.0528971286279,3.23503877224132));
#90814=CARTESIAN_POINT('Ctrl Pts',(-2.36189349098687,-2.01438161773467,
3.28807219473707));
#90815=CARTESIAN_POINT('Ctrl Pts',(-1.52737599577425,-2.52015323654691,
3.34110561723283));
#90816=CARTESIAN_POINT('Ctrl Pts',(-0.69285850056163,-3.02592485535916,
3.39413903972859));
#90817=CARTESIAN_POINT('Ctrl Pts',(0.417850495044496,-3.0759836038769,3.44717246222435));
#90818=CARTESIAN_POINT('Ctrl Pts',(1.29448167466864,-2.64733205050477,3.50020588472011));
#90819=CARTESIAN_POINT('Ctrl Pts',(2.17111285429278,-2.21868049713266,3.55323930721587));
#90820=CARTESIAN_POINT('Ctrl Pts',(2.81366621793492,-1.31131864187067,3.60627272971163));
#90821=CARTESIAN_POINT('Ctrl Pts',(2.92694719068011,-0.342096374378361,
3.65930615220739));
#90822=CARTESIAN_POINT('Ctrl Pts',(3.04022816342529,0.627125893113943,3.71233957470315));
#90823=CARTESIAN_POINT('Ctrl Pts',(2.62423674527353,1.65820857283657,3.76537299719891));
#90824=CARTESIAN_POINT('Ctrl Pts',(1.87008299284461,2.27746336585166,3.81840641969467));
#90825=CARTESIAN_POINT('Ctrl Pts',(1.11592924041568,2.89671815886675,3.87143984219043));
#90826=CARTESIAN_POINT('Ctrl Pts',(0.0236131537096002,3.1041450651743,3.92447326468619));
#90827=CARTESIAN_POINT('Ctrl Pts',(-0.905045809395506,2.80445036847489,
3.97750668718195));
#90828=CARTESIAN_POINT('Ctrl Pts',(-1.83370477250061,2.50475567177548,4.03054010967771));
#90829=CARTESIAN_POINT('Ctrl Pts',(-2.59870661200473,1.69793937206912,4.08357353217347));
#90830=CARTESIAN_POINT('Ctrl Pts',(-2.84860286558964,0.754659856831406,
4.13660695466923));
#90831=CARTESIAN_POINT('Ctrl Pts',(-2.9133416376511,0.510291417324331,4.15034593074966));
#90832=CARTESIAN_POINT('Ctrl Pts',(-2.94350990785796,0.256764463573631,
4.16408490683008));
#90833=CARTESIAN_POINT('Ctrl Pts',(-2.94122604762498,0.00270348896235926,
4.17782388291051));
#90834=CARTESIAN_POINT('Origin',(0.,0.,0.));
#90835=CARTESIAN_POINT('',(-2.93720214312355,-0.000469105519047275,5.3221761170896));
#90836=CARTESIAN_POINT('',(-2.93728841713612,-0.000715510856791167,5.17782388291051));
#90837=CARTESIAN_POINT('',(-2.942,-3.60291088309151E-16,0.));
#90838=CARTESIAN_POINT('Ctrl Pts',(-2.93720214312355,-0.000469105519047275,
5.3221761170896));
#90839=CARTESIAN_POINT('Ctrl Pts',(-2.93646371746741,0.51995090163242,5.29412995926307));
#90840=CARTESIAN_POINT('Ctrl Pts',(-2.80485920517972,1.04071981632219,5.26608380143654));
#90841=CARTESIAN_POINT('Ctrl Pts',(-2.54457459694768,1.48632472952113,5.23803764361001));
#90842=CARTESIAN_POINT('Ctrl Pts',(-2.05250308116121,2.32874674813021,5.18501600899462));
#90843=CARTESIAN_POINT('Ctrl Pts',(-1.10052368210578,2.9025295761171,5.13199437437923));
#90844=CARTESIAN_POINT('Ctrl Pts',(-0.125806028712567,2.94417966913734,
5.07897273976385));
#90845=CARTESIAN_POINT('Ctrl Pts',(0.848911624680633,2.98582976215758,5.02595110514846));
#90846=CARTESIAN_POINT('Ctrl Pts',(1.84636753241161,2.49534712021119,4.97292947053308));
#90847=CARTESIAN_POINT('Ctrl Pts',(2.40850826444871,1.69797203189426,4.9199078359177));
#90848=CARTESIAN_POINT('Ctrl Pts',(2.97064899648583,0.90059694357731,4.86688620130232));
#90849=CARTESIAN_POINT('Ctrl Pts',(3.09747455282905,-0.203670591110202,
4.81386456668693));
#90850=CARTESIAN_POINT('Ctrl Pts',(2.73074388176872,-1.10772692176276,4.76084293207154));
#90851=CARTESIAN_POINT('Ctrl Pts',(2.36401321070839,-2.01178325241532,4.70782129745616));
#90852=CARTESIAN_POINT('Ctrl Pts',(1.50372631224452,-2.71562837903293,4.65479966284077));
#90853=CARTESIAN_POINT('Ctrl Pts',(0.544945626332551,-2.8960413231487,4.60177802822539));
#90854=CARTESIAN_POINT('Ctrl Pts',(-0.413835059579424,-3.07645426726447,
4.54875639361));
#90855=CARTESIAN_POINT('Ctrl Pts',(-1.47110953293949,-2.73343502887838,
4.49573475899462));
#90856=CARTESIAN_POINT('Ctrl Pts',(-2.14135437837727,-2.02450549694995,
4.44271312437924));
#90857=CARTESIAN_POINT('Ctrl Pts',(-2.64925590704205,-1.48728929091278,
4.40253412194936));
#90858=CARTESIAN_POINT('Ctrl Pts',(-2.93491024145304,-0.739953419037798,
4.36235511951948));
#90859=CARTESIAN_POINT('Ctrl Pts',(-2.94172250344281,0.00271694754677573,
4.3221761170896));
#90860=CARTESIAN_POINT('Ctrl Pts',(-2.94122604762498,0.00270348896235926,
4.17782388291051));
#90861=CARTESIAN_POINT('Ctrl Pts',(-2.93469404531129,-0.723928924883364,
4.21711832932584));
#90862=CARTESIAN_POINT('Ctrl Pts',(-2.66270342590315,-1.45492963249676,
4.25641277574117));
#90863=CARTESIAN_POINT('Ctrl Pts',(-2.17481432996248,-1.98852518595228,
4.2957072221565));
#90864=CARTESIAN_POINT('Ctrl Pts',(-1.51633887308468,-2.70868798272918,
4.34874064465227));
#90865=CARTESIAN_POINT('Ctrl Pts',(-0.464597291663352,-3.0692708455139,
4.40177406714803));
#90866=CARTESIAN_POINT('Ctrl Pts',(0.497231234682031,-2.90461888803337,
4.45480748964379));
#90867=CARTESIAN_POINT('Ctrl Pts',(1.45905976102742,-2.73996693055284,4.50784091213955));
#90868=CARTESIAN_POINT('Ctrl Pts',(2.33097523229686,-2.05008015280707,4.5608743346353));
#90869=CARTESIAN_POINT('Ctrl Pts',(2.71241213919701,-1.15189850786832,4.61390775713106));
#90870=CARTESIAN_POINT('Ctrl Pts',(3.09384904609714,-0.253716862929587,
4.66694117962682));
#90871=CARTESIAN_POINT('Ctrl Pts',(2.984807388628,0.852759649202112,4.71997460212259));
#90872=CARTESIAN_POINT('Ctrl Pts',(2.43538184742155,1.65920614828456,4.77300802461835));
#90873=CARTESIAN_POINT('Ctrl Pts',(1.88595630621511,2.46565264736702,4.82604144711411));
#90874=CARTESIAN_POINT('Ctrl Pts',(0.896146881271349,2.97206913340023,4.87907486960986));
#90875=CARTESIAN_POINT('Ctrl Pts',(-0.0793194161058163,2.94580349235183,
4.93210829210562));
#90876=CARTESIAN_POINT('Ctrl Pts',(-1.05478571348298,2.91953785130342,4.98514171460138));
#90877=CARTESIAN_POINT('Ctrl Pts',(-2.01590888329356,2.36059008317341,5.03817513709714));
#90878=CARTESIAN_POINT('Ctrl Pts',(-2.52114062795194,1.52574562735251,5.0912085595929));
#90879=CARTESIAN_POINT('Ctrl Pts',(-2.79619240256571,1.0712503357804,5.1200803340321));
#90880=CARTESIAN_POINT('Ctrl Pts',(-2.93612746598571,0.53498501956348,5.14895210847131));
#90881=CARTESIAN_POINT('Ctrl Pts',(-2.93728841713612,-0.000715510856791167,
5.17782388291051));
#90882=CARTESIAN_POINT('Origin',(0.,0.,0.));
#90883=CARTESIAN_POINT('',(-2.94344957106371,-0.00254475878011751,6.32217611708959));
#90884=CARTESIAN_POINT('',(-2.94385951897541,-0.00245237012002547,6.17782388291051));
#90885=CARTESIAN_POINT('',(-2.942,-3.60291088309151E-16,0.));
#90886=CARTESIAN_POINT('Ctrl Pts',(-2.94344957106371,-0.00254475878011751,
6.32217611708959));
#90887=CARTESIAN_POINT('Ctrl Pts',(-2.93616232120099,0.795681372462419,
6.27892643362204));
#90888=CARTESIAN_POINT('Ctrl Pts',(-2.59990813395451,1.59931200027747,6.23567675015448));
#90889=CARTESIAN_POINT('Ctrl Pts',(-2.02065345820614,2.14498966963894,6.19242706668693));
#90890=CARTESIAN_POINT('Ctrl Pts',(-1.31052040509786,2.81395923618761,6.13940543207154));
#90891=CARTESIAN_POINT('Ctrl Pts',(-0.235173278132946,3.0952421301662,6.08638379745616));
#90892=CARTESIAN_POINT('Ctrl Pts',(0.711565152013647,2.85966713368149,6.03336216284077));
#90893=CARTESIAN_POINT('Ctrl Pts',(1.65830358216024,2.62409213719678,5.98034052822539));
#90894=CARTESIAN_POINT('Ctrl Pts',(2.47643331548851,1.87165925024877,5.92731889361));
#90895=CARTESIAN_POINT('Ctrl Pts',(2.79025139845639,0.947902006765649,5.87429725899462));
#90896=CARTESIAN_POINT('Ctrl Pts',(3.10406948142426,0.024144763282521,5.82127562437923));
#90897=CARTESIAN_POINT('Ctrl Pts',(2.91357591403173,-1.07093683673572,5.76825398976385));
#90898=CARTESIAN_POINT('Ctrl Pts',(2.30624948232532,-1.83445752370893,5.71523235514847));
#90899=CARTESIAN_POINT('Ctrl Pts',(1.6989230506189,-2.59797821068214,5.66221072053309));
#90900=CARTESIAN_POINT('Ctrl Pts',(0.674763754598609,-3.02993798461032,
5.6091890859177));
#90901=CARTESIAN_POINT('Ctrl Pts',(-0.29591219946945,-2.93197152974308,
5.55616745130231));
#90902=CARTESIAN_POINT('Ctrl Pts',(-1.26658815353752,-2.83400507487583,
5.50314581668693));
#90903=CARTESIAN_POINT('Ctrl Pts',(-2.18378076565335,-2.20611239121314,
5.45012418207154));
#90904=CARTESIAN_POINT('Ctrl Pts',(-2.6262952554525,-1.33663544476617,5.39710254745616));
#90905=CARTESIAN_POINT('Ctrl Pts',(-2.83473866631452,-0.927074301433759,
5.37212707066731));
#90906=CARTESIAN_POINT('Ctrl Pts',(-2.93785972099746,-0.463910047749339,
5.34715159387845));
#90907=CARTESIAN_POINT('Ctrl Pts',(-2.93720214312355,-0.000469105519047275,
5.3221761170896));
#90908=CARTESIAN_POINT('Ctrl Pts',(-2.93728841713612,-0.000715510856791167,
5.17782388291051));
#90909=CARTESIAN_POINT('Ctrl Pts',(-2.93825997131497,-0.449022133194243,
5.20198553096707));
#90910=CARTESIAN_POINT('Ctrl Pts',(-2.84204308495302,-0.896933215975224,
5.22614717902362));
#90911=CARTESIAN_POINT('Ctrl Pts',(-2.64649421691623,-1.29619371435045,
5.25030882708018));
#90912=CARTESIAN_POINT('Ctrl Pts',(-2.21727574171593,-2.17254745672079,
5.30334224957594));
#90913=CARTESIAN_POINT('Ctrl Pts',(-1.30949847180912,-2.81451379794974,
5.3563756720717));
#90914=CARTESIAN_POINT('Ctrl Pts',(-0.34020313693593,-2.92716784809496,
5.40940909456746));
#90915=CARTESIAN_POINT('Ctrl Pts',(0.629092197937262,-3.03982189824018,
5.46244251706321));
#90916=CARTESIAN_POINT('Ctrl Pts',(1.65990559777684,-2.62316365730168,5.51547593955898));
#90917=CARTESIAN_POINT('Ctrl Pts',(2.2786724705311,-1.86860952511248,5.56850936205474));
#90918=CARTESIAN_POINT('Ctrl Pts',(2.89743934328536,-1.11405539292327,5.6215427845505));
#90919=CARTESIAN_POINT('Ctrl Pts',(3.1041596889543,-0.0216053694833598,
5.67457620704626));
#90920=CARTESIAN_POINT('Ctrl Pts',(2.80386439268148,0.90685955514088,5.72760962954202));
#90921=CARTESIAN_POINT('Ctrl Pts',(2.50356909640867,1.8353244797651,5.78064305203778));
#90922=CARTESIAN_POINT('Ctrl Pts',(1.69625815819413,2.59980430557365,5.83367647453354));
#90923=CARTESIAN_POINT('Ctrl Pts',(0.752817206002227,2.84909038811436,5.8867098970293));
#90924=CARTESIAN_POINT('Ctrl Pts',(-0.190623746189707,3.09837647065508,
5.93974331952506));
#90925=CARTESIAN_POINT('Ctrl Pts',(-1.27019471235901,2.83246880992794,5.99277674202081));
#90926=CARTESIAN_POINT('Ctrl Pts',(-1.98993145274738,2.17352768527678,6.04581016451657));
#90927=CARTESIAN_POINT('Ctrl Pts',(-2.5871342410519,1.62677016285567,6.08981473731455));
#90928=CARTESIAN_POINT('Ctrl Pts',(-2.93659552111978,0.809413858651952,
6.13381931011253));
#90929=CARTESIAN_POINT('Ctrl Pts',(-2.94385951897541,-0.00245237012002547,
6.17782388291051));
#90930=CARTESIAN_POINT('Origin',(0.,0.,0.));
#90931=CARTESIAN_POINT('',(-2.94561041112727,0.0017180900162133,7.3221761170896));
#90932=CARTESIAN_POINT('',(-2.94532408079935,0.00188850225021302,7.17782388291051));
#90933=CARTESIAN_POINT('',(-2.942,-3.60291088309151E-16,0.));
#90934=CARTESIAN_POINT('Ctrl Pts',(-2.94561041112727,0.0017180900162133,
7.3221761170896));
#90935=CARTESIAN_POINT('Ctrl Pts',(-2.94630377550943,0.101773161046659,
7.3167445425964));
#90936=CARTESIAN_POINT('Ctrl Pts',(-2.94164939634066,0.201762961465683,
7.3113129681032));
#90937=CARTESIAN_POINT('Ctrl Pts',(-2.93143493536931,0.301181507922605,
7.30588139361001));
#90938=CARTESIAN_POINT('Ctrl Pts',(-2.83172399186774,1.271679813862,7.25285975899462));
#90939=CARTESIAN_POINT('Ctrl Pts',(-2.20218380394821,2.18774239999403,7.19983812437924));
#90940=CARTESIAN_POINT('Ctrl Pts',(-1.33191290738037,2.62869341844419,7.14681648976385));
#90941=CARTESIAN_POINT('Ctrl Pts',(-0.46164201081253,3.06964443689435,7.09379485514847));
#90942=CARTESIAN_POINT('Ctrl Pts',(0.649359594403592,3.03548388766263,7.04077322053308));
#90943=CARTESIAN_POINT('Ctrl Pts',(1.49089582631948,2.54189903735011,6.9877515859177));
#90944=CARTESIAN_POINT('Ctrl Pts',(2.33243205823535,2.04831418703759,6.93472995130231));
#90945=CARTESIAN_POINT('Ctrl Pts',(2.90450291685098,1.09530503564424,6.88170831668693));
#90946=CARTESIAN_POINT('Ctrl Pts',(2.94440103136477,0.120514096753516,6.82868668207154));
#90947=CARTESIAN_POINT('Ctrl Pts',(2.98429914587856,-0.85427684213721,6.77566504745616));
#90948=CARTESIAN_POINT('Ctrl Pts',(2.49202451629054,-1.85084956852532,6.72264341284077));
#90949=CARTESIAN_POINT('Ctrl Pts',(1.69364035086188,-2.41155622844475,6.66962177822539));
#90950=CARTESIAN_POINT('Ctrl Pts',(0.895256185433229,-2.97226288836418,
6.61660014361));
#90951=CARTESIAN_POINT('Ctrl Pts',(-0.209237515836049,-3.09710348181494,
6.56357850899462));
#90952=CARTESIAN_POINT('Ctrl Pts',(-1.11263324192275,-2.72874849518725,
6.51055687437924));
#90953=CARTESIAN_POINT('Ctrl Pts',(-2.01602896800946,-2.36039350855957,
6.45753523976386));
#90954=CARTESIAN_POINT('Ctrl Pts',(-2.71832671891359,-1.49884294185344,
6.40451360514847));
#90955=CARTESIAN_POINT('Ctrl Pts',(-2.89701610473984,-0.539739538940995,
6.35149197053308));
#90956=CARTESIAN_POINT('Ctrl Pts',(-2.9299487738587,-0.362975626116294,
6.34172001938525));
#90957=CARTESIAN_POINT('Ctrl Pts',(-2.9450960721234,-0.182898142528554,
6.33194806823742));
#90958=CARTESIAN_POINT('Ctrl Pts',(-2.94344957106371,-0.00254475878011751,
6.32217611708959));
#90959=CARTESIAN_POINT('Ctrl Pts',(-2.94385951897541,-0.00245237012002547,
6.17782388291051));
#90960=CARTESIAN_POINT('Ctrl Pts',(-2.94534994464423,-0.169030925215637,
6.18685273260829));
#90961=CARTESIAN_POINT('Ctrl Pts',(-2.93243429156208,-0.335378354983467,
6.19588158230608));
#90962=CARTESIAN_POINT('Ctrl Pts',(-2.90429666833196,-0.499109855256177,
6.20491043200386));
#90963=CARTESIAN_POINT('Ctrl Pts',(-2.73902262892075,-1.46083168256277,
6.25794385449962));
#90964=CARTESIAN_POINT('Ctrl Pts',(-2.04857203549091,-2.33230074860083,
6.31097727699537));
#90965=CARTESIAN_POINT('Ctrl Pts',(-1.15014386281302,-2.71315662653886,
6.36401069949113));
#90966=CARTESIAN_POINT('Ctrl Pts',(-0.251715690135105,-3.09401250447689,
6.41704412198689));
#90967=CARTESIAN_POINT('Ctrl Pts',(0.854690061790863,-2.98425519431488,
6.47007754448265));
#90968=CARTESIAN_POINT('Ctrl Pts',(1.66078102051885,-2.43430815370249,6.52311096697841));
#90969=CARTESIAN_POINT('Ctrl Pts',(2.46687197924684,-1.8843611130901,6.57614438947417));
#90970=CARTESIAN_POINT('Ctrl Pts',(2.97264814477684,-0.89422434202733,6.62917781196992));
#90971=CARTESIAN_POINT('Ctrl Pts',(2.94575157188272,0.0812247625331604,
6.68221123446569));
#90972=CARTESIAN_POINT('Ctrl Pts',(2.91885499898859,1.05667386709364,6.73524465696145));
#90973=CARTESIAN_POINT('Ctrl Pts',(2.35928568767037,2.01743530515185,6.78827807945721));
#90974=CARTESIAN_POINT('Ctrl Pts',(1.52411461962062,2.52212696182345,6.84131150195297));
#90975=CARTESIAN_POINT('Ctrl Pts',(0.688943551570855,3.02681861849506,6.89434492444873));
#90976=CARTESIAN_POINT('Ctrl Pts',(-0.421829273210428,3.07544049378006,
6.94737834694448));
#90977=CARTESIAN_POINT('Ctrl Pts',(-1.29790521123388,2.64565527761082,7.00041176944024));
#90978=CARTESIAN_POINT('Ctrl Pts',(-2.17398114925735,2.21587006144158,7.053445191936));
#90979=CARTESIAN_POINT('Ctrl Pts',(-2.81536020052296,1.30767775381808,7.10647861443177));
#90980=CARTESIAN_POINT('Ctrl Pts',(-2.92738728118153,0.338309756398913,
7.15951203692753));
#90981=CARTESIAN_POINT('Ctrl Pts',(-2.94028117934613,0.226739123929774,
7.16561598558852));
#90982=CARTESIAN_POINT('Ctrl Pts',(-2.94616267287143,0.114358087958319,
7.17171993424952));
#90983=CARTESIAN_POINT('Ctrl Pts',(-2.94532408079935,0.00188850225021302,
7.17782388291051));
#90984=CARTESIAN_POINT('Origin',(0.,0.,0.));
#90985=CARTESIAN_POINT('',(-2.93809888154578,0.00167770611676693,8.3221761170896));
#90986=CARTESIAN_POINT('',(-2.93791306433702,0.00153065962940209,8.17782388291051));
#90987=CARTESIAN_POINT('',(-2.942,-3.60291088309151E-16,0.));
#90988=CARTESIAN_POINT('Ctrl Pts',(-2.93809888154578,0.00167770611676693,
8.3221761170896));
#90989=CARTESIAN_POINT('Ctrl Pts',(-2.94007633420882,0.384287406036693,
8.30154101695538));
#90990=CARTESIAN_POINT('Ctrl Pts',(-2.87073335467684,0.766208258950615,
8.28090591682115));
#90991=CARTESIAN_POINT('Ctrl Pts',(-2.72674429344234,1.11753596774236,8.26027081668693));
#90992=CARTESIAN_POINT('Ctrl Pts',(-2.35676618120986,2.02026817086468,8.20724918207155));
#90993=CARTESIAN_POINT('Ctrl Pts',(-1.49395472948062,2.72101627730632,8.15422754745616));
#90994=CARTESIAN_POINT('Ctrl Pts',(-0.534531707931531,2.89798152758675,
8.10120591284077));
#90995=CARTESIAN_POINT('Ctrl Pts',(0.424891313617566,3.07494677786719,8.04818427822539));
#90996=CARTESIAN_POINT('Ctrl Pts',(1.48092590498651,2.72812917198643,7.99516264361001));
#90997=CARTESIAN_POINT('Ctrl Pts',(2.14861803155556,2.0167948917757,7.94214100899462));
#90998=CARTESIAN_POINT('Ctrl Pts',(2.81631015812461,1.30546061156497,7.88911937437924));
#90999=CARTESIAN_POINT('Ctrl Pts',(3.09565981989376,0.229609657024259,7.83609773976385));
#91000=CARTESIAN_POINT('Ctrl Pts',(2.85838358121436,-0.716703832599229,
7.78307610514847));
#91001=CARTESIAN_POINT('Ctrl Pts',(2.62110734253496,-1.6630173222227,7.73005447053308));
#91002=CARTESIAN_POINT('Ctrl Pts',(1.86720520340702,-2.47979334692897,7.6770328359177));
#91003=CARTESIAN_POINT('Ctrl Pts',(0.942885410290185,-2.79195060559462,
7.62401120130232));
#91004=CARTESIAN_POINT('Ctrl Pts',(0.0185656171733344,-3.10410786426027,
7.57098956668693));
#91005=CARTESIAN_POINT('Ctrl Pts',(-1.07617182993241,-2.91164635688529,
7.51796793207155));
#91006=CARTESIAN_POINT('Ctrl Pts',(-1.83859970394347,-2.30294859032442,
7.46494629745616));
#91007=CARTESIAN_POINT('Ctrl Pts',(-2.52292391662041,-1.75660626200873,
7.41735623733397));
#91008=CARTESIAN_POINT('Ctrl Pts',(-2.93953533056363,-0.874938734231028,
7.36976617721179));
#91009=CARTESIAN_POINT('Ctrl Pts',(-2.94561041112727,0.0017180900162133,
7.3221761170896));
#91010=CARTESIAN_POINT('Ctrl Pts',(-2.94532408079935,0.00188850225021302,
7.17782388291051));
#91011=CARTESIAN_POINT('Ctrl Pts',(-2.93887666669244,-0.862820356365606,
7.22475335674527));
#91012=CARTESIAN_POINT('Ctrl Pts',(-2.53519706632201,-1.73276349436296,
7.27168283058004));
#91013=CARTESIAN_POINT('Ctrl Pts',(-1.8671352754884,-2.27988062150739,7.3186123044148));
#91014=CARTESIAN_POINT('Ctrl Pts',(-1.11218107908521,-2.89815931477968,
7.37164572691056));
#91015=CARTESIAN_POINT('Ctrl Pts',(-0.0195975762272904,-3.10417301410946,
7.42467914940632));
#91016=CARTESIAN_POINT('Ctrl Pts',(0.908672921418664,-2.80327724408032,
7.47771257190208));
#91017=CARTESIAN_POINT('Ctrl Pts',(1.83694341906463,-2.50238147405117,7.53074599439785));
#91018=CARTESIAN_POINT('Ctrl Pts',(2.60090091149863,-1.69457623466311,7.5837794168936));
#91019=CARTESIAN_POINT('Ctrl Pts',(2.84957671873934,-0.750974240115352,
7.63681283938936));
#91020=CARTESIAN_POINT('Ctrl Pts',(3.09825252598004,0.192627754432404,7.68984626188512));
#91021=CARTESIAN_POINT('Ctrl Pts',(2.83164664802746,1.27202650413984,7.74287968438088));
#91022=CARTESIAN_POINT('Ctrl Pts',(2.17224013125782,1.99133688698097,7.79591310687664));
#91023=CARTESIAN_POINT('Ctrl Pts',(1.51283361448819,2.71064726982209,7.8489465293724));
#91024=CARTESIAN_POINT('Ctrl Pts',(0.460626458901515,3.06986928579691,7.90197995186816));
#91025=CARTESIAN_POINT('Ctrl Pts',(-0.500988267012792,2.90397323362554,
7.95501337436392));
#91026=CARTESIAN_POINT('Ctrl Pts',(-1.46260299292711,2.73807718145418,8.00804679685968));
#91027=CARTESIAN_POINT('Ctrl Pts',(-2.33362528916906,2.04706306113661,8.06108021935544));
#91028=CARTESIAN_POINT('Ctrl Pts',(-2.71389997881596,1.14838873656999,8.1141136418512));
#91029=CARTESIAN_POINT('Ctrl Pts',(-2.86617748613125,0.788522856039455,
8.13535038887097));
#91030=CARTESIAN_POINT('Ctrl Pts',(-2.93976221721368,0.395358070397946,
8.15658713589074));
#91031=CARTESIAN_POINT('Ctrl Pts',(-2.93791306433702,0.00153065962940209,
8.17782388291051));
#91032=CARTESIAN_POINT('Origin',(0.,0.,0.));
#91033=CARTESIAN_POINT('',(-2.93946271110901,-0.00237070406174211,9.3221761170896));
#91034=CARTESIAN_POINT('',(-2.93970717506282,-0.00244914695740897,9.1778238829105));
#91035=CARTESIAN_POINT('',(-2.942,-3.60291088309151E-16,0.));
#91036=CARTESIAN_POINT('Ctrl Pts',(-2.93946271110901,-0.00237070406174211,
9.3221761170896));
#91037=CARTESIAN_POINT('Ctrl Pts',(-2.93446464588925,0.661363954518237,
9.28633749131435));
#91038=CARTESIAN_POINT('Ctrl Pts',(-2.71199962688196,1.32813253283145,9.2504988655391));
#91039=CARTESIAN_POINT('Ctrl Pts',(-2.29964025869718,1.84273594462077,9.21466023976385));
#91040=CARTESIAN_POINT('Ctrl Pts',(-1.68957312366702,2.60406854266272,9.16163860514847));
#91041=CARTESIAN_POINT('Ctrl Pts',(-0.663867679221267,3.03234398107946,
9.10861697053308));
#91042=CARTESIAN_POINT('Ctrl Pts',(0.306449843415351,2.93088887105754,9.0555953359177));
#91043=CARTESIAN_POINT('Ctrl Pts',(1.27676736605195,2.82943376103562,9.00257370130232));
#91044=CARTESIAN_POINT('Ctrl Pts',(2.19169696687942,2.19824810257508,8.94955206668694));
#91045=CARTESIAN_POINT('Ctrl Pts',(2.63108308949774,1.32718606727815,8.89653043207155));
#91046=CARTESIAN_POINT('Ctrl Pts',(3.07046921211607,0.456124031981203,8.84350879745617));
#91047=CARTESIAN_POINT('Ctrl Pts',(3.03431185652521,-0.654814380152138,
8.79048716284078));
#91048=CARTESIAN_POINT('Ctrl Pts',(2.53921526620191,-1.49546210681027,8.73746552822539));
#91049=CARTESIAN_POINT('Ctrl Pts',(2.04411867587862,-2.33610983346839,8.68444389361001));
#91050=CARTESIAN_POINT('Ctrl Pts',(1.09008285082291,-2.90646687465129,8.63142225899462));
#91051=CARTESIAN_POINT('Ctrl Pts',(0.115221775476145,-2.94461288176806,
8.57840062437923));
#91052=CARTESIAN_POINT('Ctrl Pts',(-0.85963929987063,-2.98275888888482,
8.52537898976385));
#91053=CARTESIAN_POINT('Ctrl Pts',(-1.85532562550848,-2.48869386193542,
8.47235735514847));
#91054=CARTESIAN_POINT('Ctrl Pts',(-2.41459640195952,-1.6893031985592,8.41933572053308));
#91055=CARTESIAN_POINT('Ctrl Pts',(-2.75620869696377,-1.20102150993995,
8.38694918605192));
#91056=CARTESIAN_POINT('Ctrl Pts',(-2.9349952940449,-0.598823486447531,
8.35456265157076));
#91057=CARTESIAN_POINT('Ctrl Pts',(-2.93809888154578,0.00167770611676693,
8.3221761170896));
#91058=CARTESIAN_POINT('Ctrl Pts',(-2.93791306433702,0.00153065962940209,
8.17782388291051));
#91059=CARTESIAN_POINT('Ctrl Pts',(-2.9351444240236,-0.588126615192338,
8.2096205583865));
#91060=CARTESIAN_POINT('Ctrl Pts',(-2.7632717718794,-1.17926933079271,8.24141723386249));
#91061=CARTESIAN_POINT('Ctrl Pts',(-2.4332334415684,-1.66235519794395,8.27321390933847));
#91062=CARTESIAN_POINT('Ctrl Pts',(-1.88276513162211,-2.46809027907558,
8.32624733183424));
#91063=CARTESIAN_POINT('Ctrl Pts',(-0.892301428677693,-2.97322591252315,
8.37928075433));
#91064=CARTESIAN_POINT('Ctrl Pts',(0.0831300749779144,-2.94569841903957,
8.43231417682576));
#91065=CARTESIAN_POINT('Ctrl Pts',(1.0585615786335,-2.91817092555599,8.48534759932152));
#91066=CARTESIAN_POINT('Ctrl Pts',(2.01896088300028,-2.35798030514126,8.53838102181727));
#91067=CARTESIAN_POINT('Ctrl Pts',(2.52311224054409,-1.52248297426101,8.59141444431303));
#91068=CARTESIAN_POINT('Ctrl Pts',(3.02726359808791,-0.686985643380747,
8.64444786680879));
#91069=CARTESIAN_POINT('Ctrl Pts',(3.07516700880875,0.423818397965051,8.69748128930456));
#91070=CARTESIAN_POINT('Ctrl Pts',(2.64481523147421,1.29961616512727,8.75051471180032));
#91071=CARTESIAN_POINT('Ctrl Pts',(2.21446345413967,2.17541393228948,8.80354813429608));
#91072=CARTESIAN_POINT('Ctrl Pts',(1.30585648874975,2.81620542526811,8.85658155679183));
#91073=CARTESIAN_POINT('Ctrl Pts',(0.336416234327566,2.92760548957316,8.90961497928759));
#91074=CARTESIAN_POINT('Ctrl Pts',(-0.633024020094595,3.03900555387821,
8.96264840178335));
#91075=CARTESIAN_POINT('Ctrl Pts',(-1.66329756354901,2.62101418950972,9.01568182427912));
#91076=CARTESIAN_POINT('Ctrl Pts',(-2.2810878186777,1.86566024473329,9.06871524677488));
#91077=CARTESIAN_POINT('Ctrl Pts',(-2.70475933865403,1.34764955866819,9.10508479215342));
#91078=CARTESIAN_POINT('Ctrl Pts',(-2.93443931783068,0.67097671916862,9.14145433753196));
#91079=CARTESIAN_POINT('Ctrl Pts',(-2.93970717506282,-0.00244914695740897,
9.1778238829105));
#91080=CARTESIAN_POINT('Origin',(0.,0.,0.));
#91081=CARTESIAN_POINT('',(-2.94667766504495,-0.000677344457850615,10.3221761170896));
#91082=CARTESIAN_POINT('',(-2.94675654686086,-0.000527081537143387,10.1778238829105));
#91083=CARTESIAN_POINT('',(-2.942,-3.60291088309151E-16,0.));
#91084=CARTESIAN_POINT('Ctrl Pts',(-2.94667766504495,-0.000677344457850615,
10.3221761170896));
#91085=CARTESIAN_POINT('Ctrl Pts',(-2.9437606123768,0.938668430873604,10.2711339656733));
#91086=CARTESIAN_POINT('Ctrl Pts',(-2.45547363684786,1.8806215504616,10.2200918142571));
#91087=CARTESIAN_POINT('Ctrl Pts',(-1.68496058899857,2.41762877517203,10.1690496628408));
#91088=CARTESIAN_POINT('Ctrl Pts',(-0.884566010089308,2.97546186144238,
10.1160280282254));
#91089=CARTESIAN_POINT('Ctrl Pts',(0.22036931948501,3.09633132563897,10.06300639361));
#91090=CARTESIAN_POINT('Ctrl Pts',(1.12243508338583,2.72473128300808,10.0099847589946));
#91091=CARTESIAN_POINT('Ctrl Pts',(2.02450084728663,2.35313124037721,9.95696312437924));
#91092=CARTESIAN_POINT('Ctrl Pts',(2.72369704551392,1.48906169091887,9.90394148976386));
#91093=CARTESIAN_POINT('Ctrl Pts',(2.89893758856608,0.529322150128768,9.85091985514847));
#91094=CARTESIAN_POINT('Ctrl Pts',(3.07417813161823,-0.430417390661342,
9.79789822053309));
#91095=CARTESIAN_POINT('Ctrl Pts',(2.72546301949522,-1.48582692278323,9.7448765859177));
#91096=CARTESIAN_POINT('Ctrl Pts',(2.01292981013226,-2.15223945240745,9.69185495130231));
#91097=CARTESIAN_POINT('Ctrl Pts',(1.30039660076932,-2.81865198203167,9.63883331668693));
#91098=CARTESIAN_POINT('Ctrl Pts',(0.22404529416644,-3.09606750915824,9.58581168207154));
#91099=CARTESIAN_POINT('Ctrl Pts',(-0.721840197888351,-2.85709079479997,
9.53279004745616));
#91100=CARTESIAN_POINT('Ctrl Pts',(-1.66772568994314,-2.6181140804417,9.47976841284078));
#91101=CARTESIAN_POINT('Ctrl Pts',(-2.48314536744984,-1.8627451245986,9.42674677822539));
#91102=CARTESIAN_POINT('Ctrl Pts',(-2.79364079339589,-0.937865767843463,
9.37372514361001));
#91103=CARTESIAN_POINT('Ctrl Pts',(-2.89426473091789,-0.638135096043858,
9.35654213476987));
#91104=CARTESIAN_POINT('Ctrl Pts',(-2.94185905854134,-0.320601614404311,
9.33935912592974));
#91105=CARTESIAN_POINT('Ctrl Pts',(-2.93946271110901,-0.00237070406174211,
9.3221761170896));
#91106=CARTESIAN_POINT('Ctrl Pts',(-2.93970717506282,-0.00244914695740897,
9.1778238829105));
#91107=CARTESIAN_POINT('Ctrl Pts',(-2.94212081330531,-0.311000869666037,
9.19448776002772));
#91108=CARTESIAN_POINT('Ctrl Pts',(-2.89742341321448,-0.618870952337822,
9.21115163714493));
#91109=CARTESIAN_POINT('Ctrl Pts',(-2.80268892270593,-0.91048590754583,
9.22781551426215));
#91110=CARTESIAN_POINT('Ctrl Pts',(-2.50119280480251,-1.83856158986408,
9.28084893675791));
#91111=CARTESIAN_POINT('Ctrl Pts',(-1.69289360219275,-2.6019964293162,9.33388235925367));
#91112=CARTESIAN_POINT('Ctrl Pts',(-0.749130960052534,-2.8500618572215,
9.38691578174943));
#91113=CARTESIAN_POINT('Ctrl Pts',(0.194631682087679,-3.09812728512679,
9.43994920424519));
#91114=CARTESIAN_POINT('Ctrl Pts',(1.27385776375836,-2.83082330148527,9.49298262674095));
#91115=CARTESIAN_POINT('Ctrl Pts',(1.99274148812309,-2.17095166846502,9.54601604923671));
#91116=CARTESIAN_POINT('Ctrl Pts',(2.71162521248781,-1.51108003544478,9.59904947173247));
#91117=CARTESIAN_POINT('Ctrl Pts',(3.07016657954661,-0.458640753045832,
9.65208289422823));
#91118=CARTESIAN_POINT('Ctrl Pts',(2.90364858401899,0.50286646917705,9.70511631672399));
#91119=CARTESIAN_POINT('Ctrl Pts',(2.73713058849137,1.46437369139994,9.75814973921975));
#91120=CARTESIAN_POINT('Ctrl Pts',(2.04555323037731,2.33494885344676,9.8111831617155));
#91121=CARTESIAN_POINT('Ctrl Pts',(1.14663312988947,2.71464219571161,9.86421658421126));
#91122=CARTESIAN_POINT('Ctrl Pts',(0.247713029401628,3.09433553797646,9.91725000670703));
#91123=CARTESIAN_POINT('Ctrl Pts',(-0.858549813459989,2.98314706045934,
9.9702834292028));
#91124=CARTESIAN_POINT('Ctrl Pts',(-1.66392867990964,2.4321577114719,10.0233168516986));
#91125=CARTESIAN_POINT('Ctrl Pts',(-2.44605620000286,1.89707546499944,10.0748191954359));
#91126=CARTESIAN_POINT('Ctrl Pts',(-2.94442204707364,0.947219947536058,
10.1263215391732));
#91127=CARTESIAN_POINT('Ctrl Pts',(-2.94675654686086,-0.000527081537143387,
10.1778238829105));
#91128=CARTESIAN_POINT('Origin',(0.,0.,0.));
#91129=CARTESIAN_POINT('',(-2.94150967972677,0.00271347918382847,11.3221761170896));
#91130=CARTESIAN_POINT('',(-2.94130162828673,0.0027079682416201,11.1778238829105));
#91131=CARTESIAN_POINT('',(-2.942,-3.60291088309151E-16,0.));
#91132=CARTESIAN_POINT('Ctrl Pts',(-2.94150967972677,0.00271347918382847,
11.3221761170896));
#91133=CARTESIAN_POINT('Ctrl Pts',(-2.94373491656768,0.247192333748545,
11.3089520746477));
#91134=CARTESIAN_POINT('Ctrl Pts',(-2.9158155052491,0.491169927694146,11.2957280322058));
#91135=CARTESIAN_POINT('Ctrl Pts',(-2.85578877861464,0.726974231288132,
11.2825039897639));
#91136=CARTESIAN_POINT('Ctrl Pts',(-2.61511236058667,1.67242867011129,11.2294823551485));
#91137=CARTESIAN_POINT('Ctrl Pts',(-1.85827902823171,2.48648936622251,11.1764607205331));
#91138=CARTESIAN_POINT('Ctrl Pts',(-0.932843095641359,2.7953219564001,11.1234390859177));
#91139=CARTESIAN_POINT('Ctrl Pts',(-0.00740716305097949,3.1041545465777,
11.0704174513023));
#91140=CARTESIAN_POINT('Ctrl Pts',(1.08663136977481,2.90775903082164,11.0173958166869));
#91141=CARTESIAN_POINT('Ctrl Pts',(1.8468662323789,2.29632449813104,10.9643741820716));
#91142=CARTESIAN_POINT('Ctrl Pts',(2.60710109498298,1.68488996544046,10.9113525474562));
#91143=CARTESIAN_POINT('Ctrl Pts',(3.03353228736538,0.658416415815393,10.8583309128408));
#91144=CARTESIAN_POINT('Ctrl Pts',(2.93033333857171,-0.311717188928345,
10.8053092782254));
#91145=CARTESIAN_POINT('Ctrl Pts',(2.82713438977805,-1.28185079367208,10.75228764361));
#91146=CARTESIAN_POINT('Ctrl Pts',(2.19430529980826,-2.1956444535345,10.6992660089946));
#91147=CARTESIAN_POINT('Ctrl Pts',(1.32245493972955,-2.63346426089346,10.6462443743792));
#91148=CARTESIAN_POINT('Ctrl Pts',(0.450604579650845,-3.07128406825242,
10.5932227397639));
#91149=CARTESIAN_POINT('Ctrl Pts',(-0.66026705053676,-3.03313002310796,
10.5402011051485));
#91150=CARTESIAN_POINT('Ctrl Pts',(-1.50002355624255,-2.53652329217291,
10.4871794705331));
#91151=CARTESIAN_POINT('Ctrl Pts',(-2.33978006194835,-2.03991656123784,
10.4341578359177));
#91152=CARTESIAN_POINT('Ctrl Pts',(-2.90842144317229,-1.08485714451215,
10.3811362013023));
#91153=CARTESIAN_POINT('Ctrl Pts',(-2.94481521966216,-0.109929081977263,
10.3281145666869));
#91154=CARTESIAN_POINT('Ctrl Pts',(-2.94617392671893,-0.0735316050958383,
10.3261350834878));
#91155=CARTESIAN_POINT('Ctrl Pts',(-2.94679079226602,-0.0371064354900674,
10.3241556002887));
#91156=CARTESIAN_POINT('Ctrl Pts',(-2.94667766504495,-0.000677344457850615,
10.3221761170896));
#91157=CARTESIAN_POINT('Ctrl Pts',(-2.94675654686086,-0.000527081537143387,
10.1778238829105));
#91158=CARTESIAN_POINT('Ctrl Pts',(-2.94682594764491,-0.0287020195940664,
10.1793549616689));
#91159=CARTESIAN_POINT('Ctrl Pts',(-2.94645696896677,-0.0568750942243903,
10.1808860404274));
#91160=CARTESIAN_POINT('Ctrl Pts',(-2.94564403384026,-0.0850353526445027,
10.1824171191858));
#91161=CARTESIAN_POINT('Ctrl Pts',(-2.91748563128357,-1.06044884731575,
10.2354505416816));
#91162=CARTESIAN_POINT('Ctrl Pts',(-2.35667393613251,-2.02048561620049,
10.2884839641773));
#91163=CARTESIAN_POINT('Ctrl Pts',(-1.52085069195865,-2.52409646370082,
10.3415173866731));
#91164=CARTESIAN_POINT('Ctrl Pts',(-0.685027447784799,-3.02770731120113,
10.3945508091689));
#91165=CARTESIAN_POINT('Ctrl Pts',(0.425807345411858,-3.07489223731705,
10.4475842316646));
#91166=CARTESIAN_POINT('Ctrl Pts',(1.30132657531592,-2.6439740788583,10.5006176541604));
#91167=CARTESIAN_POINT('Ctrl Pts',(2.17684580522,-2.21305592039955,10.5536510766561));
#91168=CARTESIAN_POINT('Ctrl Pts',(2.81704947183149,-1.3040346773661,10.6066844991519));
#91169=CARTESIAN_POINT('Ctrl Pts',(2.92782247317795,-0.334522571513875,
10.6597179216477));
#91170=CARTESIAN_POINT('Ctrl Pts',(3.0385954745244,0.634989534338361,10.7127513441434));
#91171=CARTESIAN_POINT('Ctrl Pts',(2.61993781060583,1.66499250300936,10.7657847666392));
#91172=CARTESIAN_POINT('Ctrl Pts',(1.8641844334644,2.28229406153701,10.8188181891349));
#91173=CARTESIAN_POINT('Ctrl Pts',(1.10843105632298,2.89959562006465,10.8718516116307));
#91174=CARTESIAN_POINT('Ctrl Pts',(0.0155819659587191,3.10419576844893,
10.9248850341265));
#91175=CARTESIAN_POINT('Ctrl Pts',(-0.912298512764032,2.80209942880452,
10.9779184566222));
#91176=CARTESIAN_POINT('Ctrl Pts',(-1.84017899148677,2.50000308916011,11.030951879118));
#91177=CARTESIAN_POINT('Ctrl Pts',(-2.60309085856801,1.69121026148702,11.0839853016137));
#91178=CARTESIAN_POINT('Ctrl Pts',(-2.85054580335778,0.747287366584909,
11.1370187241095));
#91179=CARTESIAN_POINT('Ctrl Pts',(-2.91401168231396,0.505195230407465,
11.1506204437098));
#91180=CARTESIAN_POINT('Ctrl Pts',(-2.94357123776359,0.254214351879716,
11.1642221633102));
#91181=CARTESIAN_POINT('Ctrl Pts',(-2.94130162828673,0.0027079682416201,
11.1778238829105));
#91182=CARTESIAN_POINT('Origin',(0.,0.,0.));
#91183=CARTESIAN_POINT('',(-2.937239763848,-0.000584049131356901,12.3221761170896));
#91184=CARTESIAN_POINT('',(-2.93727053600114,-0.00067468657406146,12.1778238829105));
#91185=CARTESIAN_POINT('',(-2.942,-3.60291088309151E-16,0.));
#91186=CARTESIAN_POINT('Ctrl Pts',(-2.937239763848,-0.000584049131356901,
12.3221761170896));
#91187=CARTESIAN_POINT('Ctrl Pts',(-2.93630723827878,0.526896498967096,
12.2937485490067));
#91188=CARTESIAN_POINT('Ctrl Pts',(-2.80088780003305,1.05482369633564,12.2653209809237));
#91189=CARTESIAN_POINT('Ctrl Pts',(-2.53382312395941,1.50458015988076,12.2368934128408));
#91190=CARTESIAN_POINT('Ctrl Pts',(-2.03570785669002,2.34344273181871,12.1838717782254));
#91191=CARTESIAN_POINT('Ctrl Pts',(-1.07962793359348,2.91036661609979,12.13085014361));
#91192=CARTESIAN_POINT('Ctrl Pts',(-0.104636033354822,2.94500804439343,
12.0778285089946));
#91193=CARTESIAN_POINT('Ctrl Pts',(0.870355866883847,2.97964947268707,12.0248068743792));
#91194=CARTESIAN_POINT('Ctrl Pts',(1.86425974426462,2.48200844499326,11.9717852397639));
#91195=CARTESIAN_POINT('Ctrl Pts',(2.42065333828634,1.68061253620858,11.9187636051485));
#91196=CARTESIAN_POINT('Ctrl Pts',(2.97704693230805,0.879216627423909,11.8657419705331));
#91197=CARTESIAN_POINT('Ctrl Pts',(3.09593024297072,-0.22593416245163,11.8127203359177));
#91198=CARTESIAN_POINT('Ctrl Pts',(2.72270947038747,-1.12733057302667,11.7596987013023));
#91199=CARTESIAN_POINT('Ctrl Pts',(2.34948869780421,-2.02872698360171,11.7066770666869));
#91200=CARTESIAN_POINT('Ctrl Pts',(1.48416384197505,-2.72636901487625,11.6536554320716));
#91201=CARTESIAN_POINT('Ctrl Pts',(0.524110882362077,-2.89988428458928,
11.6006337974562));
#91202=CARTESIAN_POINT('Ctrl Pts',(-0.435942077250893,-3.07339955430231,
11.5476121628408));
#91203=CARTESIAN_POINT('Ctrl Pts',(-1.49072314064766,-2.72278806245382,
11.4945905282254));
#91204=CARTESIAN_POINT('Ctrl Pts',(-2.15585392049559,-2.00905822576202,
11.44156889361));
#91205=CARTESIAN_POINT('Ctrl Pts',(-2.6550954793503,-1.47333862434378,11.4017713014365));
#91206=CARTESIAN_POINT('Ctrl Pts',(-2.93481285697586,-0.733042609904606,
11.3619737092631));
#91207=CARTESIAN_POINT('Ctrl Pts',(-2.94150967972677,0.00271347918382847,
11.3221761170896));
#91208=CARTESIAN_POINT('Ctrl Pts',(-2.94130162828673,0.0027079682416201,
11.1778238829105));
#91209=CARTESIAN_POINT('Ctrl Pts',(-2.9347219773889,-0.726414913814524,
11.2172555858059));
#91210=CARTESIAN_POINT('Ctrl Pts',(-2.66063931527267,-1.45995431762841,
11.2566872887014));
#91211=CARTESIAN_POINT('Ctrl Pts',(-2.16966229743749,-1.99414525558605,
11.2961189915968));
#91212=CARTESIAN_POINT('Ctrl Pts',(-1.50932582422915,-2.71260202072372,
11.3491524140925));
#91213=CARTESIAN_POINT('Ctrl Pts',(-0.456654855314183,-3.0704625888679,
11.4021858365883));
#91214=CARTESIAN_POINT('Ctrl Pts',(0.504744460963153,-2.90332271964814,
11.4552192590841));
#91215=CARTESIAN_POINT('Ctrl Pts',(1.46614377724048,-2.73618285042839,11.5082526815798));
#91216=CARTESIAN_POINT('Ctrl Pts',(2.33627144088016,-2.04404254384471,11.5612861040756));
#91217=CARTESIAN_POINT('Ctrl Pts',(2.71538327691526,-1.14487704350598,11.6143195265713));
#91218=CARTESIAN_POINT('Ctrl Pts',(3.09449511295038,-0.245711543167243,
11.6673529490671));
#91219=CARTESIAN_POINT('Ctrl Pts',(2.98259112138089,0.860479150926533,11.7203863715629));
#91220=CARTESIAN_POINT('Ctrl Pts',(2.43108096386306,1.6655014657576,11.7734197940586));
#91221=CARTESIAN_POINT('Ctrl Pts',(1.87957080634523,2.47052378058866,11.8264532165544));
#91222=CARTESIAN_POINT('Ctrl Pts',(0.88845448287903,2.97437771615703,11.8794866390501));
#91223=CARTESIAN_POINT('Ctrl Pts',(-0.0869405947359189,2.94558841630752,
11.9325200615459));
#91224=CARTESIAN_POINT('Ctrl Pts',(-1.06233567235088,2.916799116458,11.9855534840417));
#91225=CARTESIAN_POINT('Ctrl Pts',(-2.02200950411461,2.35536658119062,12.0385869065374));
#91226=CARTESIAN_POINT('Ctrl Pts',(-2.52507963088188,1.5192177733964,12.0916203290332));
#91227=CARTESIAN_POINT('Ctrl Pts',(-2.79765260301929,1.0661764307228,12.1203548469923));
#91228=CARTESIAN_POINT('Ctrl Pts',(-2.93618139806878,0.532487217082399,
12.1490893649514));
#91229=CARTESIAN_POINT('Ctrl Pts',(-2.93727053600114,-0.00067468657406146,
12.1778238829105));
#91230=CARTESIAN_POINT('Origin',(0.,0.,0.));
#91231=CARTESIAN_POINT('',(-2.94365959218558,-0.00249856367199902,13.3221761170896));
#91232=CARTESIAN_POINT('',(-2.94378501997585,-0.00247147196094728,13.1778238829105));
#91233=CARTESIAN_POINT('',(-2.942,-3.60291088309151E-16,0.));
#91234=CARTESIAN_POINT('Ctrl Pts',(-2.94365959218558,-0.00249856367199902,
13.3221761170896));
#91235=CARTESIAN_POINT('Ctrl Pts',(-2.93637971808012,0.802618607647404,
13.2785450233656));
#91236=CARTESIAN_POINT('Ctrl Pts',(-2.59348572085056,1.61318695127993,13.2349139296417));
#91237=CARTESIAN_POINT('Ctrl Pts',(-2.00518015117195,2.15946142414359,13.1912828359177));
#91238=CARTESIAN_POINT('Ctrl Pts',(-1.29025599284032,2.82330830552441,13.1382612013023));
#91239=CARTESIAN_POINT('Ctrl Pts',(-0.212914415108081,3.0968528810621,13.0852395666869));
#91240=CARTESIAN_POINT('Ctrl Pts',(0.732105916213065,2.85447753686451,13.0322179320716));
#91241=CARTESIAN_POINT('Ctrl Pts',(1.6771262475342,2.61210219266691,12.9791962974562));
#91242=CARTESIAN_POINT('Ctrl Pts',(2.48982533244424,1.85380692873404,12.9261746628408));
#91243=CARTESIAN_POINT('Ctrl Pts',(2.79699408917628,0.927817409909507,12.8731530282254));
#91244=CARTESIAN_POINT('Ctrl Pts',(3.10416284590832,0.00182789108496756,
12.82013139361));
#91245=CARTESIAN_POINT('Ctrl Pts',(2.90580127446235,-1.09185588263124,12.7671097589946));
#91246=CARTESIAN_POINT('Ctrl Pts',(2.29300131933759,-1.85099055387495,12.7140881243793));
#91247=CARTESIAN_POINT('Ctrl Pts',(1.68020136421283,-2.61012522511867,12.6610664897639));
#91248=CARTESIAN_POINT('Ctrl Pts',(0.652963025409289,-3.03471079388989,
12.6080448551485));
#91249=CARTESIAN_POINT('Ctrl Pts',(-0.316983527445643,-2.92976833970646,
12.5550232205331));
#91250=CARTESIAN_POINT('Ctrl Pts',(-1.28693008030059,-2.82482588552303,
12.5020015859177));
#91251=CARTESIAN_POINT('Ctrl Pts',(-2.19958484720692,-2.19035540838494,
12.4489799513023));
#91252=CARTESIAN_POINT('Ctrl Pts',(-2.63583692493897,-1.31771954001848,
12.3959583166869));
#91253=CARTESIAN_POINT('Ctrl Pts',(-2.83819229746733,-0.912947699978407,
12.3713642501545));
#91254=CARTESIAN_POINT('Ctrl Pts',(-2.93804653690103,-0.456933028989684,
12.346770183622));
#91255=CARTESIAN_POINT('Ctrl Pts',(-2.937239763848,-0.000584049131356901,
12.3221761170896));
#91256=CARTESIAN_POINT('Ctrl Pts',(-2.93727053600114,-0.00067468657406146,
12.1778238829105));
#91257=CARTESIAN_POINT('Ctrl Pts',(-2.93819154879431,-0.451534875631614,
12.2021227874472));
#91258=CARTESIAN_POINT('Ctrl Pts',(-2.84082973894426,-0.902017986379197,
12.2264216919838));
#91259=CARTESIAN_POINT('Ctrl Pts',(-2.64313182011494,-1.30303644108441,
12.2507205965204));
#91260=CARTESIAN_POINT('Ctrl Pts',(-2.21164746080996,-2.17827676744996,
12.3037540190162));
#91261=CARTESIAN_POINT('Ctrl Pts',(-1.30221232042921,-2.81789233986001,
12.356787441512));
#91262=CARTESIAN_POINT('Ctrl Pts',(-0.332628768749986,-2.9280382319051,
12.4098208640077));
#91263=CARTESIAN_POINT('Ctrl Pts',(0.636954782929239,-3.03818412395018,
12.4628542865035));
#91264=CARTESIAN_POINT('Ctrl Pts',(1.66668674590694,-2.61886033563027,12.5158877089993));
#91265=CARTESIAN_POINT('Ctrl Pts',(2.28349934958056,-1.86270784229927,12.568921131495));
#91266=CARTESIAN_POINT('Ctrl Pts',(2.90031195325417,-1.10655534896829,12.6219545539908));
#91267=CARTESIAN_POINT('Ctrl Pts',(3.10420519762372,-0.0135741506262503,
12.6749879764865));
#91268=CARTESIAN_POINT('Ctrl Pts',(2.80150876262273,0.914110736314876,12.7280213989823));
#91269=CARTESIAN_POINT('Ctrl Pts',(2.49881232762173,1.84179562325603,12.781054821478));
#91270=CARTESIAN_POINT('Ctrl Pts',(1.68952621325013,2.60418419879625,12.8340882439738));
#91271=CARTESIAN_POINT('Ctrl Pts',(0.745443460483677,2.85102855694575,12.8871216664696));
#91272=CARTESIAN_POINT('Ctrl Pts',(-0.198639292282781,3.09787291509526,
12.9401550889653));
#91273=CARTESIAN_POINT('Ctrl Pts',(-1.27751868344409,2.82917305585407,12.9931885114611));
#91274=CARTESIAN_POINT('Ctrl Pts',(-1.99554818878264,2.16837201871459,13.0462219339568));
#91275=CARTESIAN_POINT('Ctrl Pts',(-2.58947605453147,1.62178145836176,13.0900892502747));
#91276=CARTESIAN_POINT('Ctrl Pts',(-2.93651056908799,0.806915424962724,
13.1339565665926));
#91277=CARTESIAN_POINT('Ctrl Pts',(-2.94378501997585,-0.00247147196094728,
13.1778238829105));
#91278=CARTESIAN_POINT('Origin',(0.,0.,0.));
#91279=CARTESIAN_POINT('',(-2.94544838002636,0.00181532900233754,14.3221761170896));
#91280=CARTESIAN_POINT('',(-2.94538511207558,0.00185514841678406,14.1778238829105));
#91281=CARTESIAN_POINT('',(-2.942,-3.60291088309151E-16,0.));
#91282=CARTESIAN_POINT('Ctrl Pts',(-2.94544838002636,0.00181532900233754,
14.3221761170896));
#91283=CARTESIAN_POINT('Ctrl Pts',(-2.94622316443012,0.108911839184011,
14.31636313234));
#91284=CARTESIAN_POINT('Ctrl Pts',(-2.94089026946329,0.215930373720906,
14.3105501475904));
#91285=CARTESIAN_POINT('Ctrl Pts',(-2.929193876287,0.322248841954449,14.3047371628408));
#91286=CARTESIAN_POINT('Ctrl Pts',(-2.82250825572816,1.2920052095289,14.2517155282254));
#91287=CARTESIAN_POINT('Ctrl Pts',(-2.18639844106512,2.20351813516736,14.19869389361));
#91288=CARTESIAN_POINT('Ctrl Pts',(-1.3129798834425,2.63820107396945,14.1456722589946));
#91289=CARTESIAN_POINT('Ctrl Pts',(-0.439561325819871,3.07288401277154,
14.0926506243793));
#91290=CARTESIAN_POINT('Ctrl Pts',(0.67116597476233,3.03073696473725,14.0396289897639));
#91291=CARTESIAN_POINT('Ctrl Pts',(1.50913190300478,2.53111477028431,13.9866073551485));
#91292=CARTESIAN_POINT('Ctrl Pts',(2.34709783124724,2.03149257583137,13.9335857205331));
#91293=CARTESIAN_POINT('Ctrl Pts',(2.91230238714993,1.07439523495978,13.8805640859177));
#91294=CARTESIAN_POINT('Ctrl Pts',(2.94519135533895,0.0993426467079052,
13.8275424513023));
#91295=CARTESIAN_POINT('Ctrl Pts',(2.97808032352798,-0.875709941543982,
13.7745208166869));
#91296=CARTESIAN_POINT('Ctrl Pts',(2.47865370400332,-1.86871777717613,13.7214991820716));
#91297=CARTESIAN_POINT('Ctrl Pts',(1.67625905423563,-2.42367008153158,13.6684775474562));
#91298=CARTESIAN_POINT('Ctrl Pts',(0.873864404467956,-2.97862238588703,
13.6154559128408));
#91299=CARTESIAN_POINT('Ctrl Pts',(-0.231498275542777,-3.09551915896577,
13.5624342782254));
#91300=CARTESIAN_POINT('Ctrl Pts',(-1.13222242085015,-2.72067886211189,
13.50941264361));
#91301=CARTESIAN_POINT('Ctrl Pts',(-2.03294656615752,-2.34583856525801,
13.4563910089946));
#91302=CARTESIAN_POINT('Ctrl Pts',(-2.72903217676157,-1.47926119847154,
13.4033693743792));
#91303=CARTESIAN_POINT('Ctrl Pts',(-2.90082161259808,-0.518897921466346,
13.3503477397639));
#91304=CARTESIAN_POINT('Ctrl Pts',(-2.93124684813898,-0.348810169763627,
13.3409571988724));
#91305=CARTESIAN_POINT('Ctrl Pts',(-2.9452264095545,-0.17578062181818,13.331566657981));
#91306=CARTESIAN_POINT('Ctrl Pts',(-2.94365959218558,-0.00249856367199902,
13.3221761170896));
#91307=CARTESIAN_POINT('Ctrl Pts',(-2.94378501997585,-0.00247147196094728,
13.1778238829105));
#91308=CARTESIAN_POINT('Ctrl Pts',(-2.94530502153557,-0.171593425590788,
13.1869899890884));
#91309=CARTESIAN_POINT('Ctrl Pts',(-2.93199096538639,-0.340476157971982,
13.1961560952663));
#91310=CARTESIAN_POINT('Ctrl Pts',(-2.90299564064934,-0.506622241585387,
13.2053222014441));
#91311=CARTESIAN_POINT('Ctrl Pts',(-2.73523396766174,-1.46791324970816,
13.2583556239399));
#91312=CARTESIAN_POINT('Ctrl Pts',(-2.04253100217075,-2.33759305091599,
13.3113890464356));
#91313=CARTESIAN_POINT('Ctrl Pts',(-1.14312047815411,-2.71612322211692,
13.3644224689314));
#91314=CARTESIAN_POINT('Ctrl Pts',(-0.243709954137437,-3.09465339331786,
13.4174558914272));
#91315=CARTESIAN_POINT('Ctrl Pts',(0.862408128404901,-2.98203393451191,
13.4704893139229));
#91316=CARTESIAN_POINT('Ctrl Pts',(1.66707355482995,-2.43000319919227,13.5235227364187));
#91317=CARTESIAN_POINT('Ctrl Pts',(2.47173898125499,-1.87797246387265,13.5765561589144));
#91318=CARTESIAN_POINT('Ctrl Pts',(2.97495175156274,-0.886530452039386,
13.6295895814102));
#91319=CARTESIAN_POINT('Ctrl Pts',(2.94553156646463,0.0888458004550528,
13.682623003906));
#91320=CARTESIAN_POINT('Ctrl Pts',(2.91611138136652,1.06422205294949,13.7356564264017));
#91321=CARTESIAN_POINT('Ctrl Pts',(2.35405824086255,2.02353254610508,13.7886898488975));
#91322=CARTESIAN_POINT('Ctrl Pts',(1.51758421925744,2.52606174167593,13.8417232713932));
#91323=CARTESIAN_POINT('Ctrl Pts',(0.68111019765233,3.02859093724679,13.894756693889));
#91324=CARTESIAN_POINT('Ctrl Pts',(-0.429784705053949,3.07433883523289,
13.9477901163848));
#91325=CARTESIAN_POINT('Ctrl Pts',(-1.30474576171729,2.64228845559656,14.0008235388805));
#91326=CARTESIAN_POINT('Ctrl Pts',(-2.17970681838062,2.21023807596023,14.0538569613763));
#91327=CARTESIAN_POINT('Ctrl Pts',(-2.81873402900105,1.30038941870153,14.106890383872));
#91328=CARTESIAN_POINT('Ctrl Pts',(-2.92825276566436,0.330734826828228,
14.1599238063678));
#91329=CARTESIAN_POINT('Ctrl Pts',(-2.94057451596746,0.221640783878745,
14.1658904985487));
#91330=CARTESIAN_POINT('Ctrl Pts',(-2.94619370378806,0.111789712414528,
14.1718571907296));
#91331=CARTESIAN_POINT('Ctrl Pts',(-2.94538511207558,0.00185514841678406,
14.1778238829105));
#91332=CARTESIAN_POINT('Origin',(0.,0.,0.));
#91333=CARTESIAN_POINT('',(-2.93798069771247,0.00158343123380422,15.3221761170896));
#91334=CARTESIAN_POINT('',(-2.93795334773476,0.00156554691536136,15.1778238829105));
#91335=CARTESIAN_POINT('',(-2.942,-3.60291088309151E-16,0.));
#91336=CARTESIAN_POINT('Ctrl Pts',(-2.93798069771247,0.00158343123380422,
15.3221761170896));
#91337=CARTESIAN_POINT('Ctrl Pts',(-2.93987699576759,0.391304358149722,
15.301159606699));
#91338=CARTESIAN_POINT('Ctrl Pts',(-2.86785867215597,0.780352682464874,
15.2801430963083));
#91339=CARTESIAN_POINT('Ctrl Pts',(-2.71863946474125,1.13711061105315,15.2591265859177));
#91340=CARTESIAN_POINT('Ctrl Pts',(-2.34218085453035,2.03715958132271,15.2061049513023));
#91341=CARTESIAN_POINT('Ctrl Pts',(-1.47435377624626,2.73168652256657,15.1530833166869));
#91342=CARTESIAN_POINT('Ctrl Pts',(-0.513683284281933,2.90174956956447,
15.1000616820716));
#91343=CARTESIAN_POINT('Ctrl Pts',(0.446987207682398,3.07181261656237,15.0470400474562));
#91344=CARTESIAN_POINT('Ctrl Pts',(1.50050111332698,2.71741176931431,14.9940184128408));
#91345=CARTESIAN_POINT('Ctrl Pts',(2.16306195169747,2.00129559889012,14.9409967782254));
#91346=CARTESIAN_POINT('Ctrl Pts',(2.82562279006796,1.28517942846593,14.88797514361));
#91347=CARTESIAN_POINT('Ctrl Pts',(3.09723056116435,0.207347934865625,14.8349535089946));
#91348=CARTESIAN_POINT('Ctrl Pts',(2.85315707378551,-0.737235236085434,
14.7819318743792));
#91349=CARTESIAN_POINT('Ctrl Pts',(2.60908358640667,-1.68181840703649,14.7289102397639));
#91350=CARTESIAN_POINT('Ctrl Pts',(1.84932884055259,-2.49315325533829,14.6758886051485));
#91351=CARTESIAN_POINT('Ctrl Pts',(0.922788726883278,-2.79865718632264,
14.6228669705331));
#91352=CARTESIAN_POINT('Ctrl Pts',(-0.00375138678601547,-3.104161117307,
14.5698453359177));
#91353=CARTESIAN_POINT('Ctrl Pts',(-1.09707686827054,-2.90383413097393,
14.5168237013023));
#91354=CARTESIAN_POINT('Ctrl Pts',(-1.85510889578549,-2.2896707330522,14.4638020666869));
#91355=CARTESIAN_POINT('Ctrl Pts',(-2.53003468473154,-1.74284065089456,
14.4165934168212));
#91356=CARTESIAN_POINT('Ctrl Pts',(-2.93915616918906,-0.86794123647866,
14.3693847669554));
#91357=CARTESIAN_POINT('Ctrl Pts',(-2.94544838002636,0.00181532900233754,
14.3221761170896));
#91358=CARTESIAN_POINT('Ctrl Pts',(-2.94538511207558,0.00185514841678406,
14.1778238829105));
#91359=CARTESIAN_POINT('Ctrl Pts',(-2.93900674246776,-0.865335636541155,
14.2248906132254));
#91360=CARTESIAN_POINT('Ctrl Pts',(-2.5326635796891,-1.73772169519058,14.2719573435402));
#91361=CARTESIAN_POINT('Ctrl Pts',(-1.86123047185566,-2.28470368230412,
14.3190240738551));
#91362=CARTESIAN_POINT('Ctrl Pts',(-1.10467917867744,-2.90102707307532,
14.3720574963508));
#91363=CARTESIAN_POINT('Ctrl Pts',(-0.0115663296148442,-3.10421332812979,
14.4250909188466));
#91364=CARTESIAN_POINT('Ctrl Pts',(0.915922577440401,-2.80091692440761,
14.4781243413424));
#91365=CARTESIAN_POINT('Ctrl Pts',(1.84341148449563,-2.49762052068544,14.5311577638381));
#91366=CARTESIAN_POINT('Ctrl Pts',(2.60527644954349,-1.6878414581866,14.5841911863339));
#91367=CARTESIAN_POINT('Ctrl Pts',(2.85151011778344,-0.743599242520295,
14.6372246088296));
#91368=CARTESIAN_POINT('Ctrl Pts',(3.09774378602338,0.200642973145996,14.6902580313254));
#91369=CARTESIAN_POINT('Ctrl Pts',(2.82834615745544,1.27934834197977,14.7432914538212));
#91370=CARTESIAN_POINT('Ctrl Pts',(2.16708083283619,1.99695028712587,14.7963248763169));
#91371=CARTESIAN_POINT('Ctrl Pts',(1.50581550821692,2.71455223227199,14.8493582988127));
#91372=CARTESIAN_POINT('Ctrl Pts',(0.452682487546306,3.07105075373044,14.9023917213084));
#91373=CARTESIAN_POINT('Ctrl Pts',(-0.508499810258251,2.9026673471594,14.9554251438042));
#91374=CARTESIAN_POINT('Ctrl Pts',(-1.46968210806282,2.73428394058836,15.0084585663));
#91375=CARTESIAN_POINT('Ctrl Pts',(-2.33891368300132,2.04101860598786,15.0614919887957));
#91376=CARTESIAN_POINT('Ctrl Pts',(-2.716862031007,1.14136343456876,15.1145254112915));
#91377=CARTESIAN_POINT('Ctrl Pts',(-2.86722980321464,0.783433191996738,
15.1356249018312));
#91378=CARTESIAN_POINT('Ctrl Pts',(-2.9398339382908,0.392834167959925,15.1567243923708));
#91379=CARTESIAN_POINT('Ctrl Pts',(-2.93795334773476,0.00156554691536136,
15.1778238829105));
#91380=CARTESIAN_POINT('Origin',(0.,0.,0.));
#91381=CARTESIAN_POINT('',(-2.93964177839095,-0.00242668875790442,16.3221761170896));
#91382=CARTESIAN_POINT('',(-2.93964149763041,-0.00243012038732958,16.1778238829105));
#91383=CARTESIAN_POINT('',(-2.942,-3.60291088309151E-16,0.));
#91384=CARTESIAN_POINT('Ctrl Pts',(-2.93964177839095,-0.00242668875790442,
16.3221761170896));
#91385=CARTESIAN_POINT('Ctrl Pts',(-2.93444969551508,0.668268699559762,
16.2859560810579));
#91386=CARTESIAN_POINT('Ctrl Pts',(-2.70680889432787,1.34215078748866,16.2497360450263));
#91387=CARTESIAN_POINT('Ctrl Pts',(-2.28633275003428,1.85922124480626,16.2135160089946));
#91388=CARTESIAN_POINT('Ctrl Pts',(-1.67080789335733,2.61614817978613,16.1604943743792));
#91389=CARTESIAN_POINT('Ctrl Pts',(-0.642049934071474,3.03703839245773,
16.1074727397639));
#91390=CARTESIAN_POINT('Ctrl Pts',(0.327513115445196,2.92860995016913,16.0544511051485));
#91391=CARTESIAN_POINT('Ctrl Pts',(1.29707616496187,2.82018150788052,16.0014294705331));
#91392=CARTESIAN_POINT('Ctrl Pts',(2.20744430470937,2.18243441063176,15.9484078359177));
#91393=CARTESIAN_POINT('Ctrl Pts',(2.64055670034754,1.30823598531302,15.8953862013023));
#91394=CARTESIAN_POINT('Ctrl Pts',(3.07366909598573,0.434037559994252,15.8423645666869));
#91395=CARTESIAN_POINT('Ctrl Pts',(3.02952574751452,-0.676612193394493,
15.7893429320716));
#91396=CARTESIAN_POINT('Ctrl Pts',(2.52839823989685,-1.51367877091038,15.7363212974562));
#91397=CARTESIAN_POINT('Ctrl Pts',(2.0272707322792,-2.35074534842623,15.6832996628408));
#91398=CARTESIAN_POINT('Ctrl Pts',(1.06915906551514,-2.91422875006925,15.6302780282254));
#91399=CARTESIAN_POINT('Ctrl Pts',(0.0940489391366825,-2.94536515190655,
15.57725639361));
#91400=CARTESIAN_POINT('Ctrl Pts',(-0.8810611872418,-2.97650155374385,15.5242347589946));
#91401=CARTESIAN_POINT('Ctrl Pts',(-1.87316977323467,-2.47529095577539,
15.4712131243793));
#91402=CARTESIAN_POINT('Ctrl Pts',(-2.42667899516226,-1.67190015714352,
15.4181914897639));
#91403=CARTESIAN_POINT('Ctrl Pts',(-2.76079037320335,-1.18695429499211,
15.3861863655391));
#91404=CARTESIAN_POINT('Ctrl Pts',(-2.93509290836528,-0.591905518505825,
15.3541812413144));
#91405=CARTESIAN_POINT('Ctrl Pts',(-2.93798069771247,0.00158343123380422,
15.3221761170896));
#91406=CARTESIAN_POINT('Ctrl Pts',(-2.93795334773476,0.00156554691536136,
15.1778238829105));
#91407=CARTESIAN_POINT('Ctrl Pts',(-2.93510708702808,-0.590616785519977,
15.2097578148666));
#91408=CARTESIAN_POINT('Ctrl Pts',(-2.76164155797149,-1.1843329378168,15.2416917468227));
#91409=CARTESIAN_POINT('Ctrl Pts',(-2.42892441791055,-1.66864494646884,
15.2736256787788));
#91410=CARTESIAN_POINT('Ctrl Pts',(-1.87637333573557,-2.47295314784975,
15.3266591012745));
#91411=CARTESIAN_POINT('Ctrl Pts',(-0.884606050312744,-2.97552454237392,
15.3796925237703));
#91412=CARTESIAN_POINT('Ctrl Pts',(0.0907509690048441,-2.94547348433537,
15.432725946266));
#91413=CARTESIAN_POINT('Ctrl Pts',(1.06610798832242,-2.91542242629683,15.4857593687618));
#91414=CARTESIAN_POINT('Ctrl Pts',(2.02505474153477,-2.35274891569562,15.5387927912575));
#91415=CARTESIAN_POINT('Ctrl Pts',(2.52704279567215,-1.51595003022512,15.5918262137533));
#91416=CARTESIAN_POINT('Ctrl Pts',(3.02903084980954,-0.679151144754612,
15.6448596362491));
#91417=CARTESIAN_POINT('Ctrl Pts',(3.07406020487193,0.431773115585177,15.6978930587448));
#91418=CARTESIAN_POINT('Ctrl Pts',(2.64144398565597,1.30645453649945,15.7509264812406));
#91419=CARTESIAN_POINT('Ctrl Pts',(2.20882776644001,2.1811359574137,15.8039599037363));
#91420=CARTESIAN_POINT('Ctrl Pts',(1.2985659729457,2.81957453890244,15.8569933262321));
#91421=CARTESIAN_POINT('Ctrl Pts',(0.328840746540987,2.92846607436597,15.9100267487279));
#91422=CARTESIAN_POINT('Ctrl Pts',(-0.640884479863755,3.0373576098295,15.9630601712236));
#91423=CARTESIAN_POINT('Ctrl Pts',(-1.67007313917891,2.6167020992678,16.0160935937194));
#91424=CARTESIAN_POINT('Ctrl Pts',(-2.2859070592039,1.85975232275157,16.0691270162151));
#91425=CARTESIAN_POINT('Ctrl Pts',(-2.70664310552638,1.34260631003568,16.1053593051136));
#91426=CARTESIAN_POINT('Ctrl Pts',(-2.93444231580981,0.668492091843893,
16.1415915940121));
#91427=CARTESIAN_POINT('Ctrl Pts',(-2.93964149763041,-0.00243012038732958,
16.1778238829105));
#91428=CARTESIAN_POINT('Origin',(0.,0.,0.));
#91429=CARTESIAN_POINT('',(-2.94674177077904,-0.000549249277246588,17.3221761170896));
#91430=CARTESIAN_POINT('',(-2.94673569549022,-0.000573513903422574,17.1778238829105));
#91431=CARTESIAN_POINT('',(-2.942,-3.60291088309151E-16,0.));
#91432=CARTESIAN_POINT('Ctrl Pts',(-2.94674177077904,-0.000549249277246588,
17.3221761170896));
#91433=CARTESIAN_POINT('Ctrl Pts',(-2.94431894621181,0.945760599581783,
17.2707525554169));
#91434=CARTESIAN_POINT('Ctrl Pts',(-2.4476760535182,1.89425494672401,17.2193289937442));
#91435=CARTESIAN_POINT('Ctrl Pts',(-1.66753585901357,2.42968006945814,17.1679054320716));
#91436=CARTESIAN_POINT('Ctrl Pts',(-0.863151506854386,2.98174442085811,
17.1148837974562));
#91437=CARTESIAN_POINT('Ctrl Pts',(0.242624240201871,3.09466699229011,17.0618621628408));
#91438=CARTESIAN_POINT('Ctrl Pts',(1.14199512784458,2.71659128486371,17.0088405282254));
#91439=CARTESIAN_POINT('Ctrl Pts',(2.04136601548729,2.33851557743732,16.95581889361));
#91440=CARTESIAN_POINT('Ctrl Pts',(2.73433204371645,1.46944159115252,16.9027972589946));
#91441=CARTESIAN_POINT('Ctrl Pts',(2.90266815249068,0.508466987654616,16.8497756243792));
#91442=CARTESIAN_POINT('Ctrl Pts',(3.07100426126492,-0.452507615843304,
16.7967539897639));
#91443=CARTESIAN_POINT('Ctrl Pts',(2.7147104505842,-1.50538283655434,16.7437323551485));
#91444=CARTESIAN_POINT('Ctrl Pts',(1.99740458146546,-2.16665549152582,16.6907107205331));
#91445=CARTESIAN_POINT('Ctrl Pts',(1.28009871234673,-2.8279281464973,16.6376890859177));
#91446=CARTESIAN_POINT('Ctrl Pts',(0.20178078478999,-3.09759823572925,16.5846674513023));
#91447=CARTESIAN_POINT('Ctrl Pts',(-0.742362174335158,-2.85182739364335,
16.5316458166869));
#91448=CARTESIAN_POINT('Ctrl Pts',(-1.68650513346031,-2.60605655155744,
16.4786241820716));
#91449=CARTESIAN_POINT('Ctrl Pts',(-2.49647312415386,-1.84484477815369,
16.4256025474562));
#91450=CARTESIAN_POINT('Ctrl Pts',(-2.80031124246659,-0.917757062807729,
16.3725809128408));
#91451=CARTESIAN_POINT('Ctrl Pts',(-2.89659205567343,-0.623979706486333,
16.3557793142571));
#91452=CARTESIAN_POINT('Ctrl Pts',(-2.94205026004507,-0.313546055856832,
16.3389777156733));
#91453=CARTESIAN_POINT('Ctrl Pts',(-2.93964177839095,-0.00242668875790442,
16.3221761170896));
#91454=CARTESIAN_POINT('Ctrl Pts',(-2.93964149763041,-0.00243012038732958,
16.1778238829105));
#91455=CARTESIAN_POINT('Ctrl Pts',(-2.94205238998694,-0.313540846863508,
16.1946250165078));
#91456=CARTESIAN_POINT('Ctrl Pts',(-2.89659907789882,-0.623965217516017,
16.2114261501051));
#91457=CARTESIAN_POINT('Ctrl Pts',(-2.80032391440682,-0.91773403538245,
16.2282272837024));
#91458=CARTESIAN_POINT('Ctrl Pts',(-2.49642766884992,-1.84502657452947,
16.2812607061982));
#91459=CARTESIAN_POINT('Ctrl Pts',(-1.68615599700128,-2.60636761035277,
16.3342941286939));
#91460=CARTESIAN_POINT('Ctrl Pts',(-0.741754713466301,-2.85199048566937,
16.3873275511897));
#91461=CARTESIAN_POINT('Ctrl Pts',(0.202646570068678,-3.09761336098597,
16.4403609736855));
#91462=CARTESIAN_POINT('Ctrl Pts',(1.28117746528998,-2.82751807579589,16.4933943961812));
#91463=CARTESIAN_POINT('Ctrl Pts',(1.99835155002923,-2.16578874034239,16.546427818677));
#91464=CARTESIAN_POINT('Ctrl Pts',(2.71552563476848,-1.50405940488887,16.5994612411727));
#91465=CARTESIAN_POINT('Ctrl Pts',(3.07134290902563,-0.450696019171894,
16.6524946636685));
#91466=CARTESIAN_POINT('Ctrl Pts',(2.90233783931567,0.51037716619625,16.7055280861643));
#91467=CARTESIAN_POINT('Ctrl Pts',(2.73333276960572,1.47145035156437,16.75856150866));
#91468=CARTESIAN_POINT('Ctrl Pts',(2.03950535592868,2.34023333658368,16.8115949311558));
#91469=CARTESIAN_POINT('Ctrl Pts',(1.13960591348502,2.71759970327641,16.8646283536515));
#91470=CARTESIAN_POINT('Ctrl Pts',(0.23970647104136,3.09496606996915,16.9176617761473));
#91471=CARTESIAN_POINT('Ctrl Pts',(-0.866265000168904,2.98091581833532,
16.9706951986431));
#91472=CARTESIAN_POINT('Ctrl Pts',(-1.67021564001697,2.4278446204691,17.0237286211388));
#91473=CARTESIAN_POINT('Ctrl Pts',(-2.44887545156518,1.89217203889788,17.0750937083961));
#91474=CARTESIAN_POINT('Ctrl Pts',(-2.94421760130182,0.944665652976608,
17.1264587956533));
#91475=CARTESIAN_POINT('Ctrl Pts',(-2.94673569549022,-0.000573513903422574,
17.1778238829105));
#91476=CARTESIAN_POINT('Origin',(0.,0.,0.));
#91477=CARTESIAN_POINT('',(-2.94129852510877,0.00270460087765087,18.3221761170896));
#91478=CARTESIAN_POINT('',(-2.94137747154633,0.00271175267126415,18.1778238829105));
#91479=CARTESIAN_POINT('',(-2.942,-3.60291088309151E-16,0.));
#91480=CARTESIAN_POINT('Ctrl Pts',(-2.94129852510877,0.00270460087765087,
18.3221761170896));
#91481=CARTESIAN_POINT('Ctrl Pts',(-2.94356667986702,0.254280750264864,
18.3085706643913));
#91482=CARTESIAN_POINT('Ctrl Pts',(-2.91398910889245,0.50533156988729,18.294965211693));
#91483=CARTESIAN_POINT('Ctrl Pts',(-2.85048850073354,0.747486714399695,
18.2813597589946));
#91484=CARTESIAN_POINT('Ctrl Pts',(-2.60302109789805,1.6911864116652,18.2283381243792));
#91485=CARTESIAN_POINT('Ctrl Pts',(-1.84035475602305,2.49978492816616,18.1753164897639));
#91486=CARTESIAN_POINT('Ctrl Pts',(-0.912722433937579,2.80195625226471,
18.1222948551485));
#91487=CARTESIAN_POINT('Ctrl Pts',(0.0149098881479351,3.10412757636327,
18.0692732205331));
#91488=CARTESIAN_POINT('Ctrl Pts',(1.10750819044393,2.89987170805936,18.0162515859177));
#91489=CARTESIAN_POINT('Ctrl Pts',(1.8633275876524,2.28298738106712,17.9632299513023));
#91490=CARTESIAN_POINT('Ctrl Pts',(2.61914698486086,1.6661030540749,17.9102083166869));
#91491=CARTESIAN_POINT('Ctrl Pts',(3.03818747698181,0.636590268394331,17.8571866820716));
#91492=CARTESIAN_POINT('Ctrl Pts',(2.9280165632392,-0.3327763309118,17.8041650474562));
#91493=CARTESIAN_POINT('Ctrl Pts',(2.8178456494966,-1.30214293021795,17.7511434128408));
#91494=CARTESIAN_POINT('Ctrl Pts',(2.17846332989048,-2.21136334314964,17.6981217782254));
#91495=CARTESIAN_POINT('Ctrl Pts',(1.30348786095498,-2.64290379646351,17.64510014361));
#91496=CARTESIAN_POINT('Ctrl Pts',(0.428512392019511,-3.07444424977737,
17.5920785089946));
#91497=CARTESIAN_POINT('Ctrl Pts',(-0.682056226245346,-3.02830474347338,
17.5390568743792));
#91498=CARTESIAN_POINT('Ctrl Pts',(-1.51822074890888,-2.52567354157278,
17.4860352397639));
#91499=CARTESIAN_POINT('Ctrl Pts',(-2.35438527157246,-2.02304233967215,
17.4330136051485));
#91500=CARTESIAN_POINT('Ctrl Pts',(-2.91614569863472,-1.06391944217489,
17.3799919705331));
#91501=CARTESIAN_POINT('Ctrl Pts',(-2.94552943353478,-0.0887549277422849,
17.3269703359177));
#91502=CARTESIAN_POINT('Ctrl Pts',(-2.94641505978979,-0.0593634531772387,
17.325372262975));
#91503=CARTESIAN_POINT('Ctrl Pts',(-2.94681706409323,-0.0299574060769884,
17.3237741900323));
#91504=CARTESIAN_POINT('Ctrl Pts',(-2.94674177077904,-0.000549249277246588,
17.3221761170896));
#91505=CARTESIAN_POINT('Ctrl Pts',(-2.94673569549022,-0.000573513903422574,
17.1778238829105));
#91506=CARTESIAN_POINT('Ctrl Pts',(-2.94681748305241,-0.0312748305982578,
17.179492218149));
#91507=CARTESIAN_POINT('Ctrl Pts',(-2.94637936742245,-0.0619737554974743,
17.1811605533876));
#91508=CARTESIAN_POINT('Ctrl Pts',(-2.94541416994405,-0.092656099588213,
17.1828288886261));
#91509=CARTESIAN_POINT('Ctrl Pts',(-2.91473225153718,-1.06799347768063,
17.2358623111219));
#91510=CARTESIAN_POINT('Ctrl Pts',(-2.35143860623763,-2.02657608976683,
17.2888957336176));
#91511=CARTESIAN_POINT('Ctrl Pts',(-1.51431520698315,-2.52802279246008,
17.3419291561134));
#91512=CARTESIAN_POINT('Ctrl Pts',(-0.677191807728671,-3.02946949515333,
17.3949625786091));
#91513=CARTESIAN_POINT('Ctrl Pts',(0.433761345480731,-3.07378028845364,
17.4479960011049));
#91514=CARTESIAN_POINT('Ctrl Pts',(1.30816276471605,-2.64059841064645,17.5010294236007));
#91515=CARTESIAN_POINT('Ctrl Pts',(2.18256418395138,-2.20741653283925,17.5540628460964));
#91516=CARTESIAN_POINT('Ctrl Pts',(2.82041386921262,-1.29674198392452,17.6070962685922));
#91517=CARTESIAN_POINT('Ctrl Pts',(2.92867815792071,-0.326946528680541,
17.6601296910879));
#91518=CARTESIAN_POINT('Ctrl Pts',(3.03694244662878,0.642848926563412,17.7131631135837));
#91519=CARTESIAN_POINT('Ctrl Pts',(2.61562133878374,1.67176528813662,17.7661965360794));
#91520=CARTESIAN_POINT('Ctrl Pts',(1.85827339560542,2.28710947977642,17.8192299585752));
#91521=CARTESIAN_POINT('Ctrl Pts',(1.10092545242709,2.90245367141623,17.872263381071));
#91522=CARTESIAN_POINT('Ctrl Pts',(0.00755067391547432,3.10422569312265,
17.9252968035667));
#91523=CARTESIAN_POINT('Ctrl Pts',(-0.919545109383185,2.79972973286843,
17.9783302260625));
#91524=CARTESIAN_POINT('Ctrl Pts',(-1.84664089268186,2.49523377261421,18.0313636485583));
#91525=CARTESIAN_POINT('Ctrl Pts',(-2.60745768076757,1.68446983039934,18.084397071054));
#91526=CARTESIAN_POINT('Ctrl Pts',(-2.85246966040257,0.739909874093412,
18.1374304935498));
#91527=CARTESIAN_POINT('Ctrl Pts',(-2.91467486249146,0.500098975644197,
18.15089495667));
#91528=CARTESIAN_POINT('Ctrl Pts',(-2.94363216926481,0.251663815076334,
18.1643594197903));
#91529=CARTESIAN_POINT('Ctrl Pts',(-2.94137747154633,0.00271175267126415,
18.1778238829105));
#91530=CARTESIAN_POINT('Origin',(0.,0.,0.));
#91531=CARTESIAN_POINT('',(-2.9372855915547,-0.000697940546887099,19.3221761170896));
#91532=CARTESIAN_POINT('',(-2.93725371205965,-0.00063370482881248,19.1778238829105));
#91533=CARTESIAN_POINT('',(-2.942,-3.60291088309151E-16,0.));
#91534=CARTESIAN_POINT('Ctrl Pts',(-2.9372855915547,-0.000697940546887099,
19.3221761170896));
#91535=CARTESIAN_POINT('Ctrl Pts',(-2.93615528736924,0.533838969154223,
19.2933671387503));
#91536=CARTESIAN_POINT('Ctrl Pts',(-2.7968583901853,1.06892457674313,19.2645581604109));
#91537=CARTESIAN_POINT('Ctrl Pts',(-2.5229406841141,1.52275782232767,19.2357491820716));
#91538=CARTESIAN_POINT('Ctrl Pts',(-2.01880741166991,2.35801758892721,19.1827275474562));
#91539=CARTESIAN_POINT('Ctrl Pts',(-1.0586763818656,2.91805322665358,19.1297059128408));
#91540=CARTESIAN_POINT('Ctrl Pts',(-0.0834606296271075,2.94568419969291,
19.0766842782254));
#91541=CARTESIAN_POINT('Ctrl Pts',(0.891755122611403,2.97331517273224,19.02366264361));
#91542=CARTESIAN_POINT('Ctrl Pts',(1.88205559728409,2.46854148108454,18.9706410089946));
#91543=CARTESIAN_POINT('Ctrl Pts',(2.43267329472432,1.66316617394455,18.9176193743793));
#91544=CARTESIAN_POINT('Ctrl Pts',(2.98329099216454,0.857790866804561,18.8645977397639));
#91545=CARTESIAN_POINT('Ctrl Pts',(3.09422591237229,-0.248186055827714,
18.8115761051485));
#91546=CARTESIAN_POINT('Ctrl Pts',(2.71453432909591,-1.14687595544508,18.7585544705331));
#91547=CARTESIAN_POINT('Ctrl Pts',(2.33484274581953,-2.04556585506245,18.7055328359177));
#91548=CARTESIAN_POINT('Ctrl Pts',(1.46452465905902,-2.73696873166493,18.6525112013023));
#91549=CARTESIAN_POINT('Ctrl Pts',(0.503249048435527,-2.90357735840927,
18.5994895666869));
#91550=CARTESIAN_POINT('Ctrl Pts',(-0.458026562188004,-3.07018598515363,
18.5464679320716));
#91551=CARTESIAN_POINT('Ctrl Pts',(-1.5102596966745,-2.71200036203983,18.4934462974562));
#91552=CARTESIAN_POINT('Ctrl Pts',(-2.17024203201977,-1.99350711146786,
18.4404246628408));
#91553=CARTESIAN_POINT('Ctrl Pts',(-2.66087163973964,-1.45938060110743,
18.4010084809237));
#91554=CARTESIAN_POINT('Ctrl Pts',(-2.93472748314863,-0.726133423854732,
18.3615922990067));
#91555=CARTESIAN_POINT('Ctrl Pts',(-2.94129852510877,0.00270460087765087,
18.3221761170896));
#91556=CARTESIAN_POINT('Ctrl Pts',(-2.94137747154633,0.00271175267126415,
18.1778238829105));
#91557=CARTESIAN_POINT('Ctrl Pts',(-2.93475143368432,-0.728901082967289,
18.217392842286));
#91558=CARTESIAN_POINT('Ctrl Pts',(-2.65856701665389,-1.46497807346214,
18.2569618016615));
#91559=CARTESIAN_POINT('Ctrl Pts',(-2.16449574177378,-1.99975197690645,
18.296530761037));
#91560=CARTESIAN_POINT('Ctrl Pts',(-1.50230267232571,-2.7164979012034,18.3495641835328));
#91561=CARTESIAN_POINT('Ctrl Pts',(-0.448709362245287,-3.07163377940028,
18.4025976060286));
#91562=CARTESIAN_POINT('Ctrl Pts',(0.512254308613893,-2.90200711725602,
18.4556310285243));
#91563=CARTESIAN_POINT('Ctrl Pts',(1.47321797947303,-2.73238045511176,18.5086644510201));
#91564=CARTESIAN_POINT('Ctrl Pts',(2.34155201111092,-2.03799125262641,18.5616978735158));
#91565=CARTESIAN_POINT('Ctrl Pts',(2.71833623861653,-1.13784791563819,18.6147312960116));
#91566=CARTESIAN_POINT('Ctrl Pts',(3.09512046612215,-0.23770457864997,18.6677647185074));
#91567=CARTESIAN_POINT('Ctrl Pts',(2.98035488949546,0.868192892841143,18.7207981410031));
#91568=CARTESIAN_POINT('Ctrl Pts',(2.42676380731967,1.67178563481728,18.7738315634989));
#91569=CARTESIAN_POINT('Ctrl Pts',(1.87317272514386,2.47537837679345,18.8268649859946));
#91570=CARTESIAN_POINT('Ctrl Pts',(0.880756137418969,2.97666638925464,18.8798984084904));
#91571=CARTESIAN_POINT('Ctrl Pts',(-0.094561191408211,2.94535362331546,
18.9329318309862));
#91572=CARTESIAN_POINT('Ctrl Pts',(-1.06987852023536,2.91404085737629,18.9859652534819));
#91573=CARTESIAN_POINT('Ctrl Pts',(-2.02809659016481,2.35012731303673,19.0389986759777));
#91574=CARTESIAN_POINT('Ctrl Pts',(-2.52900173162973,1.51267975021546,19.0920320984734));
#91575=CARTESIAN_POINT('Ctrl Pts',(-2.79910527450039,1.06110212610704,19.1206293599525));
#91576=CARTESIAN_POINT('Ctrl Pts',(-2.936235941417,0.529989017990088,19.1492266214315));
#91577=CARTESIAN_POINT('Ctrl Pts',(-2.93725371205965,-0.00063370482881248,
19.1778238829105));
#91578=CARTESIAN_POINT('Origin',(0.,0.,0.));
#91579=CARTESIAN_POINT('',(-2.94386718000102,-0.00244699584354052,20.3221761170896));
#91580=CARTESIAN_POINT('',(-2.94371017125697,-0.00248988210239957,20.1778238829105));
#91581=CARTESIAN_POINT('',(-2.942,-3.60291088309151E-16,0.));
#91582=CARTESIAN_POINT('Ctrl Pts',(-2.94386718000102,-0.00244699584354052,
20.3221761170896));
#91583=CARTESIAN_POINT('Ctrl Pts',(-2.93661160233715,0.809560164967209,
20.2781636131092));
#91584=CARTESIAN_POINT('Ctrl Pts',(-2.58699792073722,1.62705246749167,20.2341511091289));
#91585=CARTESIAN_POINT('Ctrl Pts',(-1.98960320148806,2.17382156159301,20.1901386051485));
#91586=CARTESIAN_POINT('Ctrl Pts',(-1.26992489054007,2.83251144525318,20.1371169705331));
#91587=CARTESIAN_POINT('Ctrl Pts',(-0.190644547079911,3.0983035635283,20.0840953359177));
#91588=CARTESIAN_POINT('Ctrl Pts',(0.752608839724244,2.84914039938139,20.0310737013023));
#91589=CARTESIAN_POINT('Ctrl Pts',(1.6958622265284,2.59997723523449,19.9780520666869));
#91590=CARTESIAN_POINT('Ctrl Pts',(2.50308865667655,1.83585878866557,19.9250304320716));
#91591=CARTESIAN_POINT('Ctrl Pts',(2.80359221040288,0.907684856536971,19.8720087974562));
#91592=CARTESIAN_POINT('Ctrl Pts',(3.10409576412921,-0.0204890755916505,
19.8189871628408));
#91593=CARTESIAN_POINT('Ctrl Pts',(2.89787644143367,-1.11271849327995,19.7659655282254));
#91594=CARTESIAN_POINT('Ctrl Pts',(2.27963463695782,-1.86742791105854,19.71294389361));
#91595=CARTESIAN_POINT('Ctrl Pts',(1.66139283248197,-2.6221373288371,19.6599222589946));
#91596=CARTESIAN_POINT('Ctrl Pts',(0.63112854622583,-3.03932674670597,19.6069006243792));
#91597=CARTESIAN_POINT('Ctrl Pts',(-0.338038471351601,-2.92741371741415,
19.5538789897639));
#91598=CARTESIAN_POINT('Ctrl Pts',(-1.30720548892903,-2.81550068812232,
19.5008573551485));
#91599=CARTESIAN_POINT('Ctrl Pts',(-2.21527523782775,-2.1744852116698,19.4478357205331));
#91600=CARTESIAN_POINT('Ctrl Pts',(-2.64524235473507,-1.29873552570718,
19.3948140859177));
#91601=CARTESIAN_POINT('Ctrl Pts',(-2.84158948901698,-0.898819033432462,
19.3706014296417));
#91602=CARTESIAN_POINT('Ctrl Pts',(-2.93823556160944,-0.449952277475836,
19.3463887733656));
#91603=CARTESIAN_POINT('Ctrl Pts',(-2.9372855915547,-0.000697940546887099,
19.3221761170896));
#91604=CARTESIAN_POINT('Ctrl Pts',(-2.93725371205965,-0.00063370482881248,
19.1778238829105));
#91605=CARTESIAN_POINT('Ctrl Pts',(-2.93812338999438,-0.454047130567155,
19.2022600439273));
#91606=CARTESIAN_POINT('Ctrl Pts',(-2.83960909846098,-0.907102497379243,
19.226696204944));
#91607=CARTESIAN_POINT('Ctrl Pts',(-2.63975173092173,-1.30987044565247,
19.2511323659607));
#91608=CARTESIAN_POINT('Ctrl Pts',(-2.20600437574835,-2.18399149739613,
19.3041657884565));
#91609=CARTESIAN_POINT('Ctrl Pts',(-1.29491745240111,-2.82125201958039,
19.3571992109522));
#91610=CARTESIAN_POINT('Ctrl Pts',(-0.325052174039479,-2.92888901623983,
19.410232633448));
#91611=CARTESIAN_POINT('Ctrl Pts',(0.6448131043221,-3.03652601289925,19.4632660559438));
#91612=CARTESIAN_POINT('Ctrl Pts',(1.67345673769806,-2.6145394840339,19.5162994784395));
#91613=CARTESIAN_POINT('Ctrl Pts',(2.2883109435186,-1.85679369103599,19.5693329009353));
#91614=CARTESIAN_POINT('Ctrl Pts',(2.90316514933918,-1.09904789803805,19.622366323431));
#91615=CARTESIAN_POINT('Ctrl Pts',(3.10422992760428,-0.00554284090747439,
19.6753997459268));
#91616=CARTESIAN_POINT('Ctrl Pts',(2.79913438004101,0.921355798685008,19.7284331684226));
#91617=CARTESIAN_POINT('Ctrl Pts',(2.49403883247774,1.8482544382775,19.7814665909183));
#91618=CARTESIAN_POINT('Ctrl Pts',(1.6827829590861,2.60854666033193,19.8345000134141));
#91619=CARTESIAN_POINT('Ctrl Pts',(0.738064725173308,2.8529476417826,19.8875334359098));
#91620=CARTESIAN_POINT('Ctrl Pts',(-0.206653508739454,3.09734862323327,
19.9405668584056));
#91621=CARTESIAN_POINT('Ctrl Pts',(-1.28483410317334,2.82585836408022,19.9936002809014));
#91622=CARTESIAN_POINT('Ctrl Pts',(-2.00115156717165,2.16320183767131,20.0466337033971));
#91623=CARTESIAN_POINT('Ctrl Pts',(-2.59180938424943,1.6167915139912,20.0903637632349));
#91624=CARTESIAN_POINT('Ctrl Pts',(-2.93642751257773,0.804417574374107,
20.1340938230727));
#91625=CARTESIAN_POINT('Ctrl Pts',(-2.94371017125697,-0.00248988210239957,
20.1778238829105));
#91626=CARTESIAN_POINT('Origin',(0.,0.,0.));
#91627=CARTESIAN_POINT('',(-2.94527945804905,0.00190826819681383,21.3221761170896));
#91628=CARTESIAN_POINT('',(-2.94544527640723,0.00182122834732236,21.1778238829105));
#91629=CARTESIAN_POINT('',(-2.942,-3.60291088309151E-16,0.));
#91630=CARTESIAN_POINT('Ctrl Pts',(-2.94527945804905,0.00190826819681383,
21.3221761170896));
#91631=CARTESIAN_POINT('Ctrl Pts',(-2.94613741111825,0.116048922849094,
21.3159817220836));
#91632=CARTESIAN_POINT('Ctrl Pts',(-2.94007944024821,0.230097659896368,
21.3097873270776));
#91633=CARTESIAN_POINT('Ctrl Pts',(-2.92680141464145,0.343299519765235,
21.3035929320716));
#91634=CARTESIAN_POINT('Ctrl Pts',(-2.81314663133309,1.31226382474057,21.2505712974562));
#91635=CARTESIAN_POINT('Ctrl Pts',(-2.17050006882104,2.21917997610633,21.1975496628408));
#91636=CARTESIAN_POINT('Ctrl Pts',(-1.29397899492201,2.64757236760752,21.1445280282254));
#91637=CARTESIAN_POINT('Ctrl Pts',(-0.417457921022976,3.0759647591087,21.09150639361));
#91638=CARTESIAN_POINT('Ctrl Pts',(0.692937664263023,3.02583339074529,21.0384847589946));
#91639=CARTESIAN_POINT('Ctrl Pts',(1.52728997650969,2.52019967634933,20.9854631243793));
#91640=CARTESIAN_POINT('Ctrl Pts',(2.36164228875633,2.01456596195338,20.9324414897639));
#91641=CARTESIAN_POINT('Ctrl Pts',(2.91995132796366,1.05342990152483,20.8794198551485));
#91642=CARTESIAN_POINT('Ctrl Pts',(2.945829449881,0.078166061894146,20.8263982205331));
#91643=CARTESIAN_POINT('Ctrl Pts',(2.97170757179833,-0.897097777736566,
20.7733765859177));
#91644=CARTESIAN_POINT('Ctrl Pts',(2.46515477642569,-1.88648939656947,20.7203549513023));
#91645=CARTESIAN_POINT('Ctrl Pts',(1.65879111605267,-2.43565866129123,20.6673333166869));
#91646=CARTESIAN_POINT('Ctrl Pts',(0.852427455679624,-2.984827926013,20.6143116820716));
#91647=CARTESIAN_POINT('Ctrl Pts',(-0.253747069693798,-3.09377483662359,
20.5612900474562));
#91648=CARTESIAN_POINT('Ctrl Pts',(-1.15175307808728,-2.71246860408277,
20.5082684128408));
#91649=CARTESIAN_POINT('Ctrl Pts',(-2.04975908648074,-2.33116237154196,
20.4552467782254));
#91650=CARTESIAN_POINT('Ctrl Pts',(-2.73959657789424,-1.45960299584977,
20.40222514361));
#91651=CARTESIAN_POINT('Ctrl Pts',(-2.90447718438307,-0.498029483481065,
20.3492035089946));
#91652=CARTESIAN_POINT('Ctrl Pts',(-2.93249274697017,-0.334644452994275,
20.3401943783596));
#91653=CARTESIAN_POINT('Ctrl Pts',(-2.94535235900914,-0.168660638029602,
20.3311852477246));
#91654=CARTESIAN_POINT('Ctrl Pts',(-2.94386718000102,-0.00244699584354052,
20.3221761170896));
#91655=CARTESIAN_POINT('Ctrl Pts',(-2.94371017125697,-0.00248988210239957,
20.1778238829105));
#91656=CARTESIAN_POINT('Ctrl Pts',(-2.94525952232254,-0.174155613337497,
20.1871272455685));
#91657=CARTESIAN_POINT('Ctrl Pts',(-2.93154088692244,-0.345573928578387,
20.1964306082264));
#91658=CARTESIAN_POINT('Ctrl Pts',(-2.9016751811188,-0.514131236725823,
20.2057339708844));
#91659=CARTESIAN_POINT('Ctrl Pts',(-2.73142699750492,-1.47498499104929,
20.2587673933802));
#91660=CARTESIAN_POINT('Ctrl Pts',(-2.03647629671438,-2.34286970603145,
20.3118008158759));
#91661=CARTESIAN_POINT('Ctrl Pts',(-1.13608944176364,-2.71907163671928,
20.3648342383717));
#91662=CARTESIAN_POINT('Ctrl Pts',(-0.235702586812923,-3.0952735674071,
20.4178676608674));
#91663=CARTESIAN_POINT('Ctrl Pts',(0.870120422298012,-2.97979271380062,
20.4709010833632));
#91664=CARTESIAN_POINT('Ctrl Pts',(1.67335493021286,-2.42568197891447,20.523934505859));
#91665=CARTESIAN_POINT('Ctrl Pts',(2.47658943812775,-1.87157124402828,20.5769679283547));
#91666=CARTESIAN_POINT('Ctrl Pts',(2.97723544484651,-0.878830627862415,
20.6300013508505));
#91667=CARTESIAN_POINT('Ctrl Pts',(2.94529184447496,0.0964662436678312,
20.6830347733462));
#91668=CARTESIAN_POINT('Ctrl Pts',(2.9133482441034,1.07176311519802,20.736068195842));
#91669=CARTESIAN_POINT('Ctrl Pts',(2.34881503664154,2.02961624209257,20.7891016183377));
#91670=CARTESIAN_POINT('Ctrl Pts',(1.51104366060626,2.52997961277156,20.8421350408335));
#91671=CARTESIAN_POINT('Ctrl Pts',(0.67327228457098,3.03034298345054,20.8951684633293));
#91672=CARTESIAN_POINT('Ctrl Pts',(-0.437737260037742,3.07321659791399,
20.948201885825));
#91673=CARTESIAN_POINT('Ctrl Pts',(-1.31157757859425,2.63890394683606,21.0012353083208));
#91674=CARTESIAN_POINT('Ctrl Pts',(-2.18541789715079,2.20459129575811,21.0542687308166));
#91675=CARTESIAN_POINT('Ctrl Pts',(-2.82208898965512,1.29309237913876,21.1073021533123));
#91676=CARTESIAN_POINT('Ctrl Pts',(-2.92909864923512,0.323157683410274,
21.1603355758081));
#91677=CARTESIAN_POINT('Ctrl Pts',(-2.94086115485009,0.216542426904973,
21.1661650115089));
#91678=CARTESIAN_POINT('Ctrl Pts',(-2.94622407160623,0.109221125107908,
21.1719944472097));
#91679=CARTESIAN_POINT('Ctrl Pts',(-2.94544527640723,0.00182122834732236,
21.1778238829105));
#91680=CARTESIAN_POINT('Origin',(0.,0.,0.));
#91681=CARTESIAN_POINT('',(-2.93786968250863,0.00148626117932052,22.3221761170896));
#91682=CARTESIAN_POINT('',(-2.93799456442315,0.00160006380599582,22.1778238829105));
#91683=CARTESIAN_POINT('',(-2.942,-3.60291088309151E-16,0.));
#91684=CARTESIAN_POINT('Ctrl Pts',(-2.93786968250863,0.00148626117932052,
22.3221761170896));
#91685=CARTESIAN_POINT('Ctrl Pts',(-2.93967789259735,0.398317401179163,
22.3007781964426));
#91686=CARTESIAN_POINT('Ctrl Pts',(-2.86492885207122,0.794495709771153,
22.2793802757955));
#91687=CARTESIAN_POINT('Ctrl Pts',(-2.71039411649762,1.15662648001562,22.2579823551485));
#91688=CARTESIAN_POINT('Ctrl Pts',(-2.32747446649407,2.05394569619588,22.2049607205331));
#91689=CARTESIAN_POINT('Ctrl Pts',(-1.45467661742421,2.74221557391513,22.1519390859177));
#91690=CARTESIAN_POINT('Ctrl Pts',(-0.492808309653051,2.90536762750519,
22.0989174513023));
#91691=CARTESIAN_POINT('Ctrl Pts',(0.469059998118109,3.06851968109525,22.045895816687));
#91692=CARTESIAN_POINT('Ctrl Pts',(1.51999876459057,2.70655391055611,21.9928741820716));
#91693=CARTESIAN_POINT('Ctrl Pts',(2.17739406868201,1.98569286413751,21.9398525474562));
#91694=CARTESIAN_POINT('Ctrl Pts',(2.83478937277347,1.26483181771889,21.8868309128408));
#91695=CARTESIAN_POINT('Ctrl Pts',(3.0986412144839,0.185075495420776,21.8338092782254));
#91696=CARTESIAN_POINT('Ctrl Pts',(2.84778309394186,-0.757728533762051,
21.78078764361));
#91697=CARTESIAN_POINT('Ctrl Pts',(2.59692497339982,-1.70053256294485,21.7277660089946));
#91698=CARTESIAN_POINT('Ctrl Pts',(1.83135689060535,-2.50638429901237,21.6747443743793));
#91699=CARTESIAN_POINT('Ctrl Pts',(0.90264434687977,-2.80521911159614,21.6217227397639));
#91700=CARTESIAN_POINT('Ctrl Pts',(-0.0260681968458087,-3.1040539241799,
21.5687011051485));
#91701=CARTESIAN_POINT('Ctrl Pts',(-1.11792520150249,-2.89587181327991,
21.5156794705331));
#91702=CARTESIAN_POINT('Ctrl Pts',(-1.87152220177849,-2.27627452853746,
21.4626578359177));
#91703=CARTESIAN_POINT('Ctrl Pts',(-2.53707820654536,-1.72906336229535,
21.4158305963083));
#91704=CARTESIAN_POINT('Ctrl Pts',(-2.93879366340633,-0.860951103764374,
21.369003356699));
#91705=CARTESIAN_POINT('Ctrl Pts',(-2.94527945804905,0.00190826819681383,
21.3221761170896));
#91706=CARTESIAN_POINT('Ctrl Pts',(-2.94544527640723,0.00182122834732236,
21.1778238829105));
#91707=CARTESIAN_POINT('Ctrl Pts',(-2.93913896475443,-0.867851853003506,
21.2250278697055));
#91708=CARTESIAN_POINT('Ctrl Pts',(-2.53012139393514,-1.74267839595515,
21.2722318565004));
#91709=CARTESIAN_POINT('Ctrl Pts',(-1.85531320966215,-2.28951144992795,
21.3194358432953));
#91710=CARTESIAN_POINT('Ctrl Pts',(-1.09716988385351,-2.90387541270011,
21.3724692657911));
#91711=CARTESIAN_POINT('Ctrl Pts',(-0.00353500558054817,-3.10423286340682,
21.4255026882869));
#91712=CARTESIAN_POINT('Ctrl Pts',(0.923166102530367,-2.79853785617364,
21.4785361107826));
#91713=CARTESIAN_POINT('Ctrl Pts',(1.84986721064131,-2.49284284894045,21.5315695332784));
#91714=CARTESIAN_POINT('Ctrl Pts',(2.60963454859019,-1.68109538376735,21.5846029557741));
#91715=CARTESIAN_POINT('Ctrl Pts',(2.85342442960947,-0.736219267478046,
21.6376363782699));
#91716=CARTESIAN_POINT('Ctrl Pts',(3.09721431062875,0.208656848811227,21.6906698007657));
#91717=CARTESIAN_POINT('Ctrl Pts',(2.82502673471846,1.28666161621668,21.7437032232614));
#91718=CARTESIAN_POINT('Ctrl Pts',(2.16190702857628,2.00255032023931,21.7967366457572));
#91719=CARTESIAN_POINT('Ctrl Pts',(1.49878732243405,2.71843902426198,21.849770068253));
#91720=CARTESIAN_POINT('Ctrl Pts',(0.444735486059899,3.07221166490178,21.9028034907487));
#91721=CARTESIAN_POINT('Ctrl Pts',(-0.51600794974714,2.90134203104285,21.9558369132445));
#91722=CARTESIAN_POINT('Ctrl Pts',(-1.4767513855541,2.73047239718393,22.0088703357402));
#91723=CARTESIAN_POINT('Ctrl Pts',(-2.34418642079396,2.03496048882639,22.061903758236));
#91724=CARTESIAN_POINT('Ctrl Pts',(-2.71980589727694,1.13433049259714,22.1149371807317));
#91725=CARTESIAN_POINT('Ctrl Pts',(-2.86827497607355,0.778343345368319,
22.1358994147913));
#91726=CARTESIAN_POINT('Ctrl Pts',(-2.93990569515241,0.390309758900483,
22.1568616488509));
#91727=CARTESIAN_POINT('Ctrl Pts',(-2.93799456442315,0.00160006380599582,
22.1778238829105));
#91728=CARTESIAN_POINT('Origin',(0.,0.,0.));
#91729=CARTESIAN_POINT('',(-2.93982555808591,-0.00247806991730104,23.3221761170896));
#91730=CARTESIAN_POINT('',(-2.93957643049581,-0.00241049697055628,23.1778238829105));
#91731=CARTESIAN_POINT('',(-2.942,-3.60291088309151E-16,0.));
#91732=CARTESIAN_POINT('Ctrl Pts',(-2.93982555808591,-0.00247806991730104,
23.3221761170896));
#91733=CARTESIAN_POINT('Ctrl Pts',(-2.9344443745828,0.675173062708582,23.2855746708015));
#91734=CARTESIAN_POINT('Ctrl Pts',(-2.70155654492499,1.35616333535824,23.2489732245135));
#91735=CARTESIAN_POINT('Ctrl Pts',(-2.27290706666078,1.87561044658578,23.2123717782254));
#91736=CARTESIAN_POINT('Ctrl Pts',(-1.65195630324756,2.62809259488021,23.15935014361));
#91737=CARTESIAN_POINT('Ctrl Pts',(-0.620199002997637,3.04157582706469,
23.1063285089946));
#91738=CARTESIAN_POINT('Ctrl Pts',(0.348559459157085,2.92617965689914,23.0533068743793));
#91739=CARTESIAN_POINT('Ctrl Pts',(1.31731792131181,2.81078348673359,23.0002852397639));
#91740=CARTESIAN_POINT('Ctrl Pts',(2.22307754537133,2.16650791421801,22.9472636051485));
#91741=CARTESIAN_POINT('Ctrl Pts',(2.64989382755387,1.28921828396519,22.8942419705331));
#91742=CARTESIAN_POINT('Ctrl Pts',(3.07671010973638,0.411928653712412,22.8412203359177));
#91743=CARTESIAN_POINT('Ctrl Pts',(3.02458305004197,-0.698375034277577,
22.7881987013023));
#91744=CARTESIAN_POINT('Ctrl Pts',(2.5174505271332,-1.53181719681397,22.7351770666869));
#91745=CARTESIAN_POINT('Ctrl Pts',(2.0103180042244,-2.36525935935041,22.6821554320716));
#91746=CARTESIAN_POINT('Ctrl Pts',(1.04818001810119,-2.92183999643322,22.6291337974562));
#91747=CARTESIAN_POINT('Ctrl Pts',(0.0728712416473015,-2.94596518362981,
22.5761121628408));
#91748=CARTESIAN_POINT('Ctrl Pts',(-0.902437534806564,-2.9700903708264,
22.5230905282254));
#91749=CARTESIAN_POINT('Ctrl Pts',(-1.89091710159111,-2.4617601081368,22.47006889361));
#91750=CARTESIAN_POINT('Ctrl Pts',(-2.43863615951476,-1.65441069947136,
22.4170472589946));
#91751=CARTESIAN_POINT('Ctrl Pts',(-2.76531244832466,-1.17288298050626,
22.3854235450263));
#91752=CARTESIAN_POINT('Ctrl Pts',(-2.93519735188436,-0.584985418573476,
22.3537998310579));
#91753=CARTESIAN_POINT('Ctrl Pts',(-2.93786968250863,0.00148626117932052,
22.3221761170896));
#91754=CARTESIAN_POINT('Ctrl Pts',(-2.93799456442315,0.00160006380599582,
22.1778238829105));
#91755=CARTESIAN_POINT('Ctrl Pts',(-2.93507062828303,-0.593106676081661,
22.2098950713467));
#91756=CARTESIAN_POINT('Ctrl Pts',(-2.76000362972722,-1.18939601703009,
22.2419662597829));
#91757=CARTESIAN_POINT('Ctrl Pts',(-2.42459913570607,-1.67492352554719,
22.274037448219));
#91758=CARTESIAN_POINT('Ctrl Pts',(-1.86996897992613,-2.47779946336128,
22.3270708707148));
#91759=CARTESIAN_POINT('Ctrl Pts',(-0.87690475064014,-2.97780325488844,
22.3801042932106));
#91760=CARTESIAN_POINT('Ctrl Pts',(0.0983712555699952,-2.94522883344837,
22.4331377157063));
#91761=CARTESIAN_POINT('Ctrl Pts',(1.0736472617801,-2.91265441200831,22.4861711382021));
#91762=CARTESIAN_POINT('Ctrl Pts',(2.03113504491436,-2.34750177760105,22.5392045606978));
#91763=CARTESIAN_POINT('Ctrl Pts',(2.53095643547645,-1.50940693884003,22.5922379831936));
#91764=CARTESIAN_POINT('Ctrl Pts',(3.03077782603854,-0.671312100078998,
22.6452714056893));
#91765=CARTESIAN_POINT('Ctrl Pts',(3.07293282402846,0.439724943035805,22.6983048281851));
#91766=CARTESIAN_POINT('Ctrl Pts',(2.63805505874409,1.31328416282721,22.7513382506809));
#91767=CARTESIAN_POINT('Ctrl Pts',(2.20317729345972,2.18684338261864,22.8043716731766));
#91768=CARTESIAN_POINT('Ctrl Pts',(1.29126676490102,2.82292477908666,22.8574050956724));
#91769=CARTESIAN_POINT('Ctrl Pts',(0.321263057585504,2.92930705681888,22.9104385181681));
#91770=CARTESIAN_POINT('Ctrl Pts',(-0.648740649729987,3.0356893345511,22.9634719406639));
#91771=CARTESIAN_POINT('Ctrl Pts',(-1.6768375358023,2.61237249354755,23.0165053631597));
#91772=CARTESIAN_POINT('Ctrl Pts',(-2.29071099850207,1.85383195210346,23.0695387856554));
#91773=CARTESIAN_POINT('Ctrl Pts',(-2.70851889198083,1.33756232164056,23.1056338180738));
#91774=CARTESIAN_POINT('Ctrl Pts',(-2.93444656187858,0.666007415259461,
23.1417288504922));
#91775=CARTESIAN_POINT('Ctrl Pts',(-2.93957643049581,-0.00241049697055628,
23.1778238829105));
#91776=CARTESIAN_POINT('Origin',(0.,0.,0.));
#91777=CARTESIAN_POINT('',(-2.94679320362931,-0.000419630752076516,24.3221761170896));
#91778=CARTESIAN_POINT('',(-2.94671321490455,-0.00061974086392264,24.1778238829105));
#91779=CARTESIAN_POINT('',(-2.942,-3.60291088309151E-16,0.));
#91780=CARTESIAN_POINT('Ctrl Pts',(-2.94679320362931,-0.000419630752076516,
24.3221761170896));
#91781=CARTESIAN_POINT('Ctrl Pts',(-2.94489621355737,0.952864368939043,
24.2703711451605));
#91782=CARTESIAN_POINT('Ctrl Pts',(-2.43980905770987,1.90787363364129,24.2185661732314));
#91783=CARTESIAN_POINT('Ctrl Pts',(-1.65002493835147,2.44160577977619,24.1667612013023));
#91784=CARTESIAN_POINT('Ctrl Pts',(-0.841692389518663,2.98787286150696,
24.1137395666869));
#91785=CARTESIAN_POINT('Ctrl Pts',(0.264866620290473,3.09284270349453,24.0607179320716));
#91786=CARTESIAN_POINT('Ctrl Pts',(1.16149614548691,2.70831087304196,24.0076962974562));
#91787=CARTESIAN_POINT('Ctrl Pts',(2.05812567068335,2.32377904258938,23.9546746628408));
#91788=CARTESIAN_POINT('Ctrl Pts',(2.74482571126712,1.44974553969667,23.9016530282254));
#91789=CARTESIAN_POINT('Ctrl Pts',(2.90624868489911,0.487585543818128,23.84863139361));
#91790=CARTESIAN_POINT('Ctrl Pts',(3.0676716585311,-0.474574452060386,23.7956097589946));
#91791=CARTESIAN_POINT('Ctrl Pts',(2.70381756521139,-1.52486094092468,23.7425881243793));
#91792=CARTESIAN_POINT('Ctrl Pts',(1.98177611204847,-2.18095954174586,23.6895664897639));
#91793=CARTESIAN_POINT('Ctrl Pts',(1.25973465888552,-2.83705814256706,23.6365448551485));
#91794=CARTESIAN_POINT('Ctrl Pts',(0.179505845879314,-3.09896885534504,
23.5835232205331));
#91795=CARTESIAN_POINT('Ctrl Pts',(-0.762845779973811,-2.84641658879975,
23.5305015859177));
#91796=CARTESIAN_POINT('Ctrl Pts',(-1.70519740582696,-2.59386432225444,
23.4774799513023));
#91797=CARTESIAN_POINT('Ctrl Pts',(-2.50967184452705,-1.82684907638581,
23.4244583166869));
#91798=CARTESIAN_POINT('Ctrl Pts',(-2.8068369505888,-0.897600921249319,
23.3714366820716));
#91799=CARTESIAN_POINT('Ctrl Pts',(-2.89886555440755,-0.609823491887907,
23.3550164937442));
#91800=CARTESIAN_POINT('Ctrl Pts',(-2.94223967161163,-0.306486800347378,
23.3385963054169));
#91801=CARTESIAN_POINT('Ctrl Pts',(-2.93982555808591,-0.00247806991730104,
23.3221761170896));
#91802=CARTESIAN_POINT('Ctrl Pts',(-2.93957643049581,-0.00241049697055628,
23.1778238829105));
#91803=CARTESIAN_POINT('Ctrl Pts',(-2.94198373448926,-0.316080344966286,
23.1947622729879));
#91804=CARTESIAN_POINT('Ctrl Pts',(-2.89576777188966,-0.629059375834195,
23.2117006630653));
#91805=CARTESIAN_POINT('Ctrl Pts',(-2.79794016151588,-0.924976020161902,
23.2286390531427));
#91806=CARTESIAN_POINT('Ctrl Pts',(-2.4916458225027,-1.85147920909858,23.2816724756384));
#91807=CARTESIAN_POINT('Ctrl Pts',(-1.67940710514908,-2.61072134508725,
23.3347058981342));
#91808=CARTESIAN_POINT('Ctrl Pts',(-0.734373501779644,-2.85390002368373,
23.38773932063));
#91809=CARTESIAN_POINT('Ctrl Pts',(0.210660101589743,-3.09707870228019,
23.4407727431257));
#91810=CARTESIAN_POINT('Ctrl Pts',(1.28848859097492,-2.8241939234845,23.4938061656215));
#91811=CARTESIAN_POINT('Ctrl Pts',(2.00394823552418,-2.16061131503044,23.5468395881172));
#91812=CARTESIAN_POINT('Ctrl Pts',(2.71940788007347,-1.49702870657636,23.599873010613));
#91813=CARTESIAN_POINT('Ctrl Pts',(3.07249867978681,-0.442748268463822,
23.6529064331088));
#91814=CARTESIAN_POINT('Ctrl Pts',(2.90100766716762,0.517884446892132,23.7059398556045));
#91815=CARTESIAN_POINT('Ctrl Pts',(2.72951665454842,1.47851716224811,23.7589732781003));
#91816=CARTESIAN_POINT('Ctrl Pts',(2.03344382959672,2.34550215484754,23.812006700596));
#91817=CARTESIAN_POINT('Ctrl Pts',(1.13257106887453,2.72053901998234,23.8650401230918));
#91818=CARTESIAN_POINT('Ctrl Pts',(0.231698308152341,3.09557588511714,23.9180735455876));
#91819=CARTESIAN_POINT('Ctrl Pts',(-0.873974388340304,2.97866462278731,
23.9711069680833));
#91820=CARTESIAN_POINT('Ctrl Pts',(-1.67649142016412,2.42351527814746,24.0241403905791));
#91821=CARTESIAN_POINT('Ctrl Pts',(-2.4516857177852,1.88726671365922,24.0753682213562));
#91822=CARTESIAN_POINT('Ctrl Pts',(-2.94401560406121,0.942112851897334,
24.1265960521334));
#91823=CARTESIAN_POINT('Ctrl Pts',(-2.94671321490455,-0.00061974086392264,
24.1778238829105));
#91824=CARTESIAN_POINT('Origin',(0.,0.,0.));
#91825=CARTESIAN_POINT('',(-2.94108940257125,0.00269036361580877,25.3221761170896));
#91826=CARTESIAN_POINT('',(-2.94145356055697,0.00271483987803603,25.1778238829105));
#91827=CARTESIAN_POINT('',(-2.942,-3.60291088309151E-16,0.));
#91828=CARTESIAN_POINT('Ctrl Pts',(-2.94108940257125,0.00269036361580877,
25.3221761170896));
#91829=CARTESIAN_POINT('Ctrl Pts',(-2.94339537070129,0.261365886758737,
25.3081892541349));
#91830=CARTESIAN_POINT('Ctrl Pts',(-2.91210970553165,0.519492689068858,
25.2942023911801));
#91831=CARTESIAN_POINT('Ctrl Pts',(-2.84504088836942,0.767960561828773,
25.2802155282254));
#91832=CARTESIAN_POINT('Ctrl Pts',(-2.59079529168549,1.70985674010536,25.22719389361));
#91833=CARTESIAN_POINT('Ctrl Pts',(-1.82233536056913,2.51295128260037,25.1741722589946));
#91834=CARTESIAN_POINT('Ctrl Pts',(-0.892554595938133,2.80844572215451,
25.1211506243792));
#91835=CARTESIAN_POINT('Ctrl Pts',(0.037226168692838,3.10394016170864,25.0681289897638));
#91836=CARTESIAN_POINT('Ctrl Pts',(1.12832776683841,2.89183449832193,25.0151073551485));
#91837=CARTESIAN_POINT('Ctrl Pts',(1.87969263227361,2.26953226220615,24.9620857205331));
#91838=CARTESIAN_POINT('Ctrl Pts',(2.63105749770886,1.64723002609033,24.9090640859177));
#91839=CARTESIAN_POINT('Ctrl Pts',(3.04268563043366,0.614731217245394,24.8560424513023));
#91840=CARTESIAN_POINT('Ctrl Pts',(2.92554844619577,-0.353818272535112,
24.8030208166869));
#91841=CARTESIAN_POINT('Ctrl Pts',(2.80841126195789,-1.32236776231556,24.7499991820715));
#91842=CARTESIAN_POINT('Ctrl Pts',(2.16250876075731,-2.22696793303165,24.6969775474562));
#91843=CARTESIAN_POINT('Ctrl Pts',(1.28445340821624,-2.65220672707463,24.6439559128408));
#91844=CARTESIAN_POINT('Ctrl Pts',(0.406398055675107,-3.07744552111764,
24.5909342782254));
#91845=CARTESIAN_POINT('Ctrl Pts',(-0.703810148206556,-3.02332293848755,
24.53791264361));
#91846=CARTESIAN_POINT('Ctrl Pts',(-1.53633946861557,-2.51469324534669,
24.4848910089946));
#91847=CARTESIAN_POINT('Ctrl Pts',(-2.36886878902454,-2.00606355220585,
24.4318693743792));
#91848=CARTESIAN_POINT('Ctrl Pts',(-2.92371922596088,-1.04292674855432,
24.3788477397639));
#91849=CARTESIAN_POINT('Ctrl Pts',(-2.94609140050085,-0.067576185991548,
24.3258261051485));
#91850=CARTESIAN_POINT('Ctrl Pts',(-2.94660476434132,-0.0451952721601265,
24.3246094424622));
#91851=CARTESIAN_POINT('Ctrl Pts',(-2.94683775528045,-0.0228079272548677,
24.3233927797759));
#91852=CARTESIAN_POINT('Ctrl Pts',(-2.94679320362931,-0.000419630752076516,
24.3221761170896));
#91853=CARTESIAN_POINT('Ctrl Pts',(-2.94671321490455,-0.00061974086392264,
24.1778238829105));
#91854=CARTESIAN_POINT('Ctrl Pts',(-2.94680829571755,-0.0338475808200229,
24.1796294746291));
#91855=CARTESIAN_POINT('Ctrl Pts',(-2.94629510538745,-0.0670724128288604,
24.1814350663477));
#91856=CARTESIAN_POINT('Ctrl Pts',(-2.94516459026207,-0.100276226317684,
24.1832406580664));
#91857=CARTESIAN_POINT('Ctrl Pts',(-2.91195936138129,-1.07553095919334,
24.2362740805621));
#91858=CARTESIAN_POINT('Ctrl Pts',(-2.34618753646466,-2.03265299799483,
24.2893075030579));
#91859=CARTESIAN_POINT('Ctrl Pts',(-1.50776958560142,-2.53193219933579,
24.3423409255536));
#91860=CARTESIAN_POINT('Ctrl Pts',(-0.66935163473825,-3.03121140067672,
24.3953743480494));
#91861=CARTESIAN_POINT('Ctrl Pts',(0.441712442071503,-3.07264776455723,
24.4484077705452));
#91862=CARTESIAN_POINT('Ctrl Pts',(1.31499019763738,-2.63720506700099,24.5014411930409));
#91863=CARTESIAN_POINT('Ctrl Pts',(2.18826795320328,-2.20176236944474,24.5544746155367));
#91864=CARTESIAN_POINT('Ctrl Pts',(2.82375938752531,-1.28944061045169,24.6075080380325));
#91865=CARTESIAN_POINT('Ctrl Pts',(2.92951423890392,-0.319368297357882,
24.6605414605282));
#91866=CARTESIAN_POINT('Ctrl Pts',(3.03526909028253,0.650704015735951,24.713574883024));
#91867=CARTESIAN_POINT('Ctrl Pts',(2.61128735871772,1.67852688293051,24.7666083055197));
#91868=CARTESIAN_POINT('Ctrl Pts',(1.85234991897961,2.29190958873912,24.8196417280155));
#91869=CARTESIAN_POINT('Ctrl Pts',(1.09341247924151,2.90529229454771,24.8726751505112));
#91870=CARTESIAN_POINT('Ctrl Pts',(-0.000480668669881057,3.1042348389703,
24.925708573007));
#91871=CARTESIAN_POINT('Ctrl Pts',(-0.926785550822343,2.79734129631781,
24.9787419955028));
#91872=CARTESIAN_POINT('Ctrl Pts',(-1.85309043297486,2.4904477536653,25.0317754179985));
#91873=CARTESIAN_POINT('Ctrl Pts',(-2.61180704936844,1.67771812393763,25.0848088404943));
#91874=CARTESIAN_POINT('Ctrl Pts',(-2.85437442380639,0.732527428850295,
25.13784226299));
#91875=CARTESIAN_POINT('Ctrl Pts',(-2.91533118222703,0.495002654566948,
25.1511694696302));
#91876=CARTESIAN_POINT('Ctrl Pts',(-2.94369269586688,0.249112856181335,
25.1644966762703));
#91877=CARTESIAN_POINT('Ctrl Pts',(-2.94145356055697,0.00271483987803603,
25.1778238829105));
#91878=CARTESIAN_POINT('Origin',(0.,0.,0.));
#91879=CARTESIAN_POINT('',(-2.93733956291468,-0.000810573463508324,26.3221761170896));
#91880=CARTESIAN_POINT('',(-2.93723794832128,-0.000592575232268764,26.1778238829105));
#91881=CARTESIAN_POINT('',(-2.942,-3.60291088309151E-16,0.));
#91882=CARTESIAN_POINT('Ctrl Pts',(-2.93733956291468,-0.000810573463508324,
26.3221761170896));
#91883=CARTESIAN_POINT('Ctrl Pts',(-2.93600810479843,0.540778397853635,
26.2929857284938));
#91884=CARTESIAN_POINT('Ctrl Pts',(-2.79277081125737,1.0830223511668,26.2637953398981));
#91885=CARTESIAN_POINT('Ctrl Pts',(-2.5119278398973,1.54085677730512,26.2346049513023));
#91886=CARTESIAN_POINT('Ctrl Pts',(-2.00180261964182,2.3724705661185,26.1815833166869));
#91887=CARTESIAN_POINT('Ctrl Pts',(-1.03767010985474,2.92558901047594,26.1285616820716));
#91888=CARTESIAN_POINT('Ctrl Pts',(-0.0622809120321974,2.94620810008639,
26.0755400474562));
#91889=CARTESIAN_POINT('Ctrl Pts',(0.913108285790287,2.96682718969685,26.0225184128408));
#91890=CARTESIAN_POINT('Ctrl Pts',(1.89975417164822,2.4549469245604,25.9694967782254));
#91891=CARTESIAN_POINT('Ctrl Pts',(2.44456751248201,1.64563384686137,25.91647514361));
#91892=CARTESIAN_POINT('Ctrl Pts',(2.98938085331583,0.836320769162291,25.8634535089946));
#91893=CARTESIAN_POINT('Ctrl Pts',(3.09236164912545,-0.270425121099402,
25.8104318743793));
#91894=CARTESIAN_POINT('Ctrl Pts',(2.70621888044578,-1.16636205876949,25.7574102397639));
#91895=CARTESIAN_POINT('Ctrl Pts',(2.32007611176614,-2.06229899643953,25.7043886051485));
#91896=CARTESIAN_POINT('Ctrl Pts',(1.44480977859727,-2.747426981518,25.6513669705331));
#91897=CARTESIAN_POINT('Ctrl Pts',(0.482361202848739,-2.90712035371853,
25.5983453359177));
#91898=CARTESIAN_POINT('Ctrl Pts',(-0.480087372899792,-3.06681372591906,
25.5453237013023));
#91899=CARTESIAN_POINT('Ctrl Pts',(-1.52971819122799,-2.70107248524166,
25.4923020666869));
#91900=CARTESIAN_POINT('Ctrl Pts',(-2.18451796926637,-1.97785295787391,
25.4392804320716));
#91901=CARTESIAN_POINT('Ctrl Pts',(-2.66658458234967,-1.44541541014243,
25.4002456604109));
#91902=CARTESIAN_POINT('Ctrl Pts',(-2.93465386804832,-0.719225623747977,
25.3612108887503));
#91903=CARTESIAN_POINT('Ctrl Pts',(-2.94108940257125,0.00269036361580877,
25.3221761170896));
#91904=CARTESIAN_POINT('Ctrl Pts',(-2.94145356055697,0.00271483987803603,
25.1778238829105));
#91905=CARTESIAN_POINT('Ctrl Pts',(-2.93478242591144,-0.731387443210676,
25.2175300987661));
#91906=CARTESIAN_POINT('Ctrl Pts',(-2.65648652101379,-1.47000089125401,
25.2572363146217));
#91907=CARTESIAN_POINT('Ctrl Pts',(-2.15931469757571,-2.00534531244163,
25.2969425304773));
#91908=CARTESIAN_POINT('Ctrl Pts',(-1.4952694644247,-2.72037559819935,25.3499759529731));
#91909=CARTESIAN_POINT('Ctrl Pts',(-0.440760865640405,-3.07278440926782,
25.4030093754689));
#91910=CARTESIAN_POINT('Ctrl Pts',(0.519760727376244,-2.90067208963292,
25.4560427979646));
#91911=CARTESIAN_POINT('Ctrl Pts',(1.48028232039289,-2.72855976999802,25.5090762204604));
#91912=CARTESIAN_POINT('Ctrl Pts',(2.34681690764188,-2.03192631965965,25.5621096429561));
#91913=CARTESIAN_POINT('Ctrl Pts',(2.72127100452882,-1.1308111713318,25.6151430654519));
#91914=CARTESIAN_POINT('Ctrl Pts',(3.09572510141573,-0.229696023004005,
25.6681764879476));
#91915=CARTESIAN_POINT('Ctrl Pts',(2.97809870794077,0.875900823313237,25.7212099104434));
#91916=CARTESIAN_POINT('Ctrl Pts',(2.42243040669225,1.67805861340744,25.7742433329392));
#91917=CARTESIAN_POINT('Ctrl Pts',(1.8667621054437,2.48021640350168,25.8272767554349));
#91918=CARTESIAN_POINT('Ctrl Pts',(0.873051896421506,2.97893513737279,25.8803101779307));
#91919=CARTESIAN_POINT('Ctrl Pts',(-0.102181155114106,2.94509911494293,
25.9333436004265));
#91920=CARTESIAN_POINT('Ctrl Pts',(-1.07741420664972,2.91126309251307,25.9863770229222));
#91921=CARTESIAN_POINT('Ctrl Pts',(-2.03417010069878,2.34487231378225,26.039410445418));
#91922=CARTESIAN_POINT('Ctrl Pts',(-2.53290690394125,1.50613160157566,26.0924438679137));
#91923=CARTESIAN_POINT('Ctrl Pts',(-2.80055042467695,1.05602742690899,26.1209038729126));
#91924=CARTESIAN_POINT('Ctrl Pts',(-2.93629108483062,0.527490418271314,
26.1493638779116));
#91925=CARTESIAN_POINT('Ctrl Pts',(-2.93723794832128,-0.000592575232268764,
26.1778238829105));
#91926=CARTESIAN_POINT('Origin',(0.,0.,0.));
#91927=CARTESIAN_POINT('',(-2.94407188513322,-0.00239011867426281,27.3221761170896));
#91928=CARTESIAN_POINT('',(-2.94363499374191,-0.002507597635829,27.1778238829105));
#91929=CARTESIAN_POINT('',(-2.942,-3.60291088309151E-16,0.));
#91930=CARTESIAN_POINT('Ctrl Pts',(-2.94407188513322,-0.00239011867426281,
27.3221761170896));
#91931=CARTESIAN_POINT('Ctrl Pts',(-2.93685821302976,0.816506344639196,
27.2777822028528));
#91932=CARTESIAN_POINT('Ctrl Pts',(-2.58044453554868,1.64090832397564,27.233388288616));
#91933=CARTESIAN_POINT('Ctrl Pts',(-1.97392341428739,2.18806933974823,27.1889943743792));
#91934=CARTESIAN_POINT('Ctrl Pts',(-1.24952814906002,2.84156817968708,27.1359727397639));
#91935=CARTESIAN_POINT('Ctrl Pts',(-0.168364825121207,3.09959410258269,
27.0829511051485));
#91936=CARTESIAN_POINT('Ctrl Pts',(0.773072862803339,2.84365599709516,27.0299294705331));
#91937=CARTESIAN_POINT('Ctrl Pts',(1.71451055072783,2.58771789160765,26.9769078359177));
#91938=CARTESIAN_POINT('Ctrl Pts',(2.51622260263805,1.81781575773695,26.9238862013023));
#91939=CARTESIAN_POINT('Ctrl Pts',(2.81004542109612,0.887505387248421,26.870864566687));
#91940=CARTESIAN_POINT('Ctrl Pts',(3.1038682395542,-0.0428049832401568,
26.8178429320716));
#91941=CARTESIAN_POINT('Ctrl Pts',(2.88980182456017,-1.13352359034658,26.7648212974562));
#91942=CARTESIAN_POINT('Ctrl Pts',(2.26615012607589,-1.88376874565444,26.7117996628408));
#91943=CARTESIAN_POINT('Ctrl Pts',(1.6424984275916,-2.63401390096229,26.6587780282254));
#91944=CARTESIAN_POINT('Ctrl Pts',(0.609261445617043,-3.04378560447153,
26.60575639361));
#91945=CARTESIAN_POINT('Ctrl Pts',(-0.359075942910748,-2.92490778457048,
26.5527347589946));
#91946=CARTESIAN_POINT('Ctrl Pts',(-1.32741333143854,-2.80602996466943,
26.4997131243793));
#91947=CARTESIAN_POINT('Ctrl Pts',(-2.23085112651959,-2.1585026213581,26.4466914897639));
#91948=CARTESIAN_POINT('Ctrl Pts',(-2.65451105869814,-1.27968438306777,
26.3936698551485));
#91949=CARTESIAN_POINT('Ctrl Pts',(-2.84493038744279,-0.884688381998503,
26.3698386091289));
#91950=CARTESIAN_POINT('Ctrl Pts',(-2.93842657502584,-0.442967757313165,
26.3460073631092));
#91951=CARTESIAN_POINT('Ctrl Pts',(-2.93733956291468,-0.000810573463508324,
26.3221761170896));
#91952=CARTESIAN_POINT('Ctrl Pts',(-2.93723794832128,-0.000592575232268764,
26.1778238829105));
#91953=CARTESIAN_POINT('Ctrl Pts',(-2.93805550516533,-0.456558899652427,
26.2023973004073));
#91954=CARTESIAN_POINT('Ctrl Pts',(-2.83838115668472,-0.91218674524788,
26.2269707179042));
#91955=CARTESIAN_POINT('Ctrl Pts',(-2.63635397196237,-1.31669568231095,
26.251544135401));
#91956=CARTESIAN_POINT('Ctrl Pts',(-2.20034652430512,-2.18969160830876,
26.3045775578967));
#91957=CARTESIAN_POINT('Ctrl Pts',(-1.2876139165547,-2.82459281462198,26.3576109803925));
#91958=CARTESIAN_POINT('Ctrl Pts',(-0.31747340351993,-2.92972019540357,
26.4106444028883));
#91959=CARTESIAN_POINT('Ctrl Pts',(0.652667109514815,-3.03484757618516,
26.463677825384));
#91960=CARTESIAN_POINT('Ctrl Pts',(1.68021552783393,-2.61020113143511,26.5167112478798));
#91961=CARTESIAN_POINT('Ctrl Pts',(2.29310722013781,-1.85086711091042,26.5697446703756));
#91962=CARTESIAN_POINT('Ctrl Pts',(2.9059989124417,-1.09153309038574,26.6227780928713));
#91963=CARTESIAN_POINT('Ctrl Pts',(3.10423387873042,0.00248850591357333,
26.6758115153671));
#91964=CARTESIAN_POINT('Ctrl Pts',(2.79674126082988,0.928594693754894,26.7288449378628));
#91965=CARTESIAN_POINT('Ctrl Pts',(2.48924864292936,1.85470088159619,26.7818783603586));
#91966=CARTESIAN_POINT('Ctrl Pts',(1.67602844083961,2.61289166097947,26.8349117828543));
#91967=CARTESIAN_POINT('Ctrl Pts',(0.73068104946248,2.85484762977895,26.8879452053501));
#91968=CARTESIAN_POINT('Ctrl Pts',(-0.214666341914737,3.09680359857845,
26.9409786278459));
#91969=CARTESIAN_POINT('Ctrl Pts',(-1.29214092257942,2.82252475679402,26.9940120503416));
#91970=CARTESIAN_POINT('Ctrl Pts',(-2.00674155040704,2.15801717675463,27.0470454728374));
#91971=CARTESIAN_POINT('Ctrl Pts',(-2.59413423943573,1.61180034021774,27.0906382761951));
#91972=CARTESIAN_POINT('Ctrl Pts',(-2.93634634043979,0.801920292911836,
27.1342310795528));
#91973=CARTESIAN_POINT('Ctrl Pts',(-2.94363499374191,-0.002507597635829,
27.1778238829105));
#91974=CARTESIAN_POINT('Origin',(0.,0.,0.));
#91975=CARTESIAN_POINT('',(-2.94510414404698,0.00199674015882861,28.3221761170896));
#91976=CARTESIAN_POINT('',(-2.94550455047329,0.00178675002179936,28.1778238829105));
#91977=CARTESIAN_POINT('',(-2.942,-3.60291088309151E-16,0.));
#91978=CARTESIAN_POINT('Ctrl Pts',(-2.94510414404698,0.00199674015882861,
28.3221761170896));
#91979=CARTESIAN_POINT('Ctrl Pts',(-2.94604657952822,0.123184313699714,
28.3156003118272));
#91980=CARTESIAN_POINT('Ctrl Pts',(-2.93921686867972,0.244264808562547,
28.3090245065647));
#91981=CARTESIAN_POINT('Ctrl Pts',(-2.92425767409291,0.364332453299115,
28.3024487013023));
#91982=CARTESIAN_POINT('Ctrl Pts',(-2.80363960256099,1.33245461238088,28.2494270666869));
#91983=CARTESIAN_POINT('Ctrl Pts',(-2.15448950896227,2.23472711329033,28.1964054320716));
#91984=CARTESIAN_POINT('Ctrl Pts',(-1.27491122392638,2.65680681498011,28.1433837974562));
#91985=CARTESIAN_POINT('Ctrl Pts',(-0.395332938890521,3.07888651666988,
28.0903621628408));
#91986=CARTESIAN_POINT('Ctrl Pts',(0.714673537582494,3.02077341913999,28.0373405282254));
#91987=CARTESIAN_POINT('Ctrl Pts',(1.54536910828959,2.50915431971859,27.98431889361));
#91988=CARTESIAN_POINT('Ctrl Pts',(2.37606467899674,1.99753522029717,27.9312972589946));
#91989=CARTESIAN_POINT('Ctrl Pts',(2.92744934393793,1.03241011898417,27.8782756243793));
#91990=CARTESIAN_POINT('Ctrl Pts',(2.94631528200943,0.0569854368759391,
27.8252539897639));
#91991=CARTESIAN_POINT('Ctrl Pts',(2.96518122008093,-0.918439245232291,
27.7722323551485));
#91992=CARTESIAN_POINT('Ctrl Pts',(2.45152843128275,-1.90416350813576,27.7192107205331));
#91993=CARTESIAN_POINT('Ctrl Pts',(1.64123743918605,-2.44752134806466,27.6661890859177));
#91994=CARTESIAN_POINT('Ctrl Pts',(0.830946447089397,-2.99087918799354,
27.6131674513023));
#91995=CARTESIAN_POINT('Ctrl Pts',(-0.275982748305732,-3.09187060494792,
27.5601458166869));
#91996=CARTESIAN_POINT('Ctrl Pts',(-1.17122420414422,-2.7041181454672,27.5071241820716));
#91997=CARTESIAN_POINT('Ctrl Pts',(-2.06646565998275,-2.31636568598647,
27.4541025474562));
#91998=CARTESIAN_POINT('Ctrl Pts',(-2.75001937626462,-1.43986935007058,
27.4010809128408));
#91999=CARTESIAN_POINT('Ctrl Pts',(-2.90798263114761,-0.477135303621595,
27.3480592782254));
#92000=CARTESIAN_POINT('Ctrl Pts',(-2.93368653113318,-0.320478493397227,
27.3394315578468));
#92001=CARTESIAN_POINT('Ctrl Pts',(-2.94547382381967,-0.161538277289376,
27.3308038374682));
#92002=CARTESIAN_POINT('Ctrl Pts',(-2.94407188513322,-0.00239011867426281,
27.3221761170896));
#92003=CARTESIAN_POINT('Ctrl Pts',(-2.94363499374191,-0.002507597635829,
27.1778238829105));
#92004=CARTESIAN_POINT('Ctrl Pts',(-2.94521345152747,-0.176717484446133,
27.1872645020486));
#92005=CARTESIAN_POINT('Ctrl Pts',(-2.93108405332729,-0.350671665978835,
27.1967051211866));
#92006=CARTESIAN_POINT('Ctrl Pts',(-2.90033529857916,-0.521636790414356,
27.2061457403247));
#92007=CARTESIAN_POINT('Ctrl Pts',(-2.72760174393312,-1.48204685924987,
27.2591791628204));
#92008=CARTESIAN_POINT('Ctrl Pts',(-2.03040795965037,-2.34813067862668,
27.3122125853162));
#92009=CARTESIAN_POINT('Ctrl Pts',(-1.12905080070553,-2.72200185061,27.365246007812));
#92010=CARTESIAN_POINT('Ctrl Pts',(-0.227693641760674,-3.09587302259333,
27.4182794303077));
#92011=CARTESIAN_POINT('Ctrl Pts',(0.877826891846307,-2.97753154718315,
27.4713128528035));
#92012=CARTESIAN_POINT('Ctrl Pts',(1.6796251046219,-2.42134452179403,27.5243462752992));
#92013=CARTESIAN_POINT('Ctrl Pts',(2.48142331739747,-1.86515749640492,27.577379697795));
#92014=CARTESIAN_POINT('Ctrl Pts',(2.9794992093417,-0.871124921036897,27.6304131202907));
#92015=CARTESIAN_POINT('Ctrl Pts',(2.94503240751833,0.104086041162237,27.6834465427865));
#92016=CARTESIAN_POINT('Ctrl Pts',(2.91056560569497,1.07929700336143,27.7364799652823));
#92017=CARTESIAN_POINT('Ctrl Pts',(2.343556110104,2.03568635239166,27.789513387778));
#92018=CARTESIAN_POINT('Ctrl Pts',(1.50449298744779,2.53388054888515,27.8425468102738));
#92019=CARTESIAN_POINT('Ctrl Pts',(0.665429864791645,3.0320747453786,27.8955802327695));
#92020=CARTESIAN_POINT('Ctrl Pts',(-0.445686884929689,3.0720737893353,27.9486136552653));
#92021=CARTESIAN_POINT('Ctrl Pts',(-1.31840061613457,2.63550177398424,28.0016470777611));
#92022=CARTESIAN_POINT('Ctrl Pts',(-2.1911143473395,2.19892975863315,28.0546805002568));
#92023=CARTESIAN_POINT('Ctrl Pts',(-2.82542506002796,1.28578668397422,28.1077139227526));
#92024=CARTESIAN_POINT('Ctrl Pts',(-2.92992492623167,0.315578376864476,
28.1607473452483));
#92025=CARTESIAN_POINT('Ctrl Pts',(-2.94114109782648,0.211444053533942,
28.1664395244691));
#92026=CARTESIAN_POINT('Ctrl Pts',(-2.94625377339621,0.106652330639497,
28.1721317036898));
#92027=CARTESIAN_POINT('Ctrl Pts',(-2.94550455047329,0.00178675002179936,
28.1778238829105));
#92028=CARTESIAN_POINT('Origin',(0.,0.,0.));
#92029=CARTESIAN_POINT('',(-2.93776599353799,0.00138637979514328,29.3221761170896));
#92030=CARTESIAN_POINT('',(-2.9380367068104,0.00163420181435583,29.1778238829105));
#92031=CARTESIAN_POINT('',(-2.942,-3.60291088309151E-16,0.));
#92032=CARTESIAN_POINT('Ctrl Pts',(-2.93776599353799,0.00138637979514328,
29.3221761170896));
#92033=CARTESIAN_POINT('Ctrl Pts',(-2.93947922483499,0.405326537383405,
29.3003967861861));
#92034=CARTESIAN_POINT('Ctrl Pts',(-2.86194376351095,0.808637278136982,
29.2786174552827));
#92035=CARTESIAN_POINT('Ctrl Pts',(-2.7020086748925,1.17608256590425,29.2568381243793));
#92036=CARTESIAN_POINT('Ctrl Pts',(-2.31264777723671,2.07062564785274,29.2038164897639));
#92037=CARTESIAN_POINT('Ctrl Pts',(-1.43492427007663,2.7526028871322,29.1507948551485));
#92038=CARTESIAN_POINT('Ctrl Pts',(-0.471907863019101,2.90883551440073,
29.0977732205331));
#92039=CARTESIAN_POINT('Ctrl Pts',(0.491108544038425,3.06506814166927,29.0447515859177));
#92040=CARTESIAN_POINT('Ctrl Pts',(1.53941785099337,2.69555615692688,28.9917299513023));
#92041=CARTESIAN_POINT('Ctrl Pts',(2.1916136417186,1.96998749398345,28.9387083166869));
#92042=CARTESIAN_POINT('Ctrl Pts',(2.84380943244382,1.24441883104002,28.8856866820716));
#92043=CARTESIAN_POINT('Ctrl Pts',(3.09989170693931,0.162793489895487,28.8326650474562));
#92044=CARTESIAN_POINT('Ctrl Pts',(2.84226191945076,-0.778182666382572,
28.7796434128408));
#92045=CARTESIAN_POINT('Ctrl Pts',(2.58463213196221,-1.71915882266066,28.7266217782254));
#92046=CARTESIAN_POINT('Ctrl Pts',(1.81329028248965,-2.5194857940723,28.67360014361));
#92047=CARTESIAN_POINT('Ctrl Pts',(0.882453311491304,-2.81163604224591,
28.6205785089946));
#92048=CARTESIAN_POINT('Ctrl Pts',(-0.048383659506986,-3.10378629041951,
28.5675568743793));
#92049=CARTESIAN_POINT('Ctrl Pts',(-1.138715752031,-2.88775981535513,28.5145352397639));
#92050=CARTESIAN_POINT('Ctrl Pts',(-1.88783877356046,-2.26276066919592,
28.4615136051485));
#92051=CARTESIAN_POINT('Ctrl Pts',(-2.54405468004333,-1.71527464959593,
28.4150677757955));
#92052=CARTESIAN_POINT('Ctrl Pts',(-2.93844759085073,-0.853967987469306,
28.3686219464425));
#92053=CARTESIAN_POINT('Ctrl Pts',(-2.94510414404698,0.00199674015882861,
28.3221761170896));
#92054=CARTESIAN_POINT('Ctrl Pts',(-2.94550455047329,0.00178675002179936,
28.1778238829105));
#92055=CARTESIAN_POINT('Ctrl Pts',(-2.93927334388506,-0.870369022082387,
28.2251651261855));
#92056=CARTESIAN_POINT('Ctrl Pts',(-2.52757049983615,-1.74763358479836,
28.2725063694606));
#92057=CARTESIAN_POINT('Ctrl Pts',(-1.84938352851645,-2.29430389219696,
28.3198476127356));
#92058=CARTESIAN_POINT('Ctrl Pts',(-1.08965324487858,-2.90670431458808,
28.3728810352314));
#92059=CARTESIAN_POINT('Ctrl Pts',(0.00449634211611205,-3.10423161980979,
28.4259144577271));
#92060=CARTESIAN_POINT('Ctrl Pts',(0.930403448202452,-2.79614005530321,
28.4789478802229));
#92061=CARTESIAN_POINT('Ctrl Pts',(1.85631055428879,-2.48804849079663,28.5319813027187));
#92062=CARTESIAN_POINT('Ctrl Pts',(2.61397517946678,-1.67433805656175,28.5850147252144));
#92063=CARTESIAN_POINT('Ctrl Pts',(2.85531964140355,-0.72883436438824,28.6380481477102));
#92064=CARTESIAN_POINT('Ctrl Pts',(3.09666410334032,0.2166693277853,28.6910815702059));
#92065=CARTESIAN_POINT('Ctrl Pts',(2.82168840203584,1.29396627789748,28.7441149927017));
#92066=CARTESIAN_POINT('Ctrl Pts',(2.15671875311016,2.00813694883617,28.7971484151975));
#92067=CARTESIAN_POINT('Ctrl Pts',(1.4917491041845,2.72230761977483,28.8501818376932));
#92068=CARTESIAN_POINT('Ctrl Pts',(0.436785507637672,3.07335201154002,28.903215260189));
#92069=CARTESIAN_POINT('Ctrl Pts',(-0.523512635221601,2.89999729414725,
28.9562486826847));
#92070=CARTESIAN_POINT('Ctrl Pts',(-1.48381077808087,2.72664257675449,29.0092821051805));
#92071=CARTESIAN_POINT('Ctrl Pts',(-2.34944346725259,2.02888875020379,29.0623155276763));
#92072=CARTESIAN_POINT('Ctrl Pts',(-2.7227315579203,1.1272899577318,29.115348950172));
#92073=CARTESIAN_POINT('Ctrl Pts',(-2.86931301076673,0.773253319036106,
29.1361739277515));
#92074=CARTESIAN_POINT('Ctrl Pts',(-2.93997747852574,0.387784843198274,
29.156998905331));
#92075=CARTESIAN_POINT('Ctrl Pts',(-2.9380367068104,0.00163420181435583,
29.1778238829105));
#92076=CARTESIAN_POINT('Origin',(0.,0.,0.));
#92077=CARTESIAN_POINT('',(-2.94001376569275,-0.00252472911655227,30.3221761170896));
#92078=CARTESIAN_POINT('',(-2.9395119866127,-0.0023902824457737,30.1778238829105));
#92079=CARTESIAN_POINT('',(-2.942,-3.60291088309151E-16,0.));
#92080=CARTESIAN_POINT('Ctrl Pts',(-2.94001376569275,-0.00252472911655227,
30.3221761170896));
#92081=CARTESIAN_POINT('Ctrl Pts',(-2.93444893807589,0.682077234566173,
30.2851932605451));
#92082=CARTESIAN_POINT('Ctrl Pts',(-2.69624239041632,1.37017001338517,30.2482104040006));
#92083=CARTESIAN_POINT('Ctrl Pts',(-2.25936390251588,1.89190270284348,30.2112275474562));
#92084=CARTESIAN_POINT('Ctrl Pts',(-1.63301932772814,2.63990117056867,30.1582059128408));
#92085=CARTESIAN_POINT('Ctrl Pts',(-0.598316015418425,3.04595605037192,
30.1051842782254));
#92086=CARTESIAN_POINT('Ctrl Pts',(0.369587786719338,2.92359811686322,30.05216264361));
#92087=CARTESIAN_POINT('Ctrl Pts',(1.33749158885707,2.80124018335451,29.9991410089947));
#92088=CARTESIAN_POINT('Ctrl Pts',(2.23859588082286,2.15046943653388,29.9461193743793));
#92089=CARTESIAN_POINT('Ctrl Pts',(2.65909398850434,1.2701339462113,29.8930977397639));
#92090=CARTESIAN_POINT('Ctrl Pts',(3.07959209618584,0.389798455888696,29.8400761051485));
#92091=CARTESIAN_POINT('Ctrl Pts',(3.019484019583,-0.720101777935874,29.7870544705331));
#92092=CARTESIAN_POINT('Ctrl Pts',(2.50637269377013,-1.54987644699237,29.7340328359177));
#92093=CARTESIAN_POINT('Ctrl Pts',(1.99326136795729,-2.37965111604882,29.6810112013023));
#92094=CARTESIAN_POINT('Ctrl Pts',(1.02714679293448,-2.92930022033724,29.627989566687));
#92095=CARTESIAN_POINT('Ctrl Pts',(0.0516897776292723,-2.94641294592372,
29.5749679320716));
#92096=CARTESIAN_POINT('Ctrl Pts',(-0.923767237675969,-2.9635256715102,
29.5219462974562));
#92097=CARTESIAN_POINT('Ctrl Pts',(-1.90856669326362,-2.4481020183947,29.4689246628408));
#92098=CARTESIAN_POINT('Ctrl Pts',(-2.45046727698169,-1.63683572952821,
29.4159030282254));
#92099=CARTESIAN_POINT('Ctrl Pts',(-2.76977509804398,-1.15880769489887,
29.3846607245135));
#92100=CARTESIAN_POINT('Ctrl Pts',(-2.93530837476417,-0.578063059711174,
29.3534184208015));
#92101=CARTESIAN_POINT('Ctrl Pts',(-2.93776599353799,0.00138637979514328,
29.3221761170896));
#92102=CARTESIAN_POINT('Ctrl Pts',(-2.9380367068104,0.00163420181435583,
29.1778238829105));
#92103=CARTESIAN_POINT('Ctrl Pts',(-2.93503505945448,-0.595596292908616,
29.2100323278268));
#92104=CARTESIAN_POINT('Ctrl Pts',(-2.75835797892961,-1.19445856238458,
29.242240772743));
#92105=CARTESIAN_POINT('Ctrl Pts',(-2.42025762390727,-1.68119089315188,
29.2744492176593));
#92106=CARTESIAN_POINT('Ctrl Pts',(-1.86355210706285,-2.48262919317022,
29.3274826401551));
#92107=CARTESIAN_POINT('Ctrl Pts',(-0.869197581210329,-2.98006203481362,
29.3805160626508));
#92108=CARTESIAN_POINT('Ctrl Pts',(0.105990883665151,-2.9449644680162,29.4335494851466));
#92109=CARTESIAN_POINT('Ctrl Pts',(1.0811793485406,-2.90986690121879,29.4865829076423));
#92110=CARTESIAN_POINT('Ctrl Pts',(2.03720175243902,-2.34223892598059,29.5396163301381));
#92111=CARTESIAN_POINT('Ctrl Pts',(2.53485313376005,-1.50285374390355,29.5926497526339));
#92112=CARTESIAN_POINT('Ctrl Pts',(3.03250451508113,-0.663468561826437,
29.6456831751296));
#92113=CARTESIAN_POINT('Ctrl Pts',(3.07178487382474,0.447673827089566,29.6987165976254));
#92114=CARTESIAN_POINT('Ctrl Pts',(2.63464847342311,1.32010499839496,29.7517500201211));
#92115=CARTESIAN_POINT('Ctrl Pts',(2.1975120730215,2.19253616970031,29.8047834426169));
#92116=CARTESIAN_POINT('Ctrl Pts',(1.28395891347472,2.82625612339508,29.8578168651127));
#92117=CARTESIAN_POINT('Ctrl Pts',(0.313683218184318,2.93012843130256,29.9108502876084));
#92118=CARTESIAN_POINT('Ctrl Pts',(-0.656592477106082,3.03400073921004,
29.9638837101042));
#92119=CARTESIAN_POINT('Ctrl Pts',(-1.6835907081401,2.60802540133023,30.0169171325999));
#92120=CARTESIAN_POINT('Ctrl Pts',(-2.29549960441592,1.84789917241835,30.0699505550957));
#92121=CARTESIAN_POINT('Ctrl Pts',(-2.71038670676496,1.33251760099142,30.1059083310339));
#92122=CARTESIAN_POINT('Ctrl Pts',(-2.93445204415044,0.663522680698212,
30.1418661069722));
#92123=CARTESIAN_POINT('Ctrl Pts',(-2.9395119866127,-0.0023902824457737,
30.1778238829105));
#92124=CARTESIAN_POINT('Origin',(0.,0.,0.));
#92125=CARTESIAN_POINT('',(-2.94683142262726,-0.000288828235917582,31.3221761170896));
#92126=CARTESIAN_POINT('',(-2.94668913024009,-0.0006657472057589,31.1778238829105));
#92127=CARTESIAN_POINT('',(-2.942,-3.60291088309151E-16,0.));
#92128=CARTESIAN_POINT('Ctrl Pts',(-2.94683142262726,-0.000288828235917582,
31.3221761170896));
#92129=CARTESIAN_POINT('Ctrl Pts',(-2.94549260199717,0.959980156645984,
31.2699897349041));
#92130=CARTESIAN_POINT('Ctrl Pts',(-2.43187245641912,1.92147731567173,31.2178033527186));
#92131=CARTESIAN_POINT('Ctrl Pts',(-1.63242873210736,2.45340528971644,31.1656169705331));
#92132=CARTESIAN_POINT('Ctrl Pts',(-0.820189767249493,2.99384686662539,
31.1125953359177));
#92133=CARTESIAN_POINT('Ctrl Pts',(0.287095310098538,3.09085855354509,31.0595737013023));
#92134=CARTESIAN_POINT('Ctrl Pts',(1.18093712835462,2.69989047553633,31.0065520666869));
#92135=CARTESIAN_POINT('Ctrl Pts',(2.07477894661068,2.30892239752758,30.9535304320716));
#92136=CARTESIAN_POINT('Ctrl Pts',(2.75517750577479,1.42997455459038,30.9005087974562));
#92137=CARTESIAN_POINT('Ctrl Pts',(2.9096790007227,0.466678897928309,30.8474871628408));
#92138=CARTESIAN_POINT('Ctrl Pts',(3.06418049567062,-0.496616758733819,
30.7944655282254));
#92139=CARTESIAN_POINT('Ctrl Pts',(2.69278492640225,-1.54426022912084,30.74144389361));
#92140=CARTESIAN_POINT('Ctrl Pts',(1.96604520967682,-2.19515086372784,30.6884222589947));
#92141=CARTESIAN_POINT('Ctrl Pts',(1.23930549295141,-2.84604149833482,30.6354006243793));
#92142=CARTESIAN_POINT('Ctrl Pts',(0.157221628768963,-3.10017929716181,
30.5823789897638));
#92143=CARTESIAN_POINT('Ctrl Pts',(-0.783289956059199,-2.84085865993981,
30.5293573551485));
#92144=CARTESIAN_POINT('Ctrl Pts',(-1.72380154088736,-2.58153802271781,
30.4763357205331));
#92145=CARTESIAN_POINT('Ctrl Pts',(-2.52274084636124,-1.80875894944683,
30.4233140859177));
#92146=CARTESIAN_POINT('Ctrl Pts',(-2.8132175804653,-0.877398384987801,
30.3702924513024));
#92147=CARTESIAN_POINT('Ctrl Pts',(-2.9010853330696,-0.595666493737709,
30.3542536732314));
#92148=CARTESIAN_POINT('Ctrl Pts',(-2.94242712808519,-0.299423886952565,
30.3382148951605));
#92149=CARTESIAN_POINT('Ctrl Pts',(-2.94001376569275,-0.00252472911655227,
30.3221761170896));
#92150=CARTESIAN_POINT('Ctrl Pts',(-2.9395119866127,-0.0023902824457737,
30.1778238829105));
#92151=CARTESIAN_POINT('Ctrl Pts',(-2.94191485461085,-0.318619362248227,
30.194899529468));
#92152=CARTESIAN_POINT('Ctrl Pts',(-2.89492949018049,-0.634153425308857,
30.2119751760255));
#92153=CARTESIAN_POINT('Ctrl Pts',(-2.79553767998929,-0.932211813408388,
30.229050822583));
#92154=CARTESIAN_POINT('Ctrl Pts',(-2.4868472977692,-1.85791945037922,30.2820842450787));
#92155=CARTESIAN_POINT('Ctrl Pts',(-1.67264697181141,-2.61505760437691,
30.3351176675745));
#92156=CARTESIAN_POINT('Ctrl Pts',(-0.726987374400473,-2.85579045848262,
30.3881510900703));
#92157=CARTESIAN_POINT('Ctrl Pts',(0.218672223010494,-3.09652331258834,
30.441184512566));
#92158=CARTESIAN_POINT('Ctrl Pts',(1.29579109187459,-2.82085086680205,30.4942179350618));
#92159=CARTESIAN_POINT('Ctrl Pts',(2.00953150714542,-2.15541942718533,30.5472513575575));
#92160=CARTESIAN_POINT('Ctrl Pts',(2.72327192241621,-1.48998798756864,30.6002847800533));
#92161=CARTESIAN_POINT('Ctrl Pts',(3.07363388409376,-0.434797554121506,
30.653318202549));
#92162=CARTESIAN_POINT('Ctrl Pts',(2.8996580764786,0.525388261013206,30.7063516250448));
#92163=CARTESIAN_POINT('Ctrl Pts',(2.72568226886344,1.48557407614795,30.7593850475406));
#92164=CARTESIAN_POINT('Ctrl Pts',(2.02736869195559,2.35075527297029,30.8124184700363));
#92165=CARTESIAN_POINT('Ctrl Pts',(1.12552864314742,2.72346012615438,30.8654518925321));
#92166=CARTESIAN_POINT('Ctrl Pts',(0.223688594339212,3.09616497933847,30.9184853150278));
#92167=CARTESIAN_POINT('Ctrl Pts',(-0.881677926369304,2.97639348888425,
30.9715187375236));
#92168=CARTESIAN_POINT('Ctrl Pts',(-1.68275597834239,2.41916971348664,31.0245521600194));
#92169=CARTESIAN_POINT('Ctrl Pts',(-2.45448700768209,1.88235950291979,31.0756427343164));
#92170=CARTESIAN_POINT('Ctrl Pts',(-2.94381604647467,0.939561525051785,
31.1267333086134));
#92171=CARTESIAN_POINT('Ctrl Pts',(-2.94668913024009,-0.0006657472057589,
31.1778238829105));
#92172=CARTESIAN_POINT('Origin',(0.,0.,0.));
#92173=CARTESIAN_POINT('',(-2.94088266626002,0.00267082732003945,32.3221761170896));
#92174=CARTESIAN_POINT('',(-2.94152987837198,0.00271722750875524,32.1778238829105));
#92175=CARTESIAN_POINT('',(-2.942,-3.60291088309151E-16,0.));
#92176=CARTESIAN_POINT('Ctrl Pts',(-2.94088266626002,0.00267082732003945,
32.3221761170896));
#92177=CARTESIAN_POINT('Ctrl Pts',(-2.943221129712,0.268447683304989,32.3078078438784));
#92178=CARTESIAN_POINT('Ctrl Pts',(-2.91017720576495,0.533653254375284,
32.2934395706673));
#92179=CARTESIAN_POINT('Ctrl Pts',(-2.83944622309545,0.78839471533439,32.2790712974562));
#92180=CARTESIAN_POINT('Ctrl Pts',(-2.57843557386977,1.72843869041002,32.2260496628408));
#92181=CARTESIAN_POINT('Ctrl Pts',(-1.80422177324665,2.52598774898972,32.1730280282254));
#92182=CARTESIAN_POINT('Ctrl Pts',(-0.872340624067349,2.81479003064528,
32.12000639361));
#92183=CARTESIAN_POINT('Ctrl Pts',(0.0595405251119813,3.10359231230084,
32.0669847589946));
#92184=CARTESIAN_POINT('Ctrl Pts',(1.14908902284753,2.88364781703224,32.0139631243793));
#92185=CARTESIAN_POINT('Ctrl Pts',(1.89596052037525,2.25595983700877,31.9609414897639));
#92186=CARTESIAN_POINT('Ctrl Pts',(2.64283201790295,1.62827185698532,31.9079198551485));
#92187=CARTESIAN_POINT('Ctrl Pts',(3.04702651522286,0.592840392207089,31.8548982205331));
#92188=CARTESIAN_POINT('Ctrl Pts',(2.9229291150121,-0.374841926194006,31.8018765859177));
#92189=CARTESIAN_POINT('Ctrl Pts',(2.79883171480133,-1.3425242445951,31.7488549513023));
#92190=CARTESIAN_POINT('Ctrl Pts',(2.14644241705985,-2.24245741661903,31.695833316687));
#92191=CARTESIAN_POINT('Ctrl Pts',(1.26535256535564,-2.66137257188206,31.6428116820716));
#92192=CARTESIAN_POINT('Ctrl Pts',(0.384262713651435,-3.08028772714509,
31.5897900474562));
#92193=CARTESIAN_POINT('Ctrl Pts',(-0.725527692015529,-3.01818486564724,
31.5367684128408));
#92194=CARTESIAN_POINT('Ctrl Pts',(-1.55437877885202,-2.50358297103825,
31.4837467782254));
#92195=CARTESIAN_POINT('Ctrl Pts',(-2.38322986568854,-1.98898107642925,
31.43072514361));
#92196=CARTESIAN_POINT('Ctrl Pts',(-2.93114163369459,-1.02188014870908,
31.3777035089946));
#92197=CARTESIAN_POINT('Ctrl Pts',(-2.94650109151376,-0.0463939513998811,
31.3246818743793));
#92198=CARTESIAN_POINT('Ctrl Pts',(-2.94674304981169,-0.0310270691349388,
31.3238466219494));
#92199=CARTESIAN_POINT('Ctrl Pts',(-2.94685285069216,-0.0156581059935221,
31.3230113695195));
#92200=CARTESIAN_POINT('Ctrl Pts',(-2.94683142262726,-0.000288828235917582,
31.3221761170896));
#92201=CARTESIAN_POINT('Ctrl Pts',(-2.94668913024009,-0.0006657472057589,
31.1778238829105));
#92202=CARTESIAN_POINT('Ctrl Pts',(-2.94679838651085,-0.0364202652831939,
31.1797667311092));
#92203=CARTESIAN_POINT('Ctrl Pts',(-2.94620418231902,-0.0721710658817098,
31.1817095793079));
#92204=CARTESIAN_POINT('Ctrl Pts',(-2.94489529646495,-0.107895681825943,
31.1836524275066));
#92205=CARTESIAN_POINT('Ctrl Pts',(-2.90916697937683,-1.08306124139995,
31.2366858500024));
#92206=CARTESIAN_POINT('Ctrl Pts',(-2.34092076196299,-2.03871630020705,
31.2897192724982));
#92207=CARTESIAN_POINT('Ctrl Pts',(-1.50121387162844,-2.53582465815924,
31.3427526949939));
#92208=CARTESIAN_POINT('Ctrl Pts',(-0.661506981293825,-3.03293301611147,
31.3957861174897));
#92209=CARTESIAN_POINT('Ctrl Pts',(0.449660581961557,-3.07149467320871,
31.4488195399855));
#92210=CARTESIAN_POINT('Ctrl Pts',(1.32180882837894,-2.63379407063604,31.5018529624812));
#92211=CARTESIAN_POINT('Ctrl Pts',(2.19395707479628,-2.1960934680634,31.5548863849769));
#92212=CARTESIAN_POINT('Ctrl Pts',(2.82708600437565,-1.2821306058209,31.6079198074727));
#92213=CARTESIAN_POINT('Ctrl Pts',(2.9303307105311,-0.31178792827231,31.6609532299685));
#92214=CARTESIAN_POINT('Ctrl Pts',(3.03357541668656,0.658554749276281,31.7139866524642));
#92215=CARTESIAN_POINT('Ctrl Pts',(2.60693589941809,1.68527724213097,31.76702007496));
#92216=CARTESIAN_POINT('Ctrl Pts',(1.84641404323699,2.29669435629457,31.8200534974558));
#92217=CARTESIAN_POINT('Ctrl Pts',(1.08589218705586,2.90811147045818,31.8730869199515));
#92218=CARTESIAN_POINT('Ctrl Pts',(-0.00851200803791696,3.10422320593068,
31.9261203424473));
#92219=CARTESIAN_POINT('Ctrl Pts',(-0.934019788616158,2.79493413514013,
31.979153764943));
#92220=CARTESIAN_POINT('Ctrl Pts',(-1.85952756919437,2.48564506434958,32.0321871874388));
#92221=CARTESIAN_POINT('Ctrl Pts',(-2.61613893525706,1.67095518729601,32.0852206099346));
#92222=CARTESIAN_POINT('Ctrl Pts',(-2.85626008081923,0.725140080271805,
32.1382540324303));
#92223=CARTESIAN_POINT('Ctrl Pts',(-2.91598064557429,0.489906268550998,
32.1514439825904));
#92224=CARTESIAN_POINT('Ctrl Pts',(-2.94375281118411,0.246561478114943,
32.1646339327504));
#92225=CARTESIAN_POINT('Ctrl Pts',(-2.94152987837198,0.00271722750875524,
32.1778238829105));
#92226=CARTESIAN_POINT('Origin',(0.,0.,0.));
#92227=CARTESIAN_POINT('',(-2.93740160319918,-0.000921743247123685,33.3221761170896));
#92228=CARTESIAN_POINT('',(-2.93722324760469,-0.000551307423291771,33.1778238829105));
#92229=CARTESIAN_POINT('',(-2.942,-3.60291088309151E-16,0.));
#92230=CARTESIAN_POINT('Ctrl Pts',(-2.93740160319918,-0.000921743247123685,
33.3221761170896));
#92231=CARTESIAN_POINT('Ctrl Pts',(-2.93586593204594,0.54771487550154,33.2926043182374));
#92232=CARTESIAN_POINT('Ctrl Pts',(-2.78862489741151,1.09711691069357,33.2630325193853));
#92233=CARTESIAN_POINT('Ctrl Pts',(-2.50078516053484,1.55887608932429,33.2334607205331));
#92234=CARTESIAN_POINT('Ctrl Pts',(-1.98469435954012,2.386800916355,33.1804390859177));
#92235=CARTESIAN_POINT('Ctrl Pts',(-1.01661020332163,2.93297357806132,33.1274174513023));
#92236=CARTESIAN_POINT('Ctrl Pts',(-0.0410979752959005,2.94657971849479,
33.074395816687));
#92237=CARTESIAN_POINT('Ctrl Pts',(0.934414252729828,2.96018585892825,33.0213741820716));
#92238=CARTESIAN_POINT('Ctrl Pts',(1.91735455256277,2.44122547808888,32.9683525474562));
#92239=CARTESIAN_POINT('Ctrl Pts',(2.45633537677761,1.62801646116033,32.9153309128408));
#92240=CARTESIAN_POINT('Ctrl Pts',(2.99531620099246,0.814807444231778,32.8623092782254));
#92241=CARTESIAN_POINT('Ctrl Pts',(3.0903375495892,-0.292650208786009,32.80928764361));
#92242=CARTESIAN_POINT('Ctrl Pts',(2.6977635542415,-1.18578787581275,32.7562660089946));
#92243=CARTESIAN_POINT('Ctrl Pts',(2.30518955889379,-2.07892554283951,32.7032443743793));
#92244=CARTESIAN_POINT('Ctrl Pts',(1.42502021960166,-2.75774322387527,32.6502227397639));
#92245=CARTESIAN_POINT('Ctrl Pts',(0.461448425241032,-2.91051308738868,
32.5972011051485));
#92246=CARTESIAN_POINT('Ctrl Pts',(-0.502123369119543,-3.06328295090209,
32.5441794705331));
#92247=CARTESIAN_POINT('Ctrl Pts',(-1.54909761854858,-2.69000499689322,
32.4911578359177));
#92248=CARTESIAN_POINT('Ctrl Pts',(-2.19868099434898,-1.96209657410302,
32.4381362013023));
#92249=CARTESIAN_POINT('Ctrl Pts',(-2.67223450074586,-1.43144323722631,
32.3994828398981));
#92250=CARTESIAN_POINT('Ctrl Pts',(-2.93459175909169,-0.712318978087848,
32.3608294784938));
#92251=CARTESIAN_POINT('Ctrl Pts',(-2.94088266626002,0.00267082732003945,
32.3221761170896));
#92252=CARTESIAN_POINT('Ctrl Pts',(-2.94152987837198,0.00271722750875524,
32.1778238829105));
#92253=CARTESIAN_POINT('Ctrl Pts',(-2.93481496581132,-0.733874005615878,
32.2176673552462));
#92254=CARTESIAN_POINT('Ctrl Pts',(-2.65439781930278,-1.47502276218687,
32.2575108275819));
#92255=CARTESIAN_POINT('Ctrl Pts',(-2.15411919952377,-2.01092522475132,
32.2973542999176));
#92256=CARTESIAN_POINT('Ctrl Pts',(-1.48822624760452,-2.72423508575532,
32.3503877224134));
#92257=CARTESIAN_POINT('Ctrl Pts',(-0.432809418704383,-3.07391447076852,
32.4034211449091));
#92258=CARTESIAN_POINT('Ctrl Pts',(0.527263667004487,-2.89931764571512,
32.4564545674049));
#92259=CARTESIAN_POINT('Ctrl Pts',(1.48733675271336,-2.72472082066171,32.5094879899006));
#92260=CARTESIAN_POINT('Ctrl Pts',(2.35206609523099,-2.0258477855417,32.5625214123964));
#92261=CARTESIAN_POINT('Ctrl Pts',(2.72418755500742,-1.12376685768925,32.6155548348921));
#92262=CARTESIAN_POINT('Ctrl Pts',(3.09630901478386,-0.221685929836773,
32.6685882573879));
#92263=CARTESIAN_POINT('Ctrl Pts',(2.97582259181911,0.883602890748098,32.7216216798837));
#92264=CARTESIAN_POINT('Ctrl Pts',(2.41808079098732,1.68432035953859,32.7746551023794));
#92265=CARTESIAN_POINT('Ctrl Pts',(1.86033899015554,2.48503782832908,32.8276885248752));
#92266=CARTESIAN_POINT('Ctrl Pts',(0.865341811456686,2.98118394532513,32.880721947371));
#92267=CARTESIAN_POINT('Ctrl Pts',(-0.109800434847724,2.94482489289352,
32.9337553698667));
#92268=CARTESIAN_POINT('Ctrl Pts',(-1.08494268115213,2.90846584046192,32.9867887923625));
#92269=CARTESIAN_POINT('Ctrl Pts',(-2.04022999506213,2.33960161860266,33.0398222148582));
#92270=CARTESIAN_POINT('Ctrl Pts',(-2.53679512167625,1.49957337130853,33.092855637354));
#92271=CARTESIAN_POINT('Ctrl Pts',(-2.80198806119353,1.05095233805867,33.1211783858728));
#92272=CARTESIAN_POINT('Ctrl Pts',(-2.93634681713537,0.524991413987441,
33.1495011343917));
#92273=CARTESIAN_POINT('Ctrl Pts',(-2.93722324760469,-0.000551307423291771,
33.1778238829105));
#92274=CARTESIAN_POINT('Origin',(0.,0.,0.));
#92275=CARTESIAN_POINT('',(-2.94427325151691,-0.00232800721794407,34.3221761170896));
#92276=CARTESIAN_POINT('',(-2.94355950823906,-0.00252461584680807,34.1778238829105));
#92277=CARTESIAN_POINT('',(-2.942,-3.60291088309151E-16,0.));
#92278=CARTESIAN_POINT('Ctrl Pts',(-2.94427325151691,-0.00232800721794407,
34.3221761170896));
#92279=CARTESIAN_POINT('Ctrl Pts',(-2.93711978754248,0.823457452646246,
34.2774007925964));
#92280=CARTESIAN_POINT('Ctrl Pts',(-2.57382536708779,1.65475429244643,34.2326254681032));
#92281=CARTESIAN_POINT('Ctrl Pts',(-1.95814160001811,2.20220402217795,34.18785014361));
#92282=CARTESIAN_POINT('Ctrl Pts',(-1.22906682265575,2.85047804070656,34.1348285089946));
#92283=CARTESIAN_POINT('Ctrl Pts',(-0.146076400813901,3.10072443152059,
34.0818068743793));
#92284=CARTESIAN_POINT('Ctrl Pts',(0.79349692771717,2.83802461348059,34.0287852397639));
#92285=CARTESIAN_POINT('Ctrl Pts',(1.73307025624827,2.57532479544058,33.9757636051485));
#92286=CARTESIAN_POINT('Ctrl Pts',(2.52922649146857,1.79967876854651,33.9227419705331));
#92287=CARTESIAN_POINT('Ctrl Pts',(2.81635338770602,0.867280045069095,33.8697203359177));
#92288=CARTESIAN_POINT('Ctrl Pts',(3.10348028394345,-0.0651186784082651,
33.8166987013023));
#92289=CARTESIAN_POINT('Ctrl Pts',(2.88157784119809,-1.15427009846895,33.7636770666869));
#92290=CARTESIAN_POINT('Ctrl Pts',(2.25254848367163,-1.90001221304677,33.7106554320716));
#92291=CARTESIAN_POINT('Ctrl Pts',(1.62351912614512,-2.64575432762465,33.6576337974562));
#92292=CARTESIAN_POINT('Ctrl Pts',(0.587362853837422,-3.04808713671961,
33.6046121628408));
#92293=CARTESIAN_POINT('Ctrl Pts',(-0.380094854749983,-2.92225067070072,
33.5515905282254));
#92294=CARTESIAN_POINT('Ctrl Pts',(-1.34755256333731,-2.79641420468185,
33.49856889361));
#92295=CARTESIAN_POINT('Ctrl Pts',(-2.24631170820435,-2.14240846354924,
33.4455472589947));
#92296=CARTESIAN_POINT('Ctrl Pts',(-2.66364255775242,-1.2605670968054,33.3925256243793));
#92297=CARTESIAN_POINT('Ctrl Pts',(-2.84821513745164,-0.870555823683219,
33.369075788616));
#92298=CARTESIAN_POINT('Ctrl Pts',(-2.93861935922781,-0.435979436817632,
33.3456259528528));
#92299=CARTESIAN_POINT('Ctrl Pts',(-2.93740160319918,-0.000921743247123685,
33.3221761170896));
#92300=CARTESIAN_POINT('Ctrl Pts',(-2.93722324760469,-0.000551307423291771,
33.1778238829105));
#92301=CARTESIAN_POINT('Ctrl Pts',(-2.93798790459327,-0.459070184611203,
33.2025345568874));
#92302=CARTESIAN_POINT('Ctrl Pts',(-2.83714590676715,-0.917270726220104,
33.2272452308643));
#92303=CARTESIAN_POINT('Ctrl Pts',(-2.63293856598045,-1.32351210537377,
33.2519559048413));
#92304=CARTESIAN_POINT('Ctrl Pts',(-2.19467394435226,-2.195377062033,33.304989327337));
#92305=CARTESIAN_POINT('Ctrl Pts',(-1.28030176177763,-2.82791470262249,
33.3580227498328));
#92306=CARTESIAN_POINT('Ctrl Pts',(-0.309892507921363,-2.93053176383268,
33.4110561723285));
#92307=CARTESIAN_POINT('Ctrl Pts',(0.660516745934904,-3.03314882504287,
33.4640895948243));
#92308=CARTESIAN_POINT('Ctrl Pts',(1.68696307107281,-2.60584530687375,33.5171230173201));
#92309=CARTESIAN_POINT('Ctrl Pts',(2.29788814733301,-1.84492814159374,33.5701564398158));
#92310=CARTESIAN_POINT('Ctrl Pts',(2.90881322359324,-1.08401097631369,33.6231898623116));
#92311=CARTESIAN_POINT('Ctrl Pts',(3.10421705097572,0.0105198360772893,
33.6762232848074));
#92312=CARTESIAN_POINT('Ctrl Pts',(2.7943294210082,0.935827373069456,33.7292567073031));
#92313=CARTESIAN_POINT('Ctrl Pts',(2.48444179104069,1.86113491006157,33.7822901297989));
#92314=CARTESIAN_POINT('Ctrl Pts',(1.66926270372325,2.6172191716549,33.8353235522946));
#92315=CARTESIAN_POINT('Ctrl Pts',(0.723292482774982,2.85672850821692,33.8883569747904));
#92316=CARTESIAN_POINT('Ctrl Pts',(-0.222677738173258,3.09623784477894,
33.9413903972861));
#92317=CARTESIAN_POINT('Ctrl Pts',(-1.29943909275232,2.81917225630971,33.9944238197819));
#92318=CARTESIAN_POINT('Ctrl Pts',(-2.01231810107072,2.15281807066951,34.0474572422777));
#92319=CARTESIAN_POINT('Ctrl Pts',(-2.59645062931776,1.60680794745917,34.0909127891553));
#92320=CARTESIAN_POINT('Ctrl Pts',(-2.93626704149822,0.799423566697762,
34.1343683360329));
#92321=CARTESIAN_POINT('Ctrl Pts',(-2.94355950823906,-0.00252461584680807,
34.1778238829105));
#92322=CARTESIAN_POINT('Origin',(0.,0.,0.));
#92323=CARTESIAN_POINT('',(-2.94492293178134,0.00208059058526368,35.3221761170896));
#92324=CARTESIAN_POINT('',(-2.94556291087109,0.0017517216428375,35.1778238829105));
#92325=CARTESIAN_POINT('',(-2.942,-3.60291088309151E-16,0.));
#92326=CARTESIAN_POINT('Ctrl Pts',(-2.94492293178134,0.00208059058526368,
35.3221761170896));
#92327=CARTESIAN_POINT('Ctrl Pts',(-2.94595073758724,0.130317914585527,
35.3152189015707));
#92328=CARTESIAN_POINT('Ctrl Pts',(-2.9383025122363,0.258431807689072,35.3082616860519));
#92329=CARTESIAN_POINT('Ctrl Pts',(-2.92156278612083,0.385346555417464,
35.3013044705331));
#92330=CARTESIAN_POINT('Ctrl Pts',(-2.79398766080593,1.35257652883955,35.2482828359177));
#92331=CARTESIAN_POINT('Ctrl Pts',(-2.13836758903384,2.25015874312748,35.1952612013023));
#92332=CARTESIAN_POINT('Ctrl Pts',(-1.25577755602009,2.6659039387822,35.142239566687));
#92333=CARTESIAN_POINT('Ctrl Pts',(-0.373187523006309,3.08164913443693,
35.0892179320716));
#92334=CARTESIAN_POINT('Ctrl Pts',(0.73637247124921,3.01555731145834,35.0361962974562));
#92335=CARTESIAN_POINT('Ctrl Pts',(1.56336836388063,2.49797927129819,34.9831746628408));
#92336=CARTESIAN_POINT('Ctrl Pts',(2.39036425651199,1.98040123113808,34.9301530282254));
#92337=CARTESIAN_POINT('Ctrl Pts',(2.93479604751941,1.01133697379647,34.87713139361));
#92338=CARTESIAN_POINT('Ctrl Pts',(2.94664882661281,0.0358018664257049,
34.8241097589947));
#92339=CARTESIAN_POINT('Ctrl Pts',(2.95850160570621,-0.939733240945092,
34.7710881243793));
#92340=CARTESIAN_POINT('Ctrl Pts',(2.43777537288558,-1.92173919834509,34.7180664897639));
#92341=CARTESIAN_POINT('Ctrl Pts',(1.62359893094074,-2.45925752869974,34.6650448551485));
#92342=CARTESIAN_POINT('Ctrl Pts',(0.809422488995877,-2.9967758590544,34.6120232205331));
#92343=CARTESIAN_POINT('Ctrl Pts',(-0.298204162073124,-3.08980656236369,
34.5590015859177));
#92344=CARTESIAN_POINT('Ctrl Pts',(-1.19063479260833,-2.69562791787901,
34.5059799513024));
#92345=CARTESIAN_POINT('Ctrl Pts',(-2.08306542314352,-2.30144927339435,
34.452958316687));
#92346=CARTESIAN_POINT('Ctrl Pts',(-2.76030003314485,-1.42006128111569,
34.3999366820716));
#92347=CARTESIAN_POINT('Ctrl Pts',(-2.91133777170409,-0.456216461854777,
34.3469150474562));
#92348=CARTESIAN_POINT('Ctrl Pts',(-2.93482825896181,-0.306312307692763,
34.338668737334));
#92349=CARTESIAN_POINT('Ctrl Pts',(-2.9455907111456,-0.154413627445788,
34.3304224272118));
#92350=CARTESIAN_POINT('Ctrl Pts',(-2.94427325151691,-0.00232800721794407,
34.3221761170896));
#92351=CARTESIAN_POINT('Ctrl Pts',(-2.94355950823906,-0.00252461584680807,
34.1778238829105));
#92352=CARTESIAN_POINT('Ctrl Pts',(-2.94516681373656,-0.179279034937491,
34.1874017585286));
#92353=CARTESIAN_POINT('Ctrl Pts',(-2.93062046171695,-0.355769369334824,
34.1969796341468));
#92354=CARTESIAN_POINT('Ctrl Pts',(-2.89897600199921,-0.529138852410934,
34.2065575097649));
#92355=CARTESIAN_POINT('Ctrl Pts',(-2.72375823255149,-1.4890988070398,34.2595909322607));
#92356=CARTESIAN_POINT('Ctrl Pts',(-2.02432603159842,-2.35337593348627,
34.3126243547565));
#92357=CARTESIAN_POINT('Ctrl Pts',(-1.12200460209435,-2.72491384417511,
34.3656577772522));
#92358=CARTESIAN_POINT('Ctrl Pts',(-0.219683172590273,-3.09645175486395,
34.418691199748));
#92359=CARTESIAN_POINT('Ctrl Pts',(0.885527485464739,-2.97525044979509,
34.4717246222437));
#92360=CARTESIAN_POINT('Ctrl Pts',(1.68588403608615,-2.41699085686478,34.5247580447395));
#92361=CARTESIAN_POINT('Ctrl Pts',(2.48624058670757,-1.85873126393446,34.5777914672353));
#92362=CARTESIAN_POINT('Ctrl Pts',(2.98174302989538,-0.863413383142613,
34.630824889731));
#92363=CARTESIAN_POINT('Ctrl Pts',(2.94475325733136,0.111705141933711,34.6838583122268));
#92364=CARTESIAN_POINT('Ctrl Pts',(2.90776348476734,1.08682366701001,34.7368917347225));
#92365=CARTESIAN_POINT('Ctrl Pts',(2.33828149645164,2.04174283637074,34.7899251572183));
#92366=CARTESIAN_POINT('Ctrl Pts',(1.49793224363048,2.53776452390489,34.8429585797141));
#92367=CARTESIAN_POINT('Ctrl Pts',(0.657582990809354,3.03378621143902,34.8959920022098));
#92368=CARTESIAN_POINT('Ctrl Pts',(-0.453633526517266,3.07091041714649,
34.9490254247056));
#92369=CARTESIAN_POINT('Ctrl Pts',(-1.3252148286668,2.63208195981427,35.0020588472013));
#92370=CARTESIAN_POINT('Ctrl Pts',(-2.1967961308164,2.193253502482,35.0550922696971));
#92371=CARTESIAN_POINT('Ctrl Pts',(-2.82874221778894,1.27847238211,35.1081256921929));
#92372=CARTESIAN_POINT('Ctrl Pts',(-2.93073159112318,0.307996957924358,
35.1611591146886));
#92373=CARTESIAN_POINT('Ctrl Pts',(-2.94141434668702,0.20634566428115,35.1667140374292));
#92374=CARTESIAN_POINT('Ctrl Pts',(-2.94628280629519,0.104083333628536,
35.1722689601699));
#92375=CARTESIAN_POINT('Ctrl Pts',(-2.94556291087109,0.0017517216428375,
35.1778238829105));
#92376=CARTESIAN_POINT('Origin',(0.,0.,0.));
#92377=CARTESIAN_POINT('',(-2.93766977734024,0.00128397461115384,36.3221761170896));
#92378=CARTESIAN_POINT('',(-2.9380797671204,0.00166795251978762,36.1778238829105));
#92379=CARTESIAN_POINT('',(-2.942,-3.60291088309151E-16,0.));
#92380=CARTESIAN_POINT('Ctrl Pts',(-2.93766977734024,0.00128397461115384,
36.3221761170896));
#92381=CARTESIAN_POINT('Ctrl Pts',(-2.93928119520059,0.412331772833426,
36.3000153759297));
#92382=CARTESIAN_POINT('Ctrl Pts',(-2.85890327362297,0.822777322858098,
36.2778546347699));
#92383=CARTESIAN_POINT('Ctrl Pts',(-2.69348357334797,1.19547786308358,36.25569389361));
#92384=CARTESIAN_POINT('Ctrl Pts',(-2.29770155311203,2.08719857414911,36.2026722589947));
#92385=CARTESIAN_POINT('Ctrl Pts',(-1.41509775515192,2.76284792532406,36.1496506243793));
#92386=CARTESIAN_POINT('Ctrl Pts',(-0.450983024670797,2.91215305100488,
36.0966289897639));
#92387=CARTESIAN_POINT('Ctrl Pts',(0.513131705810276,3.06145817668569,36.0436073551485));
#92388=CARTESIAN_POINT('Ctrl Pts',(1.55875736881236,2.68441907687241,35.9905857205331));
#92389=CARTESIAN_POINT('Ctrl Pts',(2.20571993583375,1.95418030019847,35.9375640859177));
#92390=CARTESIAN_POINT('Ctrl Pts',(2.85268250285517,1.22394152352449,35.8845424513023));
#92391=CARTESIAN_POINT('Ctrl Pts',(3.10098197389584,0.140503069989798,35.831520816687));
#92392=CARTESIAN_POINT('Ctrl Pts',(2.83659383568765,-0.79859657672511,35.7784991820716));
#92393=CARTESIAN_POINT('Ctrl Pts',(2.57220569747947,-1.73769622343999,35.7254775474562));
#92394=CARTESIAN_POINT('Ctrl Pts',(1.79512995002246,-2.5324570633351,35.6724559128408));
#92395=CARTESIAN_POINT('Ctrl Pts',(0.862216664341213,-2.81790764659713,
35.6194342782254));
#92396=CARTESIAN_POINT('Ctrl Pts',(-0.0706966213400306,-3.10335822985915,
35.56641264361));
#92397=CARTESIAN_POINT('Ctrl Pts',(-1.15944744524551,-2.87949855648811,
35.5133910089947));
#92398=CARTESIAN_POINT('Ctrl Pts',(-1.90405776776943,-2.2491298535245,35.4603693743793));
#92399=CARTESIAN_POINT('Ctrl Pts',(-2.55096430335971,-1.70147476274293,
35.4143049552827));
#92400=CARTESIAN_POINT('Ctrl Pts',(-2.93811772684485,-0.846991544752816,
35.3682405361861));
#92401=CARTESIAN_POINT('Ctrl Pts',(-2.94492293178134,0.00208059058526368,
35.3221761170896));
#92402=CARTESIAN_POINT('Ctrl Pts',(-2.94556291087109,0.0017517216428375,
35.1778238829105));
#92403=CARTESIAN_POINT('Ctrl Pts',(-2.9394098901518,-0.872887160204899,
35.2253023826656));
#92404=CARTESIAN_POINT('Ctrl Pts',(-2.5250108881712,-1.75258724980421,35.2727808824207));
#92405=CARTESIAN_POINT('Ctrl Pts',(-1.84344146811026,-2.29908097703182,
35.3202593821759));
#92406=CARTESIAN_POINT('Ctrl Pts',(-1.08212931206705,-2.90951375980329,
35.3732928046716));
#92407=CARTESIAN_POINT('Ctrl Pts',(0.0125276597154277,-3.10420959734703,
35.4263262271674));
#92408=CARTESIAN_POINT('Ctrl Pts',(0.937634566011756,-2.79372353784658,
35.4793596496632));
#92409=CARTESIAN_POINT('Ctrl Pts',(1.86274147230814,-2.48323747834612,35.5323930721589));
#92410=CARTESIAN_POINT('Ctrl Pts',(2.61829831311838,-1.66756952180139,35.5854264946547));
#92411=CARTESIAN_POINT('Ctrl Pts',(2.85719574047968,-0.721444582683122,
35.6384599171505));
#92412=CARTESIAN_POINT('Ctrl Pts',(3.09609316784096,0.22468035643506,35.6914933396462));
#92413=CARTESIAN_POINT('Ctrl Pts',(2.81833118175345,1.30126227812671,35.744526762142));
#92414=CARTESIAN_POINT('Ctrl Pts',(2.15151604116683,2.01371013552097,35.7975601846377));
#92415=CARTESIAN_POINT('Ctrl Pts',(1.48470090058019,2.72615799291525,35.8505936071335));
#92416=CARTESIAN_POINT('Ctrl Pts',(0.428832605494414,3.07447178601207,35.9036270296292));
#92417=CARTESIAN_POINT('Ctrl Pts',(-0.53101381644764,2.89863314547388,35.956660452125));
#92418=CARTESIAN_POINT('Ctrl Pts',(-1.49086023838975,2.72279450493568,36.0096938746208));
#92419=CARTESIAN_POINT('Ctrl Pts',(-2.35468478718815,2.02280343076241,36.0627272971166));
#92420=CARTESIAN_POINT('Ctrl Pts',(-2.72563899335359,1.12024187709997,36.1157607196123));
#92421=CARTESIAN_POINT('Ctrl Pts',(-2.87034391332007,0.768163115849085,
36.1364484407117));
#92422=CARTESIAN_POINT('Ctrl Pts',(-2.94004927918245,0.385259420894169,
36.1571361618111));
#92423=CARTESIAN_POINT('Ctrl Pts',(-2.9380797671204,0.00166795251978762,
36.1778238829105));
#92424=CARTESIAN_POINT('Origin',(0.,0.,0.));
#92425=CARTESIAN_POINT('',(-2.94020610685266,-0.00256655506160552,37.3221761170895));
#92426=CARTESIAN_POINT('',(-2.93944817876675,-0.00236948266595389,37.1778238829104));
#92427=CARTESIAN_POINT('',(-2.942,-3.60291088309151E-16,0.));
#92428=CARTESIAN_POINT('Ctrl Pts',(-2.94020610685266,-0.00256655506160552,
37.3221761170895));
#92429=CARTESIAN_POINT('Ctrl Pts',(-2.93446364090639,0.688981411203281,
37.2848118502887));
#92430=CARTESIAN_POINT('Ctrl Pts',(-2.69086624171657,1.3841706554978,37.2474475834878));
#92431=CARTESIAN_POINT('Ctrl Pts',(-2.24570395761129,1.90809717147404,37.210083316687));
#92432=CARTESIAN_POINT('Ctrl Pts',(-1.61399794560321,2.65157329649626,37.1570616820716));
#92433=CARTESIAN_POINT('Ctrl Pts',(-0.576402102409894,3.05017883597682,
37.1040400474562));
#92434=CARTESIAN_POINT('Ctrl Pts',(0.390597011231107,2.92086546349461,37.0510184128408));
#92435=CARTESIAN_POINT('Ctrl Pts',(1.35759612487211,2.7915520910124,36.9979967782254));
#92436=CARTESIAN_POINT('Ctrl Pts',(2.25399850896079,2.13431980656741,36.94497514361));
#92437=CARTESIAN_POINT('Ctrl Pts',(2.66815670766614,1.25098395847206,36.8919535089947));
#92438=CARTESIAN_POINT('Ctrl Pts',(3.08231490637149,0.367648110376697,36.8389318743793));
#92439=CARTESIAN_POINT('Ctrl Pts',(3.0142289196935,-0.74179130136904,36.7859102397639));
#92440=CARTESIAN_POINT('Ctrl Pts',(2.49516531239286,-1.56785558800856,36.7328886051485));
#92441=CARTESIAN_POINT('Ctrl Pts',(1.97610170509222,-2.39391987464807,36.6798669705331));
#92442=CARTESIAN_POINT('Ctrl Pts',(1.00606047716893,-2.93660903618137,36.6268453359177));
#92443=CARTESIAN_POINT('Ctrl Pts',(0.0305056418984252,-2.94670841564458,
36.5738237013023));
#92444=CARTESIAN_POINT('Ctrl Pts',(-0.945049193372081,-2.9568077951078,
36.520802066687));
#92445=CARTESIAN_POINT('Ctrl Pts',(-1.92611763598987,-2.43431739250088,
36.4677804320716));
#92446=CARTESIAN_POINT('Ctrl Pts',(-2.4621717360428,-1.61917615571939,36.4147587974562));
#92447=CARTESIAN_POINT('Ctrl Pts',(-2.77417849683287,-1.14472856386347,
36.3838979040006));
#92448=CARTESIAN_POINT('Ctrl Pts',(-2.93542572807573,-0.571138320048433,
36.3530370105451));
#92449=CARTESIAN_POINT('Ctrl Pts',(-2.93766977734024,0.00128397461115384,
36.3221761170896));
#92450=CARTESIAN_POINT('Ctrl Pts',(-2.9380797671204,0.00166795251978762,
36.1778238829105));
#92451=CARTESIAN_POINT('Ctrl Pts',(-2.93500039222214,-0.598085642118336,
36.2101695843068));
#92452=CARTESIAN_POINT('Ctrl Pts',(-2.75670459734122,-1.19952056778637,
36.2425152857032));
#92453=CARTESIAN_POINT('Ctrl Pts',(-2.41589991157505,-1.68744700733082,
36.2748609870995));
#92454=CARTESIAN_POINT('Ctrl Pts',(-1.85712276009852,-2.48744230494769,
36.3278944095953));
#92455=CARTESIAN_POINT('Ctrl Pts',(-0.861484593612878,-2.98230086702986,
36.3809278320911));
#92456=CARTESIAN_POINT('Ctrl Pts',(0.113609802286804,-2.94468038980845,
36.4339612545869));
#92457=CARTESIAN_POINT('Ctrl Pts',(1.08870419818649,-2.90705991258703,36.4869946770826));
#92458=CARTESIAN_POINT('Ctrl Pts',(2.04325482350024,-2.33696039606203,36.5400280995784));
#92459=CARTESIAN_POINT('Ctrl Pts',(2.5387328644398,-1.49629048928052,36.5930615220741));
#92460=CARTESIAN_POINT('Ctrl Pts',(3.03421090537933,-0.655620582499062,
36.6460949445699));
#92461=CARTESIAN_POINT('Ctrl Pts',(3.07061636194475,0.455619714538897,36.6991283670656));
#92462=CARTESIAN_POINT('Ctrl Pts',(2.6312242524958,1.32691699754582,36.7521617895614));
#92463=CARTESIAN_POINT('Ctrl Pts',(2.19183214304681,2.19821428055281,36.8051952120572));
#92464=CARTESIAN_POINT('Ctrl Pts',(1.27664246758345,2.82956854952869,36.8582286345529));
#92465=CARTESIAN_POINT('Ctrl Pts',(0.306101279074561,2.93093019231898,36.9112620570487));
#92466=CARTESIAN_POINT('Ctrl Pts',(-0.66443990943427,3.03229183510927,36.9642954795444));
#92467=CARTESIAN_POINT('Ctrl Pts',(-1.69033261098858,2.60366085171396,37.0173289020402));
#92468=CARTESIAN_POINT('Ctrl Pts',(-2.30027284489196,1.84195402340849,37.070362324536));
#92469=CARTESIAN_POINT('Ctrl Pts',(-2.71224655861185,1.32747215554647,37.1061828439941));
#92470=CARTESIAN_POINT('Ctrl Pts',(-2.93445875073954,0.661037879533799,
37.1420033634523));
#92471=CARTESIAN_POINT('Ctrl Pts',(-2.93944817876675,-0.00236948266595389,
37.1778238829104));
#92472=CARTESIAN_POINT('Origin',(0.,0.,0.));
#92473=CARTESIAN_POINT('',(-2.94685588500563,-0.000157196364489465,38.3221761170895));
#92474=CARTESIAN_POINT('',(-2.94666346659597,-0.000711517969463661,38.1778238829105));
#92475=CARTESIAN_POINT('',(-2.942,-3.60291088309151E-16,0.));
#92476=CARTESIAN_POINT('Ctrl Pts',(-2.94685588500563,-0.000157196364489465,
38.3221761170895));
#92477=CARTESIAN_POINT('Ctrl Pts',(-2.94610829565176,0.967108386057703,
38.2696083246476));
#92478=CARTESIAN_POINT('Ctrl Pts',(-2.42386605731926,1.93506569372811,38.2170405322057));
#92479=CARTESIAN_POINT('Ctrl Pts',(-1.61474814978403,2.46507798939248,38.1644727397639));
#92480=CARTESIAN_POINT('Ctrl Pts',(-0.798644751462322,2.99966612743237,
38.1114511051485));
#92481=CARTESIAN_POINT('Ctrl Pts',(0.309309160682091,3.08871464499743,38.0584294705331));
#92482=CARTESIAN_POINT('Ctrl Pts',(1.20031707159314,2.69133052757559,38.0054078359177));
#92483=CARTESIAN_POINT('Ctrl Pts',(2.09132498250417,2.29394641015376,37.9523862013024));
#92484=CARTESIAN_POINT('Ctrl Pts',(2.76538689218184,1.41012965774507,37.8993645666869));
#92485=CARTESIAN_POINT('Ctrl Pts',(2.91295892265725,0.445748130595928,37.8463429320716));
#92486=CARTESIAN_POINT('Ctrl Pts',(3.06053095313266,-0.518633396553271,
37.7933212974562));
#92487=CARTESIAN_POINT('Ctrl Pts',(2.68161310440574,-1.56357969844294,37.7402996628408));
#92488=CARTESIAN_POINT('Ctrl Pts',(1.95021268744095,-2.20922872395834,37.6872780282254));
#92489=CARTESIAN_POINT('Ctrl Pts',(1.2188122704762,-2.8548777494737,37.63425639361));
#92490=CARTESIAN_POINT('Ctrl Pts',(0.134929285273619,-3.10122949861485,
37.5812347589946));
#92491=CARTESIAN_POINT('Ctrl Pts',(-0.803693645883662,-2.8351538943388,
37.5282131243792));
#92492=CARTESIAN_POINT('Ctrl Pts',(-1.74231657704105,-2.56907829006272,
37.4751914897639));
#92493=CARTESIAN_POINT('Ctrl Pts',(-2.5356794541531,-1.79057533236931,37.4221698551485));
#92494=CARTESIAN_POINT('Ctrl Pts',(-2.81945280229766,-0.857150498240605,
37.3691482205331));
#92495=CARTESIAN_POINT('Ctrl Pts',(-2.90325149541768,-0.581508751976585,
37.3534908527186));
#92496=CARTESIAN_POINT('Ctrl Pts',(-2.94261246750633,-0.292357357779581,
37.3378334849041));
#92497=CARTESIAN_POINT('Ctrl Pts',(-2.94020610685266,-0.00256655506160552,
37.3221761170895));
#92498=CARTESIAN_POINT('Ctrl Pts',(-2.93944817876675,-0.00236948266595389,
37.1778238829104));
#92499=CARTESIAN_POINT('Ctrl Pts',(-2.94184575820291,-0.321157897035699,
37.195036785948));
#92500=CARTESIAN_POINT('Ctrl Pts',(-2.89408422772848,-0.639247363929739,
37.2122496889856));
#92501=CARTESIAN_POINT('Ctrl Pts',(-2.79311648590866,-0.939441366687316,
37.2294625920232));
#92502=CARTESIAN_POINT('Ctrl Pts',(-2.48203212676952,-1.86434725526213,
37.282496014519));
#92503=CARTESIAN_POINT('Ctrl Pts',(-1.66587564223875,-2.61937635919603,
37.3355294370148));
#92504=CARTESIAN_POINT('Ctrl Pts',(-0.719596380769393,-2.85766177741203,
37.3885628595105));
#92505=CARTESIAN_POINT('Ctrl Pts',(0.226682880699967,-3.09594719562802,
37.4415962820063));
#92506=CARTESIAN_POINT('Ctrl Pts',(1.30308491910795,-2.81748892812605,37.4946297045021));
#92507=CARTESIAN_POINT('Ctrl Pts',(2.01510132751988,-2.15021311156027,37.5476631269978));
#92508=CARTESIAN_POINT('Ctrl Pts',(2.72711773593179,-1.4829372949945,37.6006965494936));
#92509=CARTESIAN_POINT('Ctrl Pts',(3.07474851434775,-0.426843929364974,
37.6537299719893));
#92510=CARTESIAN_POINT('Ctrl Pts',(2.89828907628243,0.532888558330936,37.7067633944851));
#92511=CARTESIAN_POINT('Ctrl Pts',(2.72182963821711,1.49262104602685,37.7597968169808));
#92512=CARTESIAN_POINT('Ctrl Pts',(2.02127998367054,2.3559926557891,37.8128302394766));
#92513=CARTESIAN_POINT('Ctrl Pts',(1.11847868344357,2.72636300223951,37.8658636619724));
#92514=CARTESIAN_POINT('Ctrl Pts',(0.215677383216621,3.0967333486899,37.9188970844681));
#92515=CARTESIAN_POINT('Ctrl Pts',(-0.88937556269077,2.97410243182843,37.9719305069639));
#92516=CARTESIAN_POINT('Ctrl Pts',(-1.68900927261872,2.41480795557453,38.0249639294596));
#92517=CARTESIAN_POINT('Ctrl Pts',(-2.45727933028583,1.87745042025602,38.0759172472766));
#92518=CARTESIAN_POINT('Ctrl Pts',(-2.94361891960952,0.937011653288061,
38.1268705650935));
#92519=CARTESIAN_POINT('Ctrl Pts',(-2.94666346659597,-0.000711517969463661,
38.1778238829105));
#92520=CARTESIAN_POINT('Origin',(0.,0.,0.));
#92521=CARTESIAN_POINT('',(-2.940678661329,0.00264606062658684,39.3221761170896));
#92522=CARTESIAN_POINT('',(-2.9416064078984,0.00271891336319057,39.1778238829104));
#92523=CARTESIAN_POINT('',(-2.942,-3.60291088309151E-16,0.));
#92524=CARTESIAN_POINT('Ctrl Pts',(-2.940678661329,0.00264606062658684,
39.3221761170896));
#92525=CARTESIAN_POINT('Ctrl Pts',(-2.94304410098273,0.275526082595591,
39.307426433622));
#92526=CARTESIAN_POINT('Ctrl Pts',(-2.90819151789947,0.547813233612533,
39.2926767501545));
#92527=CARTESIAN_POINT('Ctrl Pts',(-2.8337047940856,0.808788118727334,39.277927066687));
#92528=CARTESIAN_POINT('Ctrl Pts',(-2.56594258329314,1.74693130212563,39.2249054320716));
#92529=CARTESIAN_POINT('Ctrl Pts',(-1.78601493030073,2.53889365351255,39.1718837974562));
#92530=CARTESIAN_POINT('Ctrl Pts',(-0.852081563133812,2.82098884981591,
39.1188621628408));
#92531=CARTESIAN_POINT('Ctrl Pts',(0.0818518040331556,3.10308404611928,
39.0658405282254));
#92532=CARTESIAN_POINT('Ctrl Pts',(1.16979088537462,2.87531208733904,39.01281889361));
#92533=CARTESIAN_POINT('Ctrl Pts',(1.91213041111138,2.24227080699929,38.9597972589946));
#92534=CARTESIAN_POINT('Ctrl Pts',(2.65446993684809,1.60922952665959,38.9067756243793));
#92535=CARTESIAN_POINT('Ctrl Pts',(3.05120990698014,0.570918924760407,38.8537539897639));
#92536=CARTESIAN_POINT('Ctrl Pts',(2.92015870507473,-0.395846205229427,
38.8007323551485));
#92537=CARTESIAN_POINT('Ctrl Pts',(2.7891075031693,-1.36261133521934,38.7477107205331));
#92538=CARTESIAN_POINT('Ctrl Pts',(2.13026512922635,-2.25783099329993,38.6946890859177));
#92539=CARTESIAN_POINT('Ctrl Pts',(1.246186319647,-2.67040085712668,38.6416674513023));
#92540=CARTESIAN_POINT('Ctrl Pts',(0.362107510067668,-3.08297072095342,
38.5886458166869));
#92541=CARTESIAN_POINT('Ctrl Pts',(-0.747207735148027,-3.01289079052633,
38.5356241820716));
#92542=CARTESIAN_POINT('Ctrl Pts',(-1.57233774721256,-2.49234329290906,
38.4826025474562));
#92543=CARTESIAN_POINT('Ctrl Pts',(-2.39746775927708,-1.97179579529179,
38.4295809128408));
#92544=CARTESIAN_POINT('Ctrl Pts',(-2.93841253819042,-1.00078073048434,
38.3765592782254));
#92545=CARTESIAN_POINT('Ctrl Pts',(-2.94675848539759,-0.0252093188232366,
38.32353764361));
#92546=CARTESIAN_POINT('Ctrl Pts',(-2.94682992308237,-0.0168588510740105,
38.3230838014365));
#92547=CARTESIAN_POINT('Ctrl Pts',(-2.94686233929183,-0.00850804949871229,
38.322629959263));
#92548=CARTESIAN_POINT('Ctrl Pts',(-2.94685588500563,-0.000157196364489465,
38.3221761170895));
#92549=CARTESIAN_POINT('Ctrl Pts',(-2.94666346659597,-0.000711517969463661,
38.1778238829105));
#92550=CARTESIAN_POINT('Ctrl Pts',(-2.94678775637145,-0.0389928790179145,
38.1799039875893));
#92551=CARTESIAN_POINT('Ctrl Pts',(-2.94610659763157,-0.0772697143163753,
38.1819840922681));
#92552=CARTESIAN_POINT('Ctrl Pts',(-2.94460629035526,-0.11551441511034,
38.1840641969469));
#92553=CARTESIAN_POINT('Ctrl Pts',(-2.90635512421528,-1.09058427389499,
38.2370976194427));
#92554=CARTESIAN_POINT('Ctrl Pts',(-2.33563831798667,-2.0447659558179,38.2901310419384));
#92555=CARTESIAN_POINT('Ctrl Pts',(-1.4946481089457,-2.53970014287575,38.3431644644342));
#92556=CARTESIAN_POINT('Ctrl Pts',(-0.653657899904804,-3.03463432993356,
38.3961978869299));
#92557=CARTESIAN_POINT('Ctrl Pts',(0.457605711948423,-3.07032102212643,
38.4492313094257));
#92558=CARTESIAN_POINT('Ctrl Pts',(1.32861861129864,-2.63036544438391,38.5022647319215));
#92559=CARTESIAN_POINT('Ctrl Pts',(2.19963151064891,-2.19040986664136,38.5552981544172));
#92560=CARTESIAN_POINT('Ctrl Pts',(2.83039369749616,-1.27481201896335,38.608331576913));
#92561=CARTESIAN_POINT('Ctrl Pts',(2.93112756733703,-0.304205472164799,
38.6613649994088));
#92562=CARTESIAN_POINT('Ctrl Pts',(3.03186143717789,0.666401074633756,38.7143984219045));
#92563=CARTESIAN_POINT('Ctrl Pts',(2.60256699001241,1.69201632055282,38.7674318444003));
#92564=CARTESIAN_POINT('Ctrl Pts',(1.84046580811073,2.30146375041481,38.820465266896));
#92565=CARTESIAN_POINT('Ctrl Pts',(1.07836462620906,2.91091118027678,38.8734986893918));
#92566=CARTESIAN_POINT('Ctrl Pts',(-0.0165432904288121,3.10419079408163,
38.9265321118876));
#92567=CARTESIAN_POINT('Ctrl Pts',(-0.941247774340326,2.79250826544837,
38.9795655343833));
#92568=CARTESIAN_POINT('Ctrl Pts',(-1.86595225825184,2.4808257368151,39.0325989568791));
#92569=CARTESIAN_POINT('Ctrl Pts',(-2.62045330943702,1.66418106574372,39.0856323793748));
#92570=CARTESIAN_POINT('Ctrl Pts',(-2.85812661881906,0.717747877806678,
39.1386658018706));
#92571=CARTESIAN_POINT('Ctrl Pts',(-2.9166232565481,0.484809818950013,39.1517184955505));
#92572=CARTESIAN_POINT('Ctrl Pts',(-2.94381250888963,0.244009683839058,
39.1647711892305));
#92573=CARTESIAN_POINT('Ctrl Pts',(-2.9416064078984,0.00271891336319057,
39.1778238829104));
#92574=CARTESIAN_POINT('Origin',(0.,0.,0.));
#92575=CARTESIAN_POINT('',(-2.93747162631023,-0.00103124720635284,40.3221761170895));
#92576=CARTESIAN_POINT('',(-2.93720961253691,-0.000509911063724039,40.1778238829105));
#92577=CARTESIAN_POINT('',(-2.942,-3.60291088309151E-16,0.));
#92578=CARTESIAN_POINT('Ctrl Pts',(-2.93747162631023,-0.00103124720635284,
40.3221761170895));
#92579=CARTESIAN_POINT('Ctrl Pts',(-2.93572901194389,0.554648497353495,
40.292222907981));
#92580=CARTESIAN_POINT('Ctrl Pts',(-2.78442048137917,1.11120814384935,40.2622696988724));
#92581=CARTESIAN_POINT('Ctrl Pts',(-2.48951322196339,1.57681482701289,40.2323164897639));
#92582=CARTESIAN_POINT('Ctrl Pts',(-1.96748351564707,2.40100789893758,40.1792948551485));
#92583=CARTESIAN_POINT('Ctrl Pts',(-0.995497750798812,2.94020654772044,
40.1262732205331));
#92584=CARTESIAN_POINT('Ctrl Pts',(-0.019912914309713,2.94679903571009,
40.0732515859177));
#92585=CARTESIAN_POINT('Ctrl Pts',(0.95567192217922,2.95339152369975,40.0202299513023));
#92586=CARTESIAN_POINT('Ctrl Pts',(1.93485583030902,2.42737785089641,39.967208316687));
#92587=CARTESIAN_POINT('Ctrl Pts',(2.46797627936023,1.61031492743918,39.9141866820716));
#92588=CARTESIAN_POINT('Ctrl Pts',(3.00109672841152,0.793252003981841,39.8611650474562));
#92589=CARTESIAN_POINT('Ctrl Pts',(3.08815371838411,-0.314860170129411,
39.8081434128408));
#92590=CARTESIAN_POINT('Ctrl Pts',(2.68916878751728,-1.20515240250397,39.7551217782254));
#92591=CARTESIAN_POINT('Ctrl Pts',(2.29018385665045,-2.09544463487851,39.70210014361));
#92592=CARTESIAN_POINT('Ctrl Pts',(1.4051570049442,-2.76791692551632,39.6490785089946));
#92593=CARTESIAN_POINT('Ctrl Pts',(0.440511796540892,-2.91375538405792,
39.5960568743793));
#92594=CARTESIAN_POINT('Ctrl Pts',(-0.52413341186236,-3.05959384259952,
39.5430352397639));
#92595=CARTESIAN_POINT('Ctrl Pts',(-1.56839697696268,-2.67879846904497,
39.4900136051485));
#92596=CARTESIAN_POINT('Ctrl Pts',(-2.2127303752166,-1.94623877456288,39.4369919705331));
#92597=CARTESIAN_POINT('Ctrl Pts',(-2.67782158788453,-1.41746426499749,
39.3987200193853));
#92598=CARTESIAN_POINT('Ctrl Pts',(-2.93454090311404,-0.705413260986069,
39.3604480682374));
#92599=CARTESIAN_POINT('Ctrl Pts',(-2.940678661329,0.00264606062658684,
39.3221761170896));
#92600=CARTESIAN_POINT('Ctrl Pts',(-2.9416064078984,0.00271891336319057,
39.1778238829104));
#92601=CARTESIAN_POINT('Ctrl Pts',(-2.93484906511283,-0.736360781348812,
39.2178046117262));
#92602=CARTESIAN_POINT('Ctrl Pts',(-2.65230090246203,-1.4800436773904,39.257785340542));
#92603=CARTESIAN_POINT('Ctrl Pts',(-2.14890928239526,-2.01649167648507,
39.2977660693579));
#92604=CARTESIAN_POINT('Ctrl Pts',(-1.48117306901056,-2.72807633803696,
39.3507994918536));
#92605=CARTESIAN_POINT('Ctrl Pts',(-0.424855074662313,-3.07502395633807,
39.4038329143494));
#92606=CARTESIAN_POINT('Ctrl Pts',(0.534763077275774,-2.89794379456894,
39.4568663368451));
#92607=CARTESIAN_POINT('Ctrl Pts',(1.49438122921394,-2.7208636327998,39.5098997593409));
#92608=CARTESIAN_POINT('Ctrl Pts',(2.35729953874191,-2.01975569096034,39.5629331818367));
#92609=CARTESIAN_POINT('Ctrl Pts',(2.72708587052995,-1.11671502186279,39.6159666043324));
#92610=CARTESIAN_POINT('Ctrl Pts',(3.09687220231795,-0.213674352765307,
39.6690000268282));
#92611=CARTESIAN_POINT('Ctrl Pts',(2.97352655636609,0.891299043590286,39.7220334493239));
#92612=CARTESIAN_POINT('Ctrl Pts',(2.41371498932006,1.69057083129627,39.7750668718197));
#92613=CARTESIAN_POINT('Ctrl Pts',(1.85390342227401,2.48984261900228,39.8281002943154));
#92614=CARTESIAN_POINT('Ctrl Pts',(0.857625934133788,2.98341279805871,39.8811337168112));
#92615=CARTESIAN_POINT('Ctrl Pts',(-0.117418979607592,2.9445309590028,39.934167139307));
#92616=CARTESIAN_POINT('Ctrl Pts',(-1.09246389334897,2.9056491199469,39.9872005618027));
#92617=CARTESIAN_POINT('Ctrl Pts',(-2.04627623269148,2.33431526277864,40.0402339842985));
#92618=CARTESIAN_POINT('Ctrl Pts',(-2.54066635880802,1.4930051033132,40.0932674067943));
#92619=CARTESIAN_POINT('Ctrl Pts',(-2.80341819166967,1.04587686444428,40.121452898833));
#92620=CARTESIAN_POINT('Ctrl Pts',(-2.93640312718175,0.522492001279797,
40.1496383908717));
#92621=CARTESIAN_POINT('Ctrl Pts',(-2.93720961253691,-0.000509911063724039,
40.1778238829105));
#92622=CARTESIAN_POINT('Origin',(0.,0.,0.));
#92623=CARTESIAN_POINT('',(-2.94447081660296,-0.00226074840892904,41.3221761170895));
#92624=CARTESIAN_POINT('',(-2.94348373544085,-0.00254093421303839,41.1778238829105));
#92625=CARTESIAN_POINT('',(-2.942,-3.60291088309151E-16,0.));
#92626=CARTESIAN_POINT('Ctrl Pts',(-2.94447081660296,-0.00226074840892904,
41.3221761170895));
#92627=CARTESIAN_POINT('Ctrl Pts',(-2.93739656150027,0.830413800742868,
41.27701938234));
#92628=CARTESIAN_POINT('Ctrl Pts',(-2.56714021706357,1.6685901412572,41.2318626475904));
#92629=CARTESIAN_POINT('Ctrl Pts',(-1.94225857440192,2.21622487829653,41.1867059128408));
#92630=CARTESIAN_POINT('Ctrl Pts',(-1.20854196892092,2.85924056778373,41.1336842782254));
#92631=CARTESIAN_POINT('Ctrl Pts',(-0.123780426189747,3.10169449191821,
41.08066264361));
#92632=CARTESIAN_POINT('Ctrl Pts',(0.813879978798057,2.83224653960949,41.0276410089946));
#92633=CARTESIAN_POINT('Ctrl Pts',(1.75154038378581,2.56279858730078,40.9746193743793));
#92634=CARTESIAN_POINT('Ctrl Pts',(2.54209965103021,1.78144875854892,40.9215977397639));
#92635=CARTESIAN_POINT('Ctrl Pts',(2.82251578418982,0.847009875395524,40.8685761051485));
#92636=CARTESIAN_POINT('Ctrl Pts',(3.10293191734945,-0.0874290077579226,
40.8155544705331));
#92637=CARTESIAN_POINT('Ctrl Pts',(2.87320491642424,-1.17495694531292,40.7625328359177));
#92638=CARTESIAN_POINT('Ctrl Pts',(2.23883041277921,-1.91615747365217,40.7095112013023));
#92639=CARTESIAN_POINT('Ctrl Pts',(1.60445590913423,-2.65735800199139,40.656489566687));
#92640=CARTESIAN_POINT('Ctrl Pts',(0.565433902769473,-3.05223112111489,
40.6034679320716));
#92641=CARTESIAN_POINT('Ctrl Pts',(-0.401094120455098,-2.91944251314435,
40.5504462974562));
#92642=CARTESIAN_POINT('Ctrl Pts',(-1.36762214367972,-2.7866539051738,40.4974246628408));
#92643=CARTESIAN_POINT('Ctrl Pts',(-2.26165618376416,-2.12620357010914,
40.4444030282254));
#92644=CARTESIAN_POINT('Ctrl Pts',(-2.67263637991414,-1.24138465504358,
40.39138139361));
#92645=CARTESIAN_POINT('Ctrl Pts',(-2.8514438819544,-0.856421434326478,
40.3683129681032));
#92646=CARTESIAN_POINT('Ctrl Pts',(-2.9388136985253,-0.428987288463168,
40.3452445425964));
#92647=CARTESIAN_POINT('Ctrl Pts',(-2.93747162631023,-0.00103124720635284,
40.3221761170895));
#92648=CARTESIAN_POINT('Ctrl Pts',(-2.93720961253691,-0.000509911063724039,
40.1778238829105));
#92649=CARTESIAN_POINT('Ctrl Pts',(-2.93792059859996,-0.461580987238054,
40.2026718133675));
#92650=CARTESIAN_POINT('Ctrl Pts',(-2.83590334183077,-0.922354436493001,
40.2275197438245));
#92651=CARTESIAN_POINT('Ctrl Pts',(-2.62950553583792,-1.33031966921331,
40.2523676742815));
#92652=CARTESIAN_POINT('Ctrl Pts',(-2.18898667386072,-2.20104782051176,
40.3054010967773));
#92653=CARTESIAN_POINT('Ctrl Pts',(-1.27298103701576,-2.83121766134602,
40.358434519273));
#92654=CARTESIAN_POINT('Ctrl Pts',(-0.30230953798844,-2.93132371609471,
40.4114679417688));
#92655=CARTESIAN_POINT('Ctrl Pts',(0.668361961038936,-3.0314297708434,40.4645013642645));
#92656=CARTESIAN_POINT('Ctrl Pts',(1.69369932224868,-2.60147203950645,40.5175347867603));
#92657=CARTESIAN_POINT('Ctrl Pts',(2.30265369310215,-1.83897682283957,40.5705682092561));
#92658=CARTESIAN_POINT('Ctrl Pts',(2.91160806395557,-1.07648160617274,40.6236016317518));
#92659=CARTESIAN_POINT('Ctrl Pts',(3.10417944445277,0.01855109582397,40.6766350542476));
#92660=CARTESIAN_POINT('Ctrl Pts',(2.79189887672024,0.943053788214828,40.7296684767434));
#92661=CARTESIAN_POINT('Ctrl Pts',(2.47961830898771,1.86755648060569,40.7827018992391));
#92662=CARTESIAN_POINT('Ctrl Pts',(1.66248579302546,2.62152916339069,40.8357353217349));
#92663=CARTESIAN_POINT('Ctrl Pts',(0.715899074568479,2.85859026450628,40.8887687442307));
#92664=CARTESIAN_POINT('Ctrl Pts',(-0.230687643888503,3.09565136562187,
40.9418021667264));
#92665=CARTESIAN_POINT('Ctrl Pts',(-1.30672856484022,2.81580088506805,40.9948355892222));
#92666=CARTESIAN_POINT('Ctrl Pts',(-2.01788118183506,2.14760455421709,41.0478690117179));
#92667=CARTESIAN_POINT('Ctrl Pts',(-2.59875856312033,1.60181434607681,41.0911873021154));
#92668=CARTESIAN_POINT('Ctrl Pts',(-2.9361896045507,0.796927381949951,41.1345055925129));
#92669=CARTESIAN_POINT('Ctrl Pts',(-2.94348373544085,-0.00254093421303839,
41.1778238829105));
#92670=CARTESIAN_POINT('Origin',(0.,0.,0.));
#92671=CARTESIAN_POINT('',(-2.94473630969457,0.00215967812386454,42.3221761170896));
#92672=CARTESIAN_POINT('',(-2.94562033411779,0.00171615163861752,42.1778238829104));
#92673=CARTESIAN_POINT('',(-2.942,-3.60291088309151E-16,0.));
#92674=CARTESIAN_POINT('Ctrl Pts',(-2.94473630969457,0.00215967812386454,
42.3221761170896));
#92675=CARTESIAN_POINT('Ctrl Pts',(-2.94584995717871,0.137449629621458,
42.3148374913143));
#92676=CARTESIAN_POINT('Ctrl Pts',(-2.93733632589731,0.27259864460851,42.3074988655391));
#92677=CARTESIAN_POINT('Ctrl Pts',(-2.91871689001713,0.406340739954757,
42.3001602397639));
#92678=CARTESIAN_POINT('Ctrl Pts',(-2.78419130495222,1.37262853406591,42.2471386051485));
#92679=CARTESIAN_POINT('Ctrl Pts',(-2.12213514233659,2.26547406799627,42.1941169705331));
#92680=CARTESIAN_POINT('Ctrl Pts',(-1.23657898017349,2.67486326880671,42.1410953359177));
#92681=CARTESIAN_POINT('Ctrl Pts',(-0.351022818010432,3.08425246961713,
42.0880737013023));
#92682=CARTESIAN_POINT('Ctrl Pts',(0.758033343700066,3.0101853373077,42.035052066687));
#92683=CARTESIAN_POINT('Ctrl Pts',(1.58128681294659,2.48667510869825,41.9820304320716));
#92684=CARTESIAN_POINT('Ctrl Pts',(2.40454028219315,1.96316488008877,41.9290087974562));
#92685=CARTESIAN_POINT('Ctrl Pts',(2.94199105897571,0.990211555179222,41.8759871628408));
#92686=CARTESIAN_POINT('Ctrl Pts',(2.94683006645108,0.0146164454682759,
41.8229655282254));
#92687=CARTESIAN_POINT('Ctrl Pts',(2.95166907392646,-0.960978664242615,
41.76994389361));
#92688=CARTESIAN_POINT('Ctrl Pts',(2.4238963120947,-1.9392155587549,41.7169222589946));
#92689=CARTESIAN_POINT('Ctrl Pts',(1.60587650300619,-2.47086659658324,41.6639006243793));
#92690=CARTESIAN_POINT('Ctrl Pts',(0.787856693917635,-3.00251763441161,
41.6108789897639));
#92691=CARTESIAN_POINT('Ctrl Pts',(-0.320410162427715,-3.08758281555597,
41.5578573551485));
#92692=CARTESIAN_POINT('Ctrl Pts',(-1.20998384019564,-2.68699836015649,
41.5048357205331));
#92693=CARTESIAN_POINT('Ctrl Pts',(-2.09955751796362,-2.28641390475698,
41.4518140859177));
#92694=CARTESIAN_POINT('Ctrl Pts',(-2.77043801715415,-1.40017981281356,
41.3987924513023));
#92695=CARTESIAN_POINT('Ctrl Pts',(-2.91454243263391,-0.43527403942188,
41.3457708166869));
#92696=CARTESIAN_POINT('Ctrl Pts',(-2.93591798633362,-0.292145911767843,
41.3379059168211));
#92697=CARTESIAN_POINT('Ctrl Pts',(-2.94570293199651,-0.147286777996668,
41.3300410169553));
#92698=CARTESIAN_POINT('Ctrl Pts',(-2.94447081660296,-0.00226074840892904,
41.3221761170895));
#92699=CARTESIAN_POINT('Ctrl Pts',(-2.94348373544085,-0.00254093421303839,
41.1778238829105));
#92700=CARTESIAN_POINT('Ctrl Pts',(-2.94511961359969,-0.181840260862772,
41.1875390150087));
#92701=CARTESIAN_POINT('Ctrl Pts',(-2.93015010916664,-0.360867037792384,
41.197254147107));
#92702=CARTESIAN_POINT('Ctrl Pts',(-2.89759730047774,-0.536637372498586,
41.2069692792052));
#92703=CARTESIAN_POINT('Ctrl Pts',(-2.71989648908757,-1.49614078721505,
41.260002701701));
#92704=CARTESIAN_POINT('Ctrl Pts',(-2.01823055326929,-2.3586054354999,41.3130361241967));
#92705=CARTESIAN_POINT('Ctrl Pts',(-1.11495089309546,-2.7278075979225,41.3660695466925));
#92706=CARTESIAN_POINT('Ctrl Pts',(-0.211671232921631,-3.0970097603451,
41.4191029691882));
#92707=CARTESIAN_POINT('Ctrl Pts',(0.893222151607806,-2.97294943690546,
41.472136391684));
#92708=CARTESIAN_POINT('Ctrl Pts',(1.69213168271017,-2.41262101326887,41.5251698141798));
#92709=CARTESIAN_POINT('Ctrl Pts',(2.49104121381259,-1.85229258963225,41.5782032366755));
#92710=CARTESIAN_POINT('Ctrl Pts',(2.9839668914879,-0.855696065798763,41.6312366591713));
#92711=CARTESIAN_POINT('Ctrl Pts',(2.94445439578259,0.119323494981688,41.684270081667));
#92712=CARTESIAN_POINT('Ctrl Pts',(2.90494190007729,1.09434305576208,41.7373035041628));
#92713=CARTESIAN_POINT('Ctrl Pts',(2.33299123099132,2.04778565348939,41.7903369266586));
#92714=CARTESIAN_POINT('Ctrl Pts',(1.49136147307008,2.54163151183257,41.8433703491543));
#92715=CARTESIAN_POINT('Ctrl Pts',(0.649731715148849,3.03547737017575,41.8964037716501));
#92716=CARTESIAN_POINT('Ctrl Pts',(-0.461577131607709,3.06972648913485,
41.9494371941458));
#92717=CARTESIAN_POINT('Ctrl Pts',(-1.33202017057833,2.6286445272175,42.0024706166416));
#92718=CARTESIAN_POINT('Ctrl Pts',(-2.20246320954901,2.18756256530014,42.0555040391373));
#92719=CARTESIAN_POINT('Ctrl Pts',(-2.83204044073378,1.27114952250626,42.1085374616331));
#92720=CARTESIAN_POINT('Ctrl Pts',(-2.93151863851002,0.300413477338171,
42.1615708841289));
#92721=CARTESIAN_POINT('Ctrl Pts',(-2.94168090317986,0.201247259653578,
42.1669885503894));
#92722=CARTESIAN_POINT('Ctrl Pts',(-2.94631116750731,0.101514138713564,
42.1724062166499));
#92723=CARTESIAN_POINT('Ctrl Pts',(-2.94562033411779,0.00171615163861752,
42.1778238829104));
#92724=CARTESIAN_POINT('Origin',(0.,0.,0.));
#92725=CARTESIAN_POINT('',(-2.93758116933064,0.00117923657373634,43.3221761170895));
#92726=CARTESIAN_POINT('',(-2.93812373739311,0.00170130757060122,43.1778238829105));
#92727=CARTESIAN_POINT('',(-2.942,-3.60291088309151E-16,0.));
#92728=CARTESIAN_POINT('Ctrl Pts',(-2.93758116933064,0.00117923657373634,
43.3221761170895));
#92729=CARTESIAN_POINT('Ctrl Pts',(-2.93908400894455,0.419333117468769,
43.2996339656733));
#92730=CARTESIAN_POINT('Ctrl Pts',(-2.85580724763625,0.836915777227387,
43.277091814257));
#92731=CARTESIAN_POINT('Ctrl Pts',(-2.68481925250477,1.21481136906017,43.2545496628408));
#92732=CARTESIAN_POINT('Ctrl Pts',(-2.28263656665219,2.10366361847272,43.2015280282254));
#92733=CARTESIAN_POINT('Ctrl Pts',(-1.39519809743223,2.77295015895075,43.1485063936101));
#92734=CARTESIAN_POINT('Ctrl Pts',(-0.430034876159872,2.91532006584257,
43.0954847589947));
#92735=CARTESIAN_POINT('Ctrl Pts',(0.535128345112486,3.05768997273439,43.0424631243793));
#92736=CARTESIAN_POINT('Ctrl Pts',(1.57801631843724,2.67314324604,42.9894414897639));
#92737=CARTESIAN_POINT('Ctrl Pts',(2.21971222190921,1.93827209981602,42.9364198551485));
#92738=CARTESIAN_POINT('Ctrl Pts',(2.86140812538118,1.20340095359203,42.8833982205331));
#92739=CARTESIAN_POINT('Ctrl Pts',(3.10191195900036,0.118205387838451,42.8303765859177));
#92740=CARTESIAN_POINT('Ctrl Pts',(2.83077913562125,-0.818969209646855,
42.7773549513024));
#92741=CARTESIAN_POINT('Ctrl Pts',(2.55964631224217,-1.75614380713211,42.724333316687));
#92742=CARTESIAN_POINT('Ctrl Pts',(1.77687683186485,-2.5452974363491,42.6713116820716));
#92743=CARTESIAN_POINT('Ctrl Pts',(0.841935451409881,-2.82403360048663,
42.6182900474562));
#92744=CARTESIAN_POINT('Ctrl Pts',(-0.0930059290451951,-3.10276976462418,
42.5652684128408));
#92745=CARTESIAN_POINT('Ctrl Pts',(-1.18011920957796,-2.87108846368215,
42.5122467782254));
#92746=CARTESIAN_POINT('Ctrl Pts',(-1.9201783460872,-2.23538278606508,42.45922514361));
#92747=CARTESIAN_POINT('Ctrl Pts',(-2.55780727474305,-1.68766394825522,
42.4135421347699));
#92748=CARTESIAN_POINT('Ctrl Pts',(-2.93780384448635,-0.840021438553098,
42.3678591259297));
#92749=CARTESIAN_POINT('Ctrl Pts',(-2.94473630969457,0.00215967812386454,
42.3221761170896));
#92750=CARTESIAN_POINT('Ctrl Pts',(-2.94562033411779,0.00171615163861752,
42.1778238829104));
#92751=CARTESIAN_POINT('Ctrl Pts',(-2.93954861380638,-0.875406283894391,
42.2254396391457));
#92752=CARTESIAN_POINT('Ctrl Pts',(-2.52244254972299,-1.75753937899873,
42.2730553953809));
#92753=CARTESIAN_POINT('Ctrl Pts',(-1.83748706821796,-2.30384267245614,
42.3206711516162));
#92754=CARTESIAN_POINT('Ctrl Pts',(-1.07459813578189,-2.91230372954013,
42.3737045741119));
#92755=CARTESIAN_POINT('Ctrl Pts',(0.0205588934579998,-3.10416679616593,
42.4267379966077));
#92756=CARTESIAN_POINT('Ctrl Pts',(0.944859407555178,-2.79128831997924,
42.4797714191034));
#92757=CARTESIAN_POINT('Ctrl Pts',(1.86915992165246,-2.47840984379252,42.5328048415992));
#92758=CARTESIAN_POINT('Ctrl Pts',(2.62260392060693,-1.66078982479322,42.5858382640949));
#92759=CARTESIAN_POINT('Ctrl Pts',(2.8590527142797,-0.714049971828252,42.6388716865907));
#92760=CARTESIAN_POINT('Ctrl Pts',(3.09550150795247,0.232689881136659,42.6919051090865));
#92761=CARTESIAN_POINT('Ctrl Pts',(2.81495509634351,1.30854956806729,42.7449385315822));
#92762=CARTESIAN_POINT('Ctrl Pts',(2.14629892757145,2.01926984298872,42.797971954078));
#92763=CARTESIAN_POINT('Ctrl Pts',(1.47764275879943,2.72999011791011,42.8510053765738));
#92764=CARTESIAN_POINT('Ctrl Pts',(0.420876832864394,3.07557098082247,42.9040387990695));
#92765=CARTESIAN_POINT('Ctrl Pts',(-0.538511443214592,2.89724959415391,
42.9570722215653));
#92766=CARTESIAN_POINT('Ctrl Pts',(-1.49789971929374,2.71892820748532,43.010105644061));
#92767=CARTESIAN_POINT('Ctrl Pts',(-2.35991034551675,2.01670457123563,43.0631390665568));
#92768=CARTESIAN_POINT('Ctrl Pts',(-2.72852818411529,1.11318629787948,43.1161724890526));
#92769=CARTESIAN_POINT('Ctrl Pts',(-2.87136768972636,0.76307273862408,43.1367229536719));
#92770=CARTESIAN_POINT('Ctrl Pts',(-2.94012108793881,0.382733492091749,
43.1572734182912));
#92771=CARTESIAN_POINT('Ctrl Pts',(-2.93812373739311,0.00170130757060122,
43.1778238829105));
#92772=CARTESIAN_POINT('Origin',(0.,0.,0.));
#92773=CARTESIAN_POINT('',(-2.94040227747744,-0.00260344384514166,44.3221761170895));
#92774=CARTESIAN_POINT('',(-2.93938501957473,-0.00234810359620528,44.1778238829104));
#92775=CARTESIAN_POINT('',(-2.942,-3.60291088309151E-16,0.));
#92776=CARTESIAN_POINT('Ctrl Pts',(-2.94040227747744,-0.00260344384514166,
44.3221761170895));
#92777=CARTESIAN_POINT('Ctrl Pts',(-2.93448873783951,0.695885794181435,
44.2844304400323));
#92778=CARTESIAN_POINT('Ctrl Pts',(-2.6854279089453,1.39816509258832,44.246684762975));
#92779=CARTESIAN_POINT('Ctrl Pts',(-2.23192793799287,1.92419301542808,44.2089390859177));
#92780=CARTESIAN_POINT('Ctrl Pts',(-1.59489314003593,2.66310836936333,44.1559174513024));
#92781=CARTESIAN_POINT('Ctrl Pts',(-0.554458396646493,3.05424396561426,
44.102895816687));
#92782=CARTESIAN_POINT('Ctrl Pts',(0.411586046778129,2.91798183803642,44.0498741820716));
#92783=CARTESIAN_POINT('Ctrl Pts',(1.37763049020286,2.78171971045856,43.9968525474562));
#92784=CARTESIAN_POINT('Ctrl Pts',(2.2692846336627,2.11805985905179,43.9438309128408));
#92785=CARTESIAN_POINT('Ctrl Pts',(2.67708151661102,1.23176931056174,43.8908092782254));
#92786=CARTESIAN_POINT('Ctrl Pts',(3.08487839955926,0.345478762071852,43.83778764361));
#92787=CARTESIAN_POINT('Ctrl Pts',(3.00881802199609,-0.763442483501333,
43.7847660089947));
#92788=CARTESIAN_POINT('Ctrl Pts',(2.48382896228187,-1.58575369056714,43.7317443743793));
#92789=CARTESIAN_POINT('Ctrl Pts',(1.95883990256756,-2.40806489763308,43.6787227397639));
#92790=CARTESIAN_POINT('Ctrl Pts',(0.984922160702103,-2.94376606619166,
43.6257011051484));
#92791=CARTESIAN_POINT('Ctrl Pts',(0.00931992940853922,-2.94685157752022,
43.572679470533));
#92792=CARTESIAN_POINT('Ctrl Pts',(-0.966282301884858,-2.94993708884877,
43.5196578359177));
#92793=CARTESIAN_POINT('Ctrl Pts',(-1.9435690226063,-2.42040694294752,43.4666362013024));
#92794=CARTESIAN_POINT('Ctrl Pts',(-2.47374893172442,-1.60143289082343,
43.413614566687));
#92795=CARTESIAN_POINT('Ctrl Pts',(-2.77852281788827,-1.13064571039558,
43.3831350834879));
#92796=CARTESIAN_POINT('Ctrl Pts',(-2.93554916387039,-0.564211082746676,
43.3526556002887));
#92797=CARTESIAN_POINT('Ctrl Pts',(-2.93758116933064,0.00117923657373634,
43.3221761170895));
#92798=CARTESIAN_POINT('Ctrl Pts',(-2.93812373739311,0.00170130757060122,
43.1778238829105));
#92799=CARTESIAN_POINT('Ctrl Pts',(-2.93496663827918,-0.600574729914202,
43.2103068407869));
#92800=CARTESIAN_POINT('Ctrl Pts',(-2.75504347670453,-1.20458202709536,
43.2427897986634));
#92801=CARTESIAN_POINT('Ctrl Pts',(-2.41152602787865,-1.69369182620744,
43.2752727565398));
#92802=CARTESIAN_POINT('Ctrl Pts',(-1.85068098206933,-2.49223876647609,
43.3283061790356));
#92803=CARTESIAN_POINT('Ctrl Pts',(-0.853765839476469,-2.98451973655098,
43.3813396015314));
#92804=CARTESIAN_POINT('Ctrl Pts',(0.121227960435853,-2.94437660072665,
43.4343730240271));
#92805=CARTESIAN_POINT('Ctrl Pts',(1.09622176034817,-2.90423346490231,43.4874064465229));
#92806=CARTESIAN_POINT('Ctrl Pts',(2.04929421758002,-2.33166622317874,43.5404398690186));
#92807=CARTESIAN_POINT('Ctrl Pts',(2.54259560154553,-1.48971721890414,43.5934732915144));
#92808=CARTESIAN_POINT('Ctrl Pts',(3.03589698551106,-0.647768214629499,
43.6465067140102));
#92809=CARTESIAN_POINT('Ctrl Pts',(3.06942729621027,0.463562552196082,43.6995401365059));
#92810=CARTESIAN_POINT('Ctrl Pts',(2.62778241888289,1.33372011468222,43.7525735590017));
#92811=CARTESIAN_POINT('Ctrl Pts',(2.18613754155555,2.20387767716831,43.8056069814974));
#92812=CARTESIAN_POINT('Ctrl Pts',(1.26931747620161,2.83286203531488,43.8586404039932));
#92813=CARTESIAN_POINT('Ctrl Pts',(0.298517291007927,2.93171233450133,43.911673826489));
#92814=CARTESIAN_POINT('Ctrl Pts',(-0.672282894185814,3.03056263368778,
43.9647072489847));
#92815=CARTESIAN_POINT('Ctrl Pts',(-1.69706319921938,2.59927887391403,44.0177406714805));
#92816=CARTESIAN_POINT('Ctrl Pts',(-2.30503068797946,1.83599654486918,44.0707740939763));
#92817=CARTESIAN_POINT('Ctrl Pts',(-2.71409845623966,1.32242599271415,44.1064573569543));
#92818=CARTESIAN_POINT('Ctrl Pts',(-2.93446666976082,0.658553003231076,
44.1421406199324));
#92819=CARTESIAN_POINT('Ctrl Pts',(-2.93938501957473,-0.00234810359620528,
44.1778238829104));
#92820=CARTESIAN_POINT('Origin',(0.,0.,0.));
#92821=CARTESIAN_POINT('',(-2.94686614867256,-2.51058573618992E-5,45.3221761170895));
#92822=CARTESIAN_POINT('',(-2.94663624902442,-0.000757038452637187,45.1778238829105));
#92823=CARTESIAN_POINT('',(-2.942,-3.60291088309151E-16,0.));
#92824=CARTESIAN_POINT('Ctrl Pts',(-2.94686604665161,-2.51053310065807E-5,
45.3221761170895));
#92825=CARTESIAN_POINT('Ctrl Pts',(-2.94674347542402,0.974249485910166,
45.2692269143912));
#92826=CARTESIAN_POINT('Ctrl Pts',(-2.41578966879103,1.94863846518009,45.216277711693));
#92827=CARTESIAN_POINT('Ctrl Pts',(-1.59698410515242,2.47662327554372,45.1633285089947));
#92828=CARTESIAN_POINT('Ctrl Pts',(-0.777058455588465,3.00533034327972,
45.1103068743793));
#92829=CARTESIAN_POINT('Ctrl Pts',(0.331507023858134,3.08641108866027,45.0572852397639));
#92830=CARTESIAN_POINT('Ctrl Pts',(1.21963497345379,2.68263147156411,45.0042636051485));
#92831=CARTESIAN_POINT('Ctrl Pts',(2.10776292304939,2.27885185446797,44.9512419705331));
#92832=CARTESIAN_POINT('Ctrl Pts',(2.77545334279413,1.39021187489515,44.8982203359177));
#92833=CARTESIAN_POINT('Ctrl Pts',(2.91608828119759,0.424794323698634,44.8451987013024));
#92834=CARTESIAN_POINT('Ctrl Pts',(3.05672321960106,-0.540623227497989,
44.792177066687));
#92835=CARTESIAN_POINT('Ctrl Pts',(2.67030267666323,-1.58281835031824,44.7391554320716));
#92836=CARTESIAN_POINT('Ctrl Pts',(1.93427936366993,-2.22319239479913,44.6861337974562));
#92837=CARTESIAN_POINT('Ctrl Pts',(1.19825605067672,-2.86356643927994,44.6331121628408));
#92838=CARTESIAN_POINT('Ctrl Pts',(0.112629967628113,-3.10211940542135,
44.5800905282254));
#92839=CARTESIAN_POINT('Ctrl Pts',(-0.82405579482585,-2.82930258685599,
44.52706889361));
#92840=CARTESIAN_POINT('Ctrl Pts',(-1.76074155727987,-2.55648576829062,
44.4740472589946));
#92841=CARTESIAN_POINT('Ctrl Pts',(-2.54848699913928,-1.77229916501841,
44.4210256243793));
#92842=CARTESIAN_POINT('Ctrl Pts',(-2.82554229380675,-0.836858307572525,
44.3680039897639));
#92843=CARTESIAN_POINT('Ctrl Pts',(-2.90536414300644,-0.567350305035001,
44.3527280322058));
#92844=CARTESIAN_POINT('Ctrl Pts',(-2.9427955311576,-0.285287257906869,
44.3374520746477));
#92845=CARTESIAN_POINT('Ctrl Pts',(-2.94040227747744,-0.00260344384514166,
44.3221761170895));
#92846=CARTESIAN_POINT('Ctrl Pts',(-2.93938501957473,-0.00234810359620528,
44.1778238829104));
#92847=CARTESIAN_POINT('Ctrl Pts',(-2.94177645316889,-0.323695947707879,
44.1951740424281));
#92848=CARTESIAN_POINT('Ctrl Pts',(-2.89323197945426,-0.644341189660126,
44.2125242019458));
#92849=CARTESIAN_POINT('Ctrl Pts',(-2.7906765954805,-0.946664631606558,
44.2298743614635));
#92850=CARTESIAN_POINT('Ctrl Pts',(-2.47720034173483,-1.87076258072161,
44.2829077839593));
#92851=CARTESIAN_POINT('Ctrl Pts',(-1.65909316175687,-2.6236775806358,44.335941206455));
#92852=CARTESIAN_POINT('Ctrl Pts',(-0.712200570359879,-2.85951396794568,
44.3889746289508));
#92853=CARTESIAN_POINT('Ctrl Pts',(0.234692021037057,-3.09535035525555,
44.4420080514465));
#92854=CARTESIAN_POINT('Ctrl Pts',(1.31037002385295,-2.81410812996117,44.4950414739423));
#92855=CARTESIAN_POINT('Ctrl Pts',(2.02065765936511,-2.14499240300543,44.548074896438));
#92856=CARTESIAN_POINT('Ctrl Pts',(2.73094529487735,-1.47587667604963,44.6011083189338));
#92857=CARTESIAN_POINT('Ctrl Pts',(3.07584256308573,-0.41888744743224,44.6541417414296));
#92858=CARTESIAN_POINT('Ctrl Pts',(2.89690067574173,0.54038528864112,44.7071751639254));
#92859=CARTESIAN_POINT('Ctrl Pts',(2.71795878839774,1.49965802471448,44.7602085864212));
#92860=CARTESIAN_POINT('Ctrl Pts',(2.01517774550148,2.36121426824389,44.8132420089169));
#92861=CARTESIAN_POINT('Ctrl Pts',(1.11142123695542,2.72924762880537,44.8662754314126));
#92862=CARTESIAN_POINT('Ctrl Pts',(0.207664728409461,3.0972809893668,44.9193088539084));
#92863=CARTESIAN_POINT('Ctrl Pts',(-0.897067245786189,2.97179146696041,
44.9723422764041));
#92864=CARTESIAN_POINT('Ctrl Pts',(-1.69525126113925,2.41043003361006,45.0253756988999));
#92865=CARTESIAN_POINT('Ctrl Pts',(-2.46006269463699,1.87253947918556,45.0761917602368));
#92866=CARTESIAN_POINT('Ctrl Pts',(-2.94342421446499,0.934463217541238,
45.1270078215736));
#92867=CARTESIAN_POINT('Ctrl Pts',(-2.94663624902442,-0.000757038452637187,
45.1778238829105));
#92868=CARTESIAN_POINT('Origin',(0.,0.,0.));
#92869=CARTESIAN_POINT('',(-2.94047772160941,0.00261614231624671,46.3221761170895));
#92870=CARTESIAN_POINT('',(-2.94168313190805,0.00271989540251569,46.1778238829104));
#92871=CARTESIAN_POINT('',(-2.942,-3.60291088309151E-16,0.));
#92872=CARTESIAN_POINT('Ctrl Pts',(-2.94047772160941,0.00261614231624671,
46.3221761170895));
#92873=CARTESIAN_POINT('Ctrl Pts',(-2.94286443428716,0.282601028255245,
46.3070450233656));
#92874=CARTESIAN_POINT('Ctrl Pts',(-2.90615255438172,0.561972588305002,
46.2919139296416));
#92875=CARTESIAN_POINT('Ctrl Pts',(-2.82781690667401,0.829139711354088,
46.2767828359177));
#92876=CARTESIAN_POINT('Ctrl Pts',(-2.55331698182402,1.76533360705024,46.2237612013023));
#92877=CARTESIAN_POINT('Ctrl Pts',(-1.76771577226658,2.55166832950176,46.170739566687));
#92878=CARTESIAN_POINT('Ctrl Pts',(-0.831778455781653,2.82704186270968,
46.1177179320716));
#92879=CARTESIAN_POINT('Ctrl Pts',(0.104158860703217,3.10241539591758,46.0646962974562));
#92880=CARTESIAN_POINT('Ctrl Pts',(1.19043228411555,2.86682773988194,46.0116746628408));
#92881=CARTESIAN_POINT('Ctrl Pts',(1.92820146634532,2.22846587792299,45.9586530282254));
#92882=CARTESIAN_POINT('Ctrl Pts',(2.66597064857513,1.590104015964,45.90563139361));
#92883=CARTESIAN_POINT('Ctrl Pts',(3.05523558962236,0.548967948081663,45.8526097589947));
#92884=CARTESIAN_POINT('Ctrl Pts',(2.91723736081436,-0.416830023037316,
45.7995881243793));
#92885=CARTESIAN_POINT('Ctrl Pts',(2.77923913200637,-1.38262799415624,45.7465664897639));
#92886=CARTESIAN_POINT('Ctrl Pts',(2.11397773334323,-2.27308786851182,45.6935448551485));
#92887=CARTESIAN_POINT('Ctrl Pts',(1.22695566109724,-2.67929111665561,45.6405232205331));
#92888=CARTESIAN_POINT('Ctrl Pts',(0.339933588851193,-3.08549436479943,
45.5875015859177));
#92889=CARTESIAN_POINT('Ctrl Pts',(-0.768849156977722,-3.00744098673142,
45.5344799513024));
#92890=CARTESIAN_POINT('Ctrl Pts',(-1.59021544510426,-2.48097479164936,
45.481458316687));
#92891=CARTESIAN_POINT('Ctrl Pts',(-2.41270378718693,-1.95378940041144,
45.4283642501545));
#92892=CARTESIAN_POINT('Ctrl Pts',(-2.94698895322209,-0.976965216459942,
45.375270183622));
#92893=CARTESIAN_POINT('Ctrl Pts',(-2.94686604665161,-2.51053310065807E-5,
45.3221761170895));
#92894=CARTESIAN_POINT('Ctrl Pts',(-2.94663624902442,-0.000757038452637187,
45.1778238829105));
#92895=CARTESIAN_POINT('Ctrl Pts',(-2.94677640629922,-0.0415654170659208,
45.1800412440694));
#92896=CARTESIAN_POINT('Ctrl Pts',(-2.94600235068899,-0.0823683577952838,
45.1822586052283));
#92897=CARTESIAN_POINT('Ctrl Pts',(-2.94429757386013,-0.123132375178255,
45.1844759663872));
#92898=CARTESIAN_POINT('Ctrl Pts',(-2.90352381471748,-1.09810000632183,
45.237509388883));
#92899=CARTESIAN_POINT('Ctrl Pts',(-2.33034023992174,-2.05080192431461,
45.2905428113787));
#92900=CARTESIAN_POINT('Ctrl Pts',(-1.48807234151735,-2.54355862753419,
45.3435762338744));
#92901=CARTESIAN_POINT('Ctrl Pts',(-0.645804443112948,-3.03631533075377,
45.3966096563702));
#92902=CARTESIAN_POINT('Ctrl Pts',(0.465547778900108,-3.06912681920016,
45.449643078866));
#92903=CARTESIAN_POINT('Ctrl Pts',(1.33541950084067,-2.62691921121265,45.5026765013617));
#92904=CARTESIAN_POINT('Ctrl Pts',(2.20529122278124,-2.18471160322514,45.5557099238575));
#92905=CARTESIAN_POINT('Ctrl Pts',(2.83368244464931,-1.26748489880373,45.6087433463532));
#92906=CARTESIAN_POINT('Ctrl Pts',(2.93190480393636,-0.296620979756358,
45.661776768849));
#92907=CARTESIAN_POINT('Ctrl Pts',(3.03012716322342,0.674242939291123,45.7148101913448));
#92908=CARTESIAN_POINT('Ctrl Pts',(2.59818065992933,1.69874407296457,45.7678436138406));
#92909=CARTESIAN_POINT('Ctrl Pts',(1.83450525351452,2.30621773911007,45.8208770363363));
#92910=CARTESIAN_POINT('Ctrl Pts',(1.07082984709984,2.91369140525546,45.8739104588321));
#92911=CARTESIAN_POINT('Ctrl Pts',(-0.0245744624354413,3.10413760387306,
45.9269438813278));
#92912=CARTESIAN_POINT('Ctrl Pts',(-0.948469459799883,2.79006370360431,
45.9799773038235));
#92913=CARTESIAN_POINT('Ctrl Pts',(-1.87236445716438,2.47598980333554,46.0330107263193));
#92914=CARTESIAN_POINT('Ctrl Pts',(-2.62475014235801,1.65739580418036,46.0860441488151));
#92915=CARTESIAN_POINT('Ctrl Pts',(-2.85997402495524,0.710350870700089,
46.1390775713109));
#92916=CARTESIAN_POINT('Ctrl Pts',(-2.9172590188444,0.479713306911208,46.1519930085107));
#92917=CARTESIAN_POINT('Ctrl Pts',(-2.94387178257188,0.241457476262084,
46.1649084457106));
#92918=CARTESIAN_POINT('Ctrl Pts',(-2.94168313190805,0.00271989540251569,
46.1778238829104));
#92919=CARTESIAN_POINT('Origin',(0.,0.,0.));
#92920=CARTESIAN_POINT('',(-2.93754881179149,-0.00113833082597881,47.3221761170895));
#92921=CARTESIAN_POINT('',(-2.93719707228474,-0.000468378137186533,47.1778238829104));
#92922=CARTESIAN_POINT('',(-2.942,-3.60291088309151E-16,0.));
#92923=CARTESIAN_POINT('Ctrl Pts',(-2.93754881179149,-0.00113833082597881,
47.3221761170895));
#92924=CARTESIAN_POINT('Ctrl Pts',(-2.93559720265068,0.561579659279432,
47.2918414977246));
#92925=CARTESIAN_POINT('Ctrl Pts',(-2.78015759911032,1.12529577977501,47.2615068783596));
#92926=CARTESIAN_POINT('Ctrl Pts',(-2.47811301989175,1.59467174661818,47.2311722589946));
#92927=CARTESIAN_POINT('Ctrl Pts',(-1.95017175502176,2.41509018377687,47.1781506243792));
#92928=CARTESIAN_POINT('Ctrl Pts',(-0.974333818001319,2.94728756516578,
47.1251289897639));
#92929=CARTESIAN_POINT('Ctrl Pts',(0.00127339248023564,2.94686620634015,
47.0721073551485));
#92930=CARTESIAN_POINT('Ctrl Pts',(0.976880602961791,2.94644484751451,47.0190857205331));
#92931=CARTESIAN_POINT('Ctrl Pts',(1.95225708690446,2.41340474847432,46.9660640859178));
#92932=CARTESIAN_POINT('Ctrl Pts',(2.47948950501506,1.59253007365169,46.9130424513024));
#92933=CARTESIAN_POINT('Ctrl Pts',(3.00672192312566,0.771655398829069,46.860020816687));
#92934=CARTESIAN_POINT('Ctrl Pts',(3.08581027540417,-0.337053851776008,
46.8069991820716));
#92935=CARTESIAN_POINT('Ctrl Pts',(2.68043508402907,-1.22445459233511,46.7539775474562));
#92936=CARTESIAN_POINT('Ctrl Pts',(2.27505989265393,-2.11185533289432,46.7009559128408));
#92937=CARTESIAN_POINT('Ctrl Pts',(1.38522115762505,-2.77794756340749,46.6479342782254));
#92938=CARTESIAN_POINT('Ctrl Pts',(0.419552367709688,-2.91684710004787,
46.59491264361));
#92939=CARTESIAN_POINT('Ctrl Pts',(-0.546116422205564,-3.05574663668823,
46.5418910089947));
#92940=CARTESIAN_POINT('Ctrl Pts',(-1.58761526700728,-2.6674534794559,46.4888693743793));
#92941=CARTESIAN_POINT('Ctrl Pts',(-2.22666536933688,-1.93028036636939,
46.4358477397639));
#92942=CARTESIAN_POINT('Ctrl Pts',(-2.68334600941247,-1.40347865253879,
46.3979571988724));
#92943=CARTESIAN_POINT('Ctrl Pts',(-2.93450103307901,-0.698508241896662,
46.360066657981));
#92944=CARTESIAN_POINT('Ctrl Pts',(-2.94047772160941,0.00261614231624671,
46.3221761170895));
#92945=CARTESIAN_POINT('Ctrl Pts',(-2.94168313190805,0.00271989540251569,
46.1778238829104));
#92946=CARTESIAN_POINT('Ctrl Pts',(-2.93488473602019,-0.738847781346994,
46.2179418682063));
#92947=CARTESIAN_POINT('Ctrl Pts',(-2.65019576255787,-1.48506362719018,
46.2580598535022));
#92948=CARTESIAN_POINT('Ctrl Pts',(-2.14368498174406,-2.02204462993227,
46.2981778387981));
#92949=CARTESIAN_POINT('Ctrl Pts',(-1.47410997593488,-2.73189932927898,
46.3512112612939));
#92950=CARTESIAN_POINT('Ctrl Pts',(-0.416897884315671,-3.07611286016707,
46.4042446837896));
#92951=CARTESIAN_POINT('Ctrl Pts',(0.542258909289073,-2.89655054624969,
46.4572781062854));
#92952=CARTESIAN_POINT('Ctrl Pts',(1.50141570289387,-2.7169882323323,46.5103115287812));
#92953=CARTESIAN_POINT('Ctrl Pts',(2.36251719848426,-2.01365007360937,46.5633449512769));
#92954=CARTESIAN_POINT('Ctrl Pts',(2.72996592922045,-1.10965570941658,46.6163783737727));
#92955=CARTESIAN_POINT('Ctrl Pts',(3.09741465995664,-0.205661345223792,
46.6694117962685));
#92956=CARTESIAN_POINT('Ctrl Pts',(2.97121062583871,0.898989224438765,46.7224452187642));
#92957=CARTESIAN_POINT('Ctrl Pts',(2.40933303563599,1.69680998371491,46.77547864126));
#92958=CARTESIAN_POINT('Ctrl Pts',(1.8474554454333,2.49463074299101,46.8285120637558));
#92959=CARTESIAN_POINT('Ctrl Pts',(0.849904299145825,2.98562169188063,46.8815454862515));
#92960=CARTESIAN_POINT('Ctrl Pts',(-0.125036747405431,2.94421732120279,
46.9345789087473));
#92961=CARTESIAN_POINT('Ctrl Pts',(-1.09997779395669,2.90281295052495,46.987612331243));
#92962=CARTESIAN_POINT('Ctrl Pts',(-2.05230874077178,2.32901326027967,47.0406457537388));
#92963=CARTESIAN_POINT('Ctrl Pts',(-2.54452057223983,1.48642683017747,47.0936791762345));
#92964=CARTESIAN_POINT('Ctrl Pts',(-2.80484081453354,1.04080100484249,47.1217274117932));
#92965=CARTESIAN_POINT('Ctrl Pts',(-2.93646001628066,0.519992184602745,
47.1497756473518));
#92966=CARTESIAN_POINT('Ctrl Pts',(-2.93719707228474,-0.000468378137186533,
47.1778238829104));
#92967=CARTESIAN_POINT('Origin',(0.,0.,0.));
#92968=CARTESIAN_POINT('',(-2.94461792262617,-0.00215304676840083,48.3221761170895));
#92969=CARTESIAN_POINT('',(-2.943409633743,-0.00255526730400832,48.1778238829104));
#92970=CARTESIAN_POINT('',(-2.942,-3.60291088309151E-16,0.));
#92971=CARTESIAN_POINT('Ctrl Pts',(-2.94461792262617,-0.00215304676840083,
48.3221761170895));
#92972=CARTESIAN_POINT('Ctrl Pts',(-2.93763702468649,0.837415355975283,
48.2766379720835));
#92973=CARTESIAN_POINT('Ctrl Pts',(-2.56039370972494,1.68241193941936,48.2310998270776));
#92974=CARTESIAN_POINT('Ctrl Pts',(-1.92629505958697,2.23011593323329,48.1855616820716));
#92975=CARTESIAN_POINT('Ctrl Pts',(-1.18799210646253,2.86782660488176,48.1325400474562));
#92976=CARTESIAN_POINT('Ctrl Pts',(-0.101476823706468,3.10250517619938,
48.0795184128408));
#92977=CARTESIAN_POINT('Ctrl Pts',(0.834231395674201,2.82633006893815,48.0264967782254));
#92978=CARTESIAN_POINT('Ctrl Pts',(1.76993961505482,2.55015496167694,47.97347514361));
#92979=CARTESIAN_POINT('Ctrl Pts',(2.55484077106006,1.76312617583694,47.9204535089946));
#92980=CARTESIAN_POINT('Ctrl Pts',(2.82852682256973,0.826691734777258,47.8674318743793));
#92981=CARTESIAN_POINT('Ctrl Pts',(3.10221287407942,-0.109742706282482,
47.8144102397639));
#92982=CARTESIAN_POINT('Ctrl Pts',(2.86468382109348,-1.19558280256193,47.7613886051485));
#92983=CARTESIAN_POINT('Ctrl Pts',(2.22499948973125,-1.93220149581064,47.7083669705331));
#92984=CARTESIAN_POINT('Ctrl Pts',(1.58531515836902,-2.66882018905935,47.6553453359178));
#92985=CARTESIAN_POINT('Ctrl Pts',(0.543475548630508,-3.05621747927732,
47.6023237013023));
#92986=CARTESIAN_POINT('Ctrl Pts',(-0.422074157754231,-2.91648460887001,
47.5493020666869));
#92987=CARTESIAN_POINT('Ctrl Pts',(-1.38762386413897,-2.77675173846269,
47.4962804320715));
#92988=CARTESIAN_POINT('Ctrl Pts',(-2.27688366716993,-2.10988870743008,
47.4432587974562));
#92989=CARTESIAN_POINT('Ctrl Pts',(-2.68149127232562,-1.2221374454495,47.3902371628408));
#92990=CARTESIAN_POINT('Ctrl Pts',(-2.8546156766408,-0.842284455905961,
47.3675501475904));
#92991=CARTESIAN_POINT('Ctrl Pts',(-2.9390084044044,-0.421990541615868,
47.34486313234));
#92992=CARTESIAN_POINT('Ctrl Pts',(-2.93754881179149,-0.00113833082597881,
47.3221761170895));
#92993=CARTESIAN_POINT('Ctrl Pts',(-2.93719707228474,-0.000468378137186533,
47.1778238829104));
#92994=CARTESIAN_POINT('Ctrl Pts',(-2.93785363700899,-0.464091283267131,
47.2028090698475));
#92995=CARTESIAN_POINT('Ctrl Pts',(-2.8346535013737,-0.9274378415004,47.2277942567846));
#92996=CARTESIAN_POINT('Ctrl Pts',(-2.62605493729491,-1.33711830655687,
47.2527794437218));
#92997=CARTESIAN_POINT('Ctrl Pts',(-2.18328475476092,-2.20670384322986,
47.3058128662175));
#92998=CARTESIAN_POINT('Ctrl Pts',(-1.26565167357192,-2.83450174661667,
47.3588462887133));
#92999=CARTESIAN_POINT('Ctrl Pts',(-0.294724481945897,-2.93209608829399,
47.4118797112091));
#93000=CARTESIAN_POINT('Ctrl Pts',(0.676202709680179,-3.02969042997131,
47.4649131337049));
#93001=CARTESIAN_POINT('Ctrl Pts',(1.70042401174323,-2.59708120993907,47.5179465562006));
#93002=CARTESIAN_POINT('Ctrl Pts',(2.30740370625557,-1.83301311549819,47.5709799786964));
#93003=CARTESIAN_POINT('Ctrl Pts',(2.91438340076788,-1.06894502105736,47.6240134011921));
#93004=CARTESIAN_POINT('Ctrl Pts',(3.10412148772949,0.0265819477921747,
47.6770468236879));
#93005=CARTESIAN_POINT('Ctrl Pts',(2.78944987179727,0.950273740143268,47.7300802461837));
#93006=CARTESIAN_POINT('Ctrl Pts',(2.47477825586507,1.87396553249431,47.7831136686794));
#93007=CARTESIAN_POINT('Ctrl Pts',(1.6556969370392,2.62582214834703,47.8361470911751));
#93008=CARTESIAN_POINT('Ctrl Pts',(0.708500440227379,2.86043317362063,47.8891805136709));
#93009=CARTESIAN_POINT('Ctrl Pts',(-0.238696056584552,3.09504419889426,
47.9422139361667));
#93010=CARTESIAN_POINT('Ctrl Pts',(-1.31400773138241,2.81240963358864,47.9952473586625));
#93011=CARTESIAN_POINT('Ctrl Pts',(-2.023429927351,2.14237611397396,48.0482807811582));
#93012=CARTESIAN_POINT('Ctrl Pts',(-2.60105781678863,1.5968193919164,48.0914618150756));
#93013=CARTESIAN_POINT('Ctrl Pts',(-2.93611593149267,0.794432991729182,
48.134642848993));
#93014=CARTESIAN_POINT('Ctrl Pts',(-2.943409633743,-0.00255526730400832,
48.1778238829104));
#93015=CARTESIAN_POINT('Origin',(0.,0.,-1.84858989190512));
#93016=CARTESIAN_POINT('',(-2.37386048877927,-0.00173572014615222,48.6514101080949));
#93017=CARTESIAN_POINT('',(-2.37475460450346,0.00138119150085991,48.8485898919049));
#93018=CARTESIAN_POINT('',(-2.37175,1.74448693060498E-12,-1.84858989190512));
#93019=CARTESIAN_POINT('',(-2.34668236863858,0.343918483395164,49.62825));
#93020=CARTESIAN_POINT('Ctrl Pts',(-2.37386048877927,-0.00173572014615207,
48.6514101080949));
#93021=CARTESIAN_POINT('Ctrl Pts',(-2.37478532824446,-0.112962957566302,
48.6588935977043));
#93022=CARTESIAN_POINT('Ctrl Pts',(-2.31708772079214,-1.01129619086623,
48.7193987219291));
#93023=CARTESIAN_POINT('Ctrl Pts',(-1.17033730995746,-2.54951603961395,
48.8329254807692));
#93024=CARTESIAN_POINT('Ctrl Pts',(1.51207452279905,-2.36256262295682,48.9919903846154));
#93025=CARTESIAN_POINT('Ctrl Pts',(2.80422967385422,-0.00687846186160384,
49.1510552884616));
#93026=CARTESIAN_POINT('Ctrl Pts',(1.52375565164409,2.35733202978189,49.3101201923077));
#93027=CARTESIAN_POINT('Ctrl Pts',(-1.16201321478499,2.55211054076708,49.4691850961539));
#93028=CARTESIAN_POINT('Ctrl Pts',(-2.23210772954909,1.12570340751462,49.5752283653847));
#93029=CARTESIAN_POINT('Ctrl Pts',(-2.34668236863857,0.343918483395232,
49.62825));
#93030=CARTESIAN_POINT('',(-0.43944522199609,2.33068358199152,49.6282500000002));
#93031=CARTESIAN_POINT('Origin',(0.,0.,49.62825));
#93032=CARTESIAN_POINT('Ctrl Pts',(-2.37475460450346,0.00138119150086006,
48.8485898919049));
#93033=CARTESIAN_POINT('Ctrl Pts',(-2.36985243589685,-0.707780462192968,
48.8963429046203));
#93034=CARTESIAN_POINT('Ctrl Pts',(-1.65515900824388,-2.21309514855009,
48.9971293398314));
#93035=CARTESIAN_POINT('Ctrl Pts',(0.905469678109174,-2.65425291543538,
49.1509491975383));
#93036=CARTESIAN_POINT('Ctrl Pts',(2.72507495425543,-0.67380191912698,49.3100494650256));
#93037=CARTESIAN_POINT('Ctrl Pts',(2.03481676979323,1.92982725944834,49.4691497325128));
#93038=CARTESIAN_POINT('Ctrl Pts',(0.337182413353676,2.47711500076564,49.5752165775044));
#93039=CARTESIAN_POINT('Ctrl Pts',(-0.43944522199609,2.33068358199152,49.6282500000002));
#93040=CARTESIAN_POINT('Origin',(0.,0.,-1.84858989190512));
#93041=CARTESIAN_POINT('',(-2.36816158883972,-0.000917687332811956,47.6514101080949));
#93042=CARTESIAN_POINT('',(-2.37288640340922,-0.00205997798142371,47.8485898919049));
#93043=CARTESIAN_POINT('',(-2.37175,1.74448693060498E-12,-1.84858989190512));
#93044=CARTESIAN_POINT('Ctrl Pts',(-2.36816158883972,-0.000917687332812299,
47.6514101080949));
#93045=CARTESIAN_POINT('Ctrl Pts',(-2.36933826755493,-0.340195807979261,
47.6740971233453));
#93046=CARTESIAN_POINT('Ctrl Pts',(-2.14229982249859,-1.47089603886295,
47.7498057732111));
#93047=CARTESIAN_POINT('Ctrl Pts',(-0.401765792635603,-2.77613641385121,
47.8785360576923));
#93048=CARTESIAN_POINT('Ctrl Pts',(2.11793144842226,-1.83921303886061,48.0376009615385));
#93049=CARTESIAN_POINT('Ctrl Pts',(2.69239732002637,0.78689972288376,48.1966658653846));
#93050=CARTESIAN_POINT('Ctrl Pts',(0.794107738018986,2.69033499428045,48.3557307692309));
#93051=CARTESIAN_POINT('Ctrl Pts',(-1.7100110252374,2.14946546110686,48.5073121834675));
#93052=CARTESIAN_POINT('Ctrl Pts',(-2.36823270336483,0.675098528394528,
48.6058719630889));
#93053=CARTESIAN_POINT('Ctrl Pts',(-2.37386048877927,-0.00173572014615207,
48.6514101080949));
#93054=CARTESIAN_POINT('Ctrl Pts',(-2.37288640340922,-0.00205997798142388,
47.8485898919049));
#93055=CARTESIAN_POINT('Ctrl Pts',(-2.37422800253445,-0.148657510252996,
47.8584422804833));
#93056=CARTESIAN_POINT('Ctrl Pts',(-2.29499082631282,-1.08291398552728,
47.9213280915575));
#93057=CARTESIAN_POINT('Ctrl Pts',(-1.05464278435862,-2.59947119907506,
48.0372473251273));
#93058=CARTESIAN_POINT('Ctrl Pts',(1.61673826111253,-2.29249989126509,48.1963475926147));
#93059=CARTESIAN_POINT('Ctrl Pts',(2.80269451719685,0.120818728651149,48.3554478601019));
#93060=CARTESIAN_POINT('Ctrl Pts',(1.41336773306382,2.42320569438391,48.5145481275892));
#93061=CARTESIAN_POINT('Ctrl Pts',(-1.27435908006578,2.49895924442061,48.6736483950764));
#93062=CARTESIAN_POINT('Ctrl Pts',(-2.33621967799716,0.945246301592545,
48.7849956498484));
#93063=CARTESIAN_POINT('Ctrl Pts',(-2.37529667415695,0.0797985293630277,
48.8433094821245));
#93064=CARTESIAN_POINT('Ctrl Pts',(-2.37475460450346,0.00138119150086006,
48.8485898919049));
#93065=CARTESIAN_POINT('Origin',(0.,0.,-1.84858989190512));
#93066=CARTESIAN_POINT('',(-2.37052278593716,0.00210905354912938,46.6514101080949));
#93067=CARTESIAN_POINT('',(-2.36787802725742,-0.000377592060197274,46.8485898919049));
#93068=CARTESIAN_POINT('',(-2.37175,1.74448693060498E-12,-1.84858989190512));
#93069=CARTESIAN_POINT('Ctrl Pts',(-2.37052278593716,0.00210905354912923,
46.6514101080949));
#93070=CARTESIAN_POINT('Ctrl Pts',(-2.36570456329227,-0.563115881276711,
46.6893006489864));
#93071=CARTESIAN_POINT('Ctrl Pts',(-1.87990249905625,-1.92672022299298,
46.7802128244932));
#93072=CARTESIAN_POINT('Ctrl Pts',(0.399362087284636,-2.7764790554831,46.9241466346154));
#93073=CARTESIAN_POINT('Ctrl Pts',(2.55144402454308,-1.16552978860435,47.0832115384616));
#93074=CARTESIAN_POINT('Ctrl Pts',(2.36016822626022,1.51589220166356,47.2422764423077));
#93075=CARTESIAN_POINT('Ctrl Pts',(0.00121257453600308,2.80505384839945,
47.4013413461539));
#93076=CARTESIAN_POINT('Ctrl Pts',(-2.02224819409324,1.70150941591366,47.5377192347496));
#93077=CARTESIAN_POINT('Ctrl Pts',(-2.36658826151806,0.452728265431197,
47.6210754887299));
#93078=CARTESIAN_POINT('Ctrl Pts',(-2.36816158883972,-0.000917687332812299,
47.6514101080949));
#93079=CARTESIAN_POINT('Ctrl Pts',(-2.36787802725742,-0.000377592060197413,
46.8485898919049));
#93080=CARTESIAN_POINT('Ctrl Pts',(-2.36840732956388,-0.374136132251743,
46.8735750788421));
#93081=CARTESIAN_POINT('Ctrl Pts',(-2.10861752023225,-1.54053686687448,
46.951593688275));
#93082=CARTESIAN_POINT('Ctrl Pts',(-0.280561895474226,-2.79119959037926,
47.0826457202037));
#93083=CARTESIAN_POINT('Ctrl Pts',(2.19652533073393,-1.74493080967452,47.241745987691));
#93084=CARTESIAN_POINT('Ctrl Pts',(2.65540837738748,0.904609729110513,47.4008462551782));
#93085=CARTESIAN_POINT('Ctrl Pts',(0.674453804384293,2.72298083242374,47.5599465226655));
#93086=CARTESIAN_POINT('Ctrl Pts',(-1.7651489471279,2.08175645129611,47.7091944015744));
#93087=CARTESIAN_POINT('Ctrl Pts',(-2.36700644477084,0.640447467076404,
47.8054088579876));
#93088=CARTESIAN_POINT('Ctrl Pts',(-2.37288640340922,-0.00205997798142388,
47.8485898919049));
#93089=CARTESIAN_POINT('Origin',(0.,0.,-1.84858989190512));
#93090=CARTESIAN_POINT('',(-2.3756729420957,-2.02395829644482E-5,45.6514101080949));
#93091=CARTESIAN_POINT('',(-2.37149455068082,0.00219269610015983,45.8485898919049));
#93092=CARTESIAN_POINT('',(-2.37175,1.74448693060498E-12,-1.84858989190512));
#93093=CARTESIAN_POINT('Ctrl Pts',(-2.37567285728959,-2.02391454256733E-5,
45.6514101080949));
#93094=CARTESIAN_POINT('Ctrl Pts',(-2.37567299246115,-0.00109466926018251,
45.651482540012));
#93095=CARTESIAN_POINT('Ctrl Pts',(-2.37518507362446,-0.788673641534315,
45.7045766065445));
#93096=CARTESIAN_POINT('Ctrl Pts',(-1.51368914530336,-2.36158227765018,
45.8106923076923));
#93097=CARTESIAN_POINT('Ctrl Pts',(1.16791059373771,-2.55035498271459,45.9697572115385));
#93098=CARTESIAN_POINT('Ctrl Pts',(2.77685048729278,-0.396770815138777,
46.1288221153846));
#93099=CARTESIAN_POINT('Ctrl Pts',(1.83541018417072,2.12122490443972,46.2878870192308));
#93100=CARTESIAN_POINT('Ctrl Pts',(-0.791750582632343,2.69099549234209,
46.446951923077));
#93101=CARTESIAN_POINT('Ctrl Pts',(-2.23914207963376,1.24225257134515,46.5681262860316));
#93102=CARTESIAN_POINT('Ctrl Pts',(-2.3724468803604,0.227824265386368,46.636279014371));
#93103=CARTESIAN_POINT('Ctrl Pts',(-2.37052278593716,0.00210905354912923,
46.6514101080949));
#93104=CARTESIAN_POINT('Ctrl Pts',(-2.37149455068082,0.00219269610015994,
45.8485898919049));
#93105=CARTESIAN_POINT('Ctrl Pts',(-2.36601389281351,-0.595636378451926,
45.8887078772009));
#93106=CARTESIAN_POINT('Ctrl Pts',(-1.83311208298173,-1.99245821506647,
45.9818592849926));
#93107=CARTESIAN_POINT('Ctrl Pts',(0.516201638739318,-2.75736203874416,
46.12804411528));
#93108=CARTESIAN_POINT('Ctrl Pts',(2.59878233775354,-1.05633320330836,46.2871443827674));
#93109=CARTESIAN_POINT('Ctrl Pts',(2.29355689460039,1.61527283537019,46.4462446502545));
#93110=CARTESIAN_POINT('Ctrl Pts',(-0.119028351361985,2.80273828373448,
46.6053449177419));
#93111=CARTESIAN_POINT('Ctrl Pts',(-2.06054937610219,1.63293049125855,46.7394599982919));
#93112=CARTESIAN_POINT('Ctrl Pts',(-2.36728383535441,0.419201721222213,
46.8205416563463));
#93113=CARTESIAN_POINT('Ctrl Pts',(-2.36787802725742,-0.000377592060197413,
46.8485898919049));
#93114=CARTESIAN_POINT('Origin',(0.,0.,-1.84858989190512));
#93115=CARTESIAN_POINT('',(-2.37046196519616,-0.00209881642975521,44.6514101080949));
#93116=CARTESIAN_POINT('',(-2.37548760150362,-0.000610301136611813,44.848589891905));
#93117=CARTESIAN_POINT('',(-2.37175,1.74448693060498E-12,-1.84858989190512));
#93118=CARTESIAN_POINT('Ctrl Pts',(-2.37046196519616,-0.00209881642975512,
44.6514101080949));
#93119=CARTESIAN_POINT('Ctrl Pts',(-2.37239133277476,-0.229989821189002,
44.666686065653));
#93120=CARTESIAN_POINT('Ctrl Pts',(-2.23747667874047,-1.24663494975249,
44.7349836578265));
#93121=CARTESIAN_POINT('Ctrl Pts',(-0.784399570615147,-2.69314741578982,
44.8563028846154));
#93122=CARTESIAN_POINT('Ctrl Pts',(1.84119559845759,-2.11620520221519,45.0153677884616));
#93123=CARTESIAN_POINT('Ctrl Pts',(2.7757567025159,0.404351850010035,45.1744326923077));
#93124=CARTESIAN_POINT('Ctrl Pts',(1.16094220248601,2.55353458782659,45.3334975961539));
#93125=CARTESIAN_POINT('Ctrl Pts',(-1.5189112200628,2.35752946495471,45.4924900680829));
#93126=CARTESIAN_POINT('Ctrl Pts',(-2.37557404413184,0.785409999391494,
45.5984609053966));
#93127=CARTESIAN_POINT('Ctrl Pts',(-2.37567285728959,-2.02391454256733E-5,
45.6514101080949));
#93128=CARTESIAN_POINT('Ctrl Pts',(-2.37548760150362,-0.000610301136611548,
44.848589891905));
#93129=CARTESIAN_POINT('Ctrl Pts',(-2.37560059199193,-0.0335087620399993,
44.8508072530639));
#93130=CARTESIAN_POINT('Ctrl Pts',(-2.3600516655157,-0.85314228325878,44.9060580367186));
#93131=CARTESIAN_POINT('Ctrl Pts',(-1.41656571057567,-2.42133250781507,
45.014342242869));
#93132=CARTESIAN_POINT('Ctrl Pts',(1.27124832670454,-2.50068734913707,45.1734425103564));
#93133=CARTESIAN_POINT('Ctrl Pts',(2.79101740943663,-0.282367393789022,
45.3325427778436));
#93134=CARTESIAN_POINT('Ctrl Pts',(1.74635141434428,2.19539660735637,45.4916430453309));
#93135=CARTESIAN_POINT('Ctrl Pts',(-0.902892471930827,2.65599222758591,
45.6507433128183));
#93136=CARTESIAN_POINT('Ctrl Pts',(-2.26370846509963,1.17542736851982,45.7697255950095));
#93137=CARTESIAN_POINT('Ctrl Pts',(-2.3732589735943,0.194655598004337,45.8356744547051));
#93138=CARTESIAN_POINT('Ctrl Pts',(-2.37149455068082,0.00219269610015994,
45.8485898919049));
#93139=CARTESIAN_POINT('Origin',(0.,0.,-1.84858989190512));
#93140=CARTESIAN_POINT('',(-2.36818767449352,0.000950664291755352,43.6514101080949));
#93141=CARTESIAN_POINT('',(-2.36964188313267,-0.00189296896605684,43.8485898919049));
#93142=CARTESIAN_POINT('',(-2.37175,1.74448693060498E-12,-1.84858989190512));
#93143=CARTESIAN_POINT('Ctrl Pts',(-2.36818767449352,0.000950664291755263,
43.6514101080949));
#93144=CARTESIAN_POINT('Ctrl Pts',(-2.36654953412987,-0.454849638172114,
43.681889591294));
#93145=CARTESIAN_POINT('Ctrl Pts',(-2.01974604676808,-1.70585947988162,
43.7653907091086));
#93146=CARTESIAN_POINT('Ctrl Pts',(0.00887142432873881,-2.80503956968683,
43.9019134615385));
#93147=CARTESIAN_POINT('Ctrl Pts',(2.36429909693514,-1.50944210551781,44.0609783653846));
#93148=CARTESIAN_POINT('Ctrl Pts',(2.54825171469771,1.17249259623757,44.2200432692308));
#93149=CARTESIAN_POINT('Ctrl Pts',(0.391779197956932,2.77755913523241,44.3791081730769));
#93150=CARTESIAN_POINT('Ctrl Pts',(-1.88286501107497,1.92244128703405,44.522897119365));
#93151=CARTESIAN_POINT('Ctrl Pts',(-2.36569465124747,0.56100174451135,44.6136644310376));
#93152=CARTESIAN_POINT('Ctrl Pts',(-2.37046196519616,-0.00209881642975512,
44.6514101080949));
#93153=CARTESIAN_POINT('Ctrl Pts',(-2.36964188313267,-0.00189296896605656,
43.8485898919049));
#93154=CARTESIAN_POINT('Ctrl Pts',(-2.37156978341398,-0.260953726706908,
43.8659400514226));
#93155=CARTESIAN_POINT('Ctrl Pts',(-2.21281240035297,-1.30957565229906,
43.9363236334361));
#93156=CARTESIAN_POINT('Ctrl Pts',(-0.677977057200952,-2.72210518454085,
44.0597406379455));
#93157=CARTESIAN_POINT('Ctrl Pts',(1.92355860205693,-2.04191866396806,44.2188409054326));
#93158=CARTESIAN_POINT('Ctrl Pts',(2.75769534156078,0.514418048784537,44.37794117292));
#93159=CARTESIAN_POINT('Ctrl Pts',(1.05801389510723,2.59809855924461,44.5370414404072));
#93160=CARTESIAN_POINT('Ctrl Pts',(-1.57655242741681,2.29883097463275,44.6939243467356));
#93161=CARTESIAN_POINT('Ctrl Pts',(-2.37289815793857,0.753335532361604,
44.7977738305682));
#93162=CARTESIAN_POINT('Ctrl Pts',(-2.37548760150362,-0.000610301136611548,
44.848589891905));
#93163=CARTESIAN_POINT('Origin',(0.,0.,-1.84858989190512));
#93164=CARTESIAN_POINT('',(-2.37395592879609,0.00174106614345369,42.6514101080949));
#93165=CARTESIAN_POINT('',(-2.36862507619379,0.00137154188862718,42.848589891905));
#93166=CARTESIAN_POINT('',(-2.37175,1.74448693060498E-12,-1.84858989190512));
#93167=CARTESIAN_POINT('Ctrl Pts',(-2.37395592879609,0.00174106614345361,
42.6514101080949));
#93168=CARTESIAN_POINT('Ctrl Pts',(-2.3683671883622,-0.677199472088916,
42.697093116935));
#93169=CARTESIAN_POINT('Ctrl Pts',(-1.70647264490752,-2.15366004211859,
42.7957977603907));
#93170=CARTESIAN_POINT('Ctrl Pts',(0.801418800438249,-2.68813199006011,
42.9475240384615));
#93171=CARTESIAN_POINT('Ctrl Pts',(2.69455290827499,-0.779557768345067,
43.1065889423078));
#93172=CARTESIAN_POINT('Ctrl Pts',(2.11289250645387,1.84499619128384,43.2656538461538));
#93173=CARTESIAN_POINT('Ctrl Pts',(-0.409340210132954,2.7750254561082,43.4247187500001));
#93174=CARTESIAN_POINT('Ctrl Pts',(-2.14435471179428,1.46651574667853,43.553304170647));
#93175=CARTESIAN_POINT('Ctrl Pts',(-2.36939921761179,0.33805347428917,43.6288679566786));
#93176=CARTESIAN_POINT('Ctrl Pts',(-2.36818767449352,0.000950664291755263,
43.6514101080949));
#93177=CARTESIAN_POINT('Ctrl Pts',(-2.36862507619379,0.00137154188862704,
42.848589891905));
#93178=CARTESIAN_POINT('Ctrl Pts',(-2.36607991989796,-0.484164893157661,
42.8810728497815));
#93179=CARTESIAN_POINT('Ctrl Pts',(-1.98421738068972,-1.76608856648426,
42.9665892301537));
#93180=CARTESIAN_POINT('Ctrl Pts',(0.11540256956664,-2.80288989664852,43.1051390330218));
#93181=CARTESIAN_POINT('Ctrl Pts',(2.42041575832236,-1.41813154631793,43.2642393005089));
#93182=CARTESIAN_POINT('Ctrl Pts',(2.50150907688241,1.26963060142386,43.4233395679963));
#93183=CARTESIAN_POINT('Ctrl Pts',(0.284172581298068,2.79083418888245,43.5824398354835));
#93184=CARTESIAN_POINT('Ctrl Pts',(-1.92398851613373,1.86151888529159,43.7241899434532));
#93185=CARTESIAN_POINT('Ctrl Pts',(-2.36567686064033,0.530905195587278,
43.8129066289269));
#93186=CARTESIAN_POINT('Ctrl Pts',(-2.36964188313267,-0.00189296896605656,
43.8485898919049));
#93187=CARTESIAN_POINT('Origin',(0.,0.,-1.84858989190512));
#93188=CARTESIAN_POINT('',(-2.37374189642354,-0.00182254589935643,41.6514101080949));
#93189=CARTESIAN_POINT('',(-2.37466860212234,0.00138350872013287,41.848589891905));
#93190=CARTESIAN_POINT('',(-2.37175,1.74448693060498E-12,-1.84858989190512));
#93191=CARTESIAN_POINT('Ctrl Pts',(-2.37374189642354,-0.0018225458993563,
41.6514101080949));
#93192=CARTESIAN_POINT('Ctrl Pts',(-2.37473518999418,-0.118738074680971,
41.6592750079607));
#93193=CARTESIAN_POINT('Ctrl Pts',(-2.31366732775003,-1.02280417077909,
41.7201615424419));
#93194=CARTESIAN_POINT('Ctrl Pts',(-1.15175551301023,-2.55769132772724,
41.8340697115385));
#93195=CARTESIAN_POINT('Ctrl Pts',(1.52859654328181,-2.35196052210647,41.9931346153846));
#93196=CARTESIAN_POINT('Ctrl Pts',(2.8050190938,0.0139130549425746,42.1521995192308));
#93197=CARTESIAN_POINT('Ctrl Pts',(1.50519018846317,2.36700827760163,42.311264423077));
#93198=CARTESIAN_POINT('Ctrl Pts',(-1.17707080902522,2.54614021613523,42.4703293269231));
#93199=CARTESIAN_POINT('Ctrl Pts',(-2.3184019631086,1.00694689508425,42.5837112219291));
#93200=CARTESIAN_POINT('Ctrl Pts',(-2.37485371717826,0.11080766793254,42.6440714823197));
#93201=CARTESIAN_POINT('Ctrl Pts',(-2.37395592879609,0.00174106614345361,
42.6514101080949));
#93202=CARTESIAN_POINT('Ctrl Pts',(-2.37466860212234,0.00138350872013286,
41.848589891905));
#93203=CARTESIAN_POINT('Ctrl Pts',(-2.36977376777603,-0.705725647118399,
41.8962056481402));
#93204=CARTESIAN_POINT('Ctrl Pts',(-1.65899852223576,-2.2089365118431,41.9968548268713));
#93205=CARTESIAN_POINT('Ctrl Pts',(0.899455893833502,-2.65715799696691,
42.1505374280981));
#93206=CARTESIAN_POINT('Ctrl Pts',(2.72166609558782,-0.679737589018599,
42.3096376955853));
#93207=CARTESIAN_POINT('Ctrl Pts',(2.04316240585326,1.92223747469062,42.4687379630726));
#93208=CARTESIAN_POINT('Ctrl Pts',(-0.512634247617058,2.75802749333056,
42.6278382305599));
#93209=CARTESIAN_POINT('Ctrl Pts',(-2.17177139308421,1.40643705594649,42.7544555401707));
#93210=CARTESIAN_POINT('Ctrl Pts',(-2.37023527883011,0.308547980922129,
42.8280394272857));
#93211=CARTESIAN_POINT('Ctrl Pts',(-2.36862507619379,0.00137154188862704,
42.848589891905));
#93212=CARTESIAN_POINT('Origin',(0.,0.,-1.84858989190512));
#93213=CARTESIAN_POINT('',(-2.36809936427644,-0.000831359809205589,40.6514101080949));
#93214=CARTESIAN_POINT('',(-2.37294614192107,-0.00204842308417053,40.848589891905));
#93215=CARTESIAN_POINT('',(-2.37175,1.74448693060498E-12,-1.84858989190512));
#93216=CARTESIAN_POINT('Ctrl Pts',(-2.36809936427644,-0.000831359809205547,
40.6514101080949));
#93217=CARTESIAN_POINT('Ctrl Pts',(-2.36918130165799,-0.345836370295785,
40.6744785336017));
#93218=CARTESIAN_POINT('Ctrl Pts',(-2.13685539616662,-1.48243054976489,
40.750568593724));
#93219=CARTESIAN_POINT('Ctrl Pts',(-0.381792176989602,-2.77894951794198,
40.8796802884616));
#93220=CARTESIAN_POINT('Ctrl Pts',(2.13109066828147,-1.82394579229869,41.0387451923077));
#93221=CARTESIAN_POINT('Ctrl Pts',(2.68668721598173,0.806249026765786,41.1978100961539));
#93222=CARTESIAN_POINT('Ctrl Pts',(0.774713447708398,2.69594969604779,41.356875));
#93223=CARTESIAN_POINT('Ctrl Pts',(-1.71907271573948,2.13856614449093,41.5080750039804));
#93224=CARTESIAN_POINT('Ctrl Pts',(-2.36803884933291,0.669454089705716,
41.6062533733453));
#93225=CARTESIAN_POINT('Ctrl Pts',(-2.37374189642354,-0.0018225458993563,
41.6514101080949));
#93226=CARTESIAN_POINT('Ctrl Pts',(-2.37294614192107,-0.00204842308417049,
40.848589891905));
#93227=CARTESIAN_POINT('Ctrl Pts',(-2.37426493662659,-0.1465940308283,40.8583050240033));
#93228=CARTESIAN_POINT('Ctrl Pts',(-2.29631986144691,-1.07877289148818,
40.9210535785973));
#93229=CARTESIAN_POINT('Ctrl Pts',(-1.0613739399866,-2.59672772645004,41.036835555687));
#93230=CARTESIAN_POINT('Ctrl Pts',(1.6108193483455,-2.29668686433149,41.1959358231744));
#93231=CARTESIAN_POINT('Ctrl Pts',(2.80296395340346,0.113589619763061,41.3550360906616));
#93232=CARTESIAN_POINT('Ctrl Pts',(1.41969678881716,2.41949799620072,41.514136358149));
#93233=CARTESIAN_POINT('Ctrl Pts',(-1.2680123450661,2.50232975815682,41.6732366256362));
#93234=CARTESIAN_POINT('Ctrl Pts',(-2.33495267914215,0.949290687493702,
41.7847211368882));
#93235=CARTESIAN_POINT('Ctrl Pts',(-2.37522553077338,0.0818375793671154,
41.8431722256445));
#93236=CARTESIAN_POINT('Ctrl Pts',(-2.37466860212234,0.00138350872013286,
41.848589891905));
#93237=CARTESIAN_POINT('Origin',(0.,0.,-1.84858989190512));
#93238=CARTESIAN_POINT('',(-2.37068477736474,0.00213317277161283,39.6514101080949));
#93239=CARTESIAN_POINT('',(-2.36788813682339,-0.000411074629237396,39.8485898919049));
#93240=CARTESIAN_POINT('',(-2.37175,1.74448693060498E-12,-1.84858989190512));
#93241=CARTESIAN_POINT('Ctrl Pts',(-2.37068477736474,0.00213317277161312,
39.6514101080949));
#93242=CARTESIAN_POINT('Ctrl Pts',(-2.36573670528941,-0.568682495493336,
39.6896820592428));
#93243=CARTESIAN_POINT('Ctrl Pts',(-1.87205793886815,-1.93797744307223,
39.780975645006));
#93244=CARTESIAN_POINT('Ctrl Pts',(0.419312947294725,-2.77353607186051,
39.9252908653846));
#93245=CARTESIAN_POINT('Ctrl Pts',(2.55975730711914,-1.14715657969204,40.0843557692308));
#93246=CARTESIAN_POINT('Ctrl Pts',(2.34920929627571,1.53282137640764,40.243420673077));
#93247=CARTESIAN_POINT('Ctrl Pts',(-0.0189546406110363,2.80498955635841,
40.4024855769231));
#93248=CARTESIAN_POINT('Ctrl Pts',(-2.02879098398741,1.6900544618181,40.5384820552624));
#93249=CARTESIAN_POINT('Ctrl Pts',(-2.36669452212011,0.447140575662978,
40.6214568989864));
#93250=CARTESIAN_POINT('Ctrl Pts',(-2.36809936427644,-0.000831359809205547,
40.6514101080949));
#93251=CARTESIAN_POINT('Ctrl Pts',(-2.36788813682339,-0.000411074629237465,
39.848589891905));
#93252=CARTESIAN_POINT('Ctrl Pts',(-2.36846131194098,-0.372112408727876,
39.873437822362));
#93253=CARTESIAN_POINT('Ctrl Pts',(-2.11068491643285,-1.5363911068291,39.9513191753148));
#93254=CARTESIAN_POINT('Ctrl Pts',(-0.287782598693457,-2.79046424483211,
40.0822339507635));
#93255=CARTESIAN_POINT('Ctrl Pts',(2.19200382528608,-1.7506081102658,40.2413342182507));
#93256=CARTESIAN_POINT('Ctrl Pts',(2.65773921450559,0.897737040271954,40.400434485738));
#93257=CARTESIAN_POINT('Ctrl Pts',(0.681497836463564,2.72122586800371,40.5595347532253));
#93258=CARTESIAN_POINT('Ctrl Pts',(-1.76200449819908,2.0857339556845,40.7089198886142));
#93259=CARTESIAN_POINT('Ctrl Pts',(-2.36706583772652,0.642458367826052,
40.8052716015075));
#93260=CARTESIAN_POINT('Ctrl Pts',(-2.37294614192107,-0.00204842308417049,
40.848589891905));
#93261=CARTESIAN_POINT('Origin',(0.,0.,-1.84858989190512));
#93262=CARTESIAN_POINT('',(-2.37566466528284,-0.000126726877739107,38.6514101080949));
#93263=CARTESIAN_POINT('',(-2.37143269814177,0.00219190441036694,38.8485898919049));
#93264=CARTESIAN_POINT('',(-2.37175,1.74448693060498E-12,-1.84858989190512));
#93265=CARTESIAN_POINT('Ctrl Pts',(-2.37566466528284,-0.000126726877739423,
38.6514101080949));
#93266=CARTESIAN_POINT('Ctrl Pts',(-2.37566986853005,-0.00685892807482193,
38.6518639502684));
#93267=CARTESIAN_POINT('Ctrl Pts',(-2.37259066578177,-0.800098223903023,
38.7053394270573));
#93268=CARTESIAN_POINT('Ctrl Pts',(-1.49667178065217,-2.37240369049618,
38.8118365384616));
#93269=CARTESIAN_POINT('Ctrl Pts',(1.18621581231896,-2.54189255010612,38.9709014423077));
#93270=CARTESIAN_POINT('Ctrl Pts',(2.77963124440541,-0.376796808380384,
39.1299663461539));
#93271=CARTESIAN_POINT('Ctrl Pts',(1.82011252500328,2.13436549962901,39.28903125));
#93272=CARTESIAN_POINT('Ctrl Pts',(-0.811076648523027,2.68523376261753,
39.4480961538463));
#93273=CARTESIAN_POINT('Ctrl Pts',(-2.24349225668707,1.23071521996542,39.5688891065444));
#93274=CARTESIAN_POINT('Ctrl Pts',(-2.37259172212968,0.222120661590212,
39.6366604246274));
#93275=CARTESIAN_POINT('Ctrl Pts',(-2.37068477736474,0.00213317277161312,
39.6514101080949));
#93276=CARTESIAN_POINT('Ctrl Pts',(-2.37143269814177,0.00219190441036694,
38.8485898919049));
#93277=CARTESIAN_POINT('Ctrl Pts',(-2.3659851360241,-0.593631435472327,
38.8885706207208));
#93278=CARTESIAN_POINT('Ctrl Pts',(-1.83605691347221,-1.98843277321527,
38.9815847720324));
#93279=CARTESIAN_POINT('Ctrl Pts',(0.509066002639091,-2.75868833519739,
39.1276323458398));
#93280=CARTESIAN_POINT('Ctrl Pts',(2.5960406803649,-1.06305329672964,39.286732613327));
#93281=CARTESIAN_POINT('Ctrl Pts',(2.29772827133774,1.60933350082956,39.4458328808143));
#93282=CARTESIAN_POINT('Ctrl Pts',(-0.111776622438346,2.80303683751629,
39.6049331483016));
#93283=CARTESIAN_POINT('Ctrl Pts',(-2.05830785667968,1.63706408555562,39.7391854853318));
#93284=CARTESIAN_POINT('Ctrl Pts',(-2.3672379731109,0.42121699661448,39.8204043998662));
#93285=CARTESIAN_POINT('Ctrl Pts',(-2.36788813682339,-0.000411074629237465,
39.848589891905));
#93286=CARTESIAN_POINT('Origin',(0.,0.,-1.84858989190512));
#93287=CARTESIAN_POINT('',(-2.37030381846627,-0.00206907782623366,37.6514101080949));
#93288=CARTESIAN_POINT('',(-2.37550954347348,-0.000573603921870391,37.848589891905));
#93289=CARTESIAN_POINT('',(-2.37175,1.74448693060498E-12,-1.84858989190512));
#93290=CARTESIAN_POINT('Ctrl Pts',(-2.37030381846627,-0.00206907782623399,
37.6514101080949));
#93291=CARTESIAN_POINT('Ctrl Pts',(-2.37224375248416,-0.235689518460821,
37.6670674759094));
#93292=CARTESIAN_POINT('Ctrl Pts',(-2.23305719905348,-1.25817407212943,
37.7357464783394));
#93293=CARTESIAN_POINT('Ctrl Pts',(-0.765017314006785,-2.69871713948505,
37.8574471153846));
#93294=CARTESIAN_POINT('Ctrl Pts',(1.8563621592982,-2.10291350825614,38.0165120192308));
#93295=CARTESIAN_POINT('Ctrl Pts',(2.77277793875275,0.424297292056489,38.175576923077));
#93296=CARTESIAN_POINT('Ctrl Pts',(1.14255394050895,2.56181501726957,38.3346418269231));
#93297=CARTESIAN_POINT('Ctrl Pts',(-1.5293958672604,2.34706495701738,38.4932528885958));
#93298=CARTESIAN_POINT('Ctrl Pts',(-2.37506198171684,0.77965306411788,38.598842315653));
#93299=CARTESIAN_POINT('Ctrl Pts',(-2.37566466528284,-0.000126726877739423,
38.6514101080949));
#93300=CARTESIAN_POINT('Ctrl Pts',(-2.37550954347348,-0.000573603921870361,
37.848589891905));
#93301=CARTESIAN_POINT('Ctrl Pts',(-2.3756097420714,-0.031434860913138,
37.8506699965838));
#93302=CARTESIAN_POINT('Ctrl Pts',(-2.3610602581339,-0.849024312195104,
37.9057835237585));
#93303=CARTESIAN_POINT('Ctrl Pts',(-1.42282549133698,-2.4176594356937,38.0139304734288));
#93304=CARTESIAN_POINT('Ctrl Pts',(1.26477424157903,-2.50396797975438,38.1730307409161));
#93305=CARTESIAN_POINT('Ctrl Pts',(2.79027752164898,-0.289587427174506,
38.3321310084034));
#93306=CARTESIAN_POINT('Ctrl Pts',(1.75202554503676,2.1908710631472,38.4912312758906));
#93307=CARTESIAN_POINT('Ctrl Pts',(-0.896017811135028,2.6583193201581,38.650331543378));
#93308=CARTESIAN_POINT('Ctrl Pts',(-2.26223403332359,1.17957625462007,38.7694510820493));
#93309=CARTESIAN_POINT('Ctrl Pts',(-2.37321118897298,0.196713109330291,
38.835537198225));
#93310=CARTESIAN_POINT('Ctrl Pts',(-2.37143269814177,0.00219190441036694,
38.8485898919049));
#93311=CARTESIAN_POINT('Origin',(0.,0.,-1.84858989190512));
#93312=CARTESIAN_POINT('',(-2.36825910754817,0.00103510087933,36.6514101080949));
#93313=CARTESIAN_POINT('',(-2.36969280013257,-0.00191020411530018,36.848589891905));
#93314=CARTESIAN_POINT('',(-2.37175,1.74448693060498E-12,-1.84858989190512));
#93315=CARTESIAN_POINT('Ctrl Pts',(-2.36825910754817,0.00103510087932999,
36.6514101080949));
#93316=CARTESIAN_POINT('Ctrl Pts',(-2.3664500239851,-0.460434164028738,
36.6822710015504));
#93317=CARTESIAN_POINT('Ctrl Pts',(-2.01311920287128,-1.71730605118079,
36.7661535296214));
#93318=CARTESIAN_POINT('Ctrl Pts',(0.0290376119636847,-2.8049032972229,
36.9030576923078));
#93319=CARTESIAN_POINT('Ctrl Pts',(2.37508990529535,-1.49240531741365,37.0621225961539));
#93320=CARTESIAN_POINT('Ctrl Pts',(2.53975639635982,1.19078257328104,37.2211875));
#93321=CARTESIAN_POINT('Ctrl Pts',(0.371800222537135,2.78030399132932,37.3802524038462));
#93322=CARTESIAN_POINT('Ctrl Pts',(-1.89062026807677,1.91116660406184,37.5236599398778));
#93323=CARTESIAN_POINT('Ctrl Pts',(-2.36567441887122,0.555435643107899,
37.6140458412941));
#93324=CARTESIAN_POINT('Ctrl Pts',(-2.37030381846627,-0.00206907782623399,
37.6514101080949));
#93325=CARTESIAN_POINT('Ctrl Pts',(-2.36969280013257,-0.00191020411530039,
36.848589891905));
#93326=CARTESIAN_POINT('Ctrl Pts',(-2.37162565500284,-0.258907628242798,
36.8658027949426));
#93327=CARTESIAN_POINT('Ctrl Pts',(-2.21449028033011,-1.30542157081352,
36.936049120476));
#93328=CARTESIAN_POINT('Ctrl Pts',(-0.685017475287161,-2.72034199768123,
37.0593288685051));
#93329=CARTESIAN_POINT('Ctrl Pts',(1.91826926971012,-2.04688850079404,37.2184291359924));
#93330=CARTESIAN_POINT('Ctrl Pts',(2.75901702502127,0.507281560319236,37.3775294034797));
#93331=CARTESIAN_POINT('Ctrl Pts',(1.06473220873587,2.59535254820565,37.536629670967));
#93332=CARTESIAN_POINT('Ctrl Pts',(-1.57290521304256,2.30264630586829,37.6936498337753));
#93333=CARTESIAN_POINT('Ctrl Pts',(-2.37305512324333,0.755390002953853,
37.7976365740881));
#93334=CARTESIAN_POINT('Ctrl Pts',(-2.37550954347348,-0.000573603921870361,
37.848589891905));
#93335=CARTESIAN_POINT('Origin',(0.,0.,-1.84858989190512));
#93336=CARTESIAN_POINT('',(-2.37410637778804,0.00167730819971897,35.6514101080949));
#93337=CARTESIAN_POINT('',(-2.36858962871103,0.00134465207171072,35.848589891905));
#93338=CARTESIAN_POINT('',(-2.37175,1.74448693060498E-12,-1.84858989190512));
#93339=CARTESIAN_POINT('Ctrl Pts',(-2.37410637778804,0.00167730819971894,
35.6514101080949));
#93340=CARTESIAN_POINT('Ctrl Pts',(-2.36862023067477,-0.682818557534048,
35.6974745271915));
#93341=CARTESIAN_POINT('Ctrl Pts',(-1.69725896922413,-2.16457461681033,
35.7965605809035));
#93342=CARTESIAN_POINT('Ctrl Pts',(0.820724015952912,-2.68230083684112,
35.9486682692308));
#93343=CARTESIAN_POINT('Ctrl Pts',(2.70008778620931,-0.760165532265031,
36.107733173077));
#93344=CARTESIAN_POINT('Ctrl Pts',(2.09957357433953,1.86013883772571,36.2667980769231));
#93345=CARTESIAN_POINT('Ctrl Pts',(-0.429280266134804,2.77201084824496,
36.4258629807693));
#93346=CARTESIAN_POINT('Ctrl Pts',(-2.14972422622322,1.45497952790296,36.5540669911599));
#93347=CARTESIAN_POINT('Ctrl Pts',(-2.36955818311237,0.332409205377294,
36.6292493669351));
#93348=CARTESIAN_POINT('Ctrl Pts',(-2.36825910754817,0.00103510087932999,
36.6514101080949));
#93349=CARTESIAN_POINT('Ctrl Pts',(-2.36858962871103,0.00134465207171076,
35.848589891905));
#93350=CARTESIAN_POINT('Ctrl Pts',(-2.36610713128963,-0.482158267059727,
35.8809355933014));
#93351=CARTESIAN_POINT('Ctrl Pts',(-1.98670264463906,-1.76198154825171,
35.9663147171935));
#93352=CARTESIAN_POINT('Ctrl Pts',(0.108150488259582,-2.80317908769424,
36.1047272635815));
#93353=CARTESIAN_POINT('Ctrl Pts',(2.41673863807743,-1.42438895004866,36.2638275310687));
#93354=CARTESIAN_POINT('Ctrl Pts',(2.50478551939227,1.26315439580437,36.422927798556));
#93355=CARTESIAN_POINT('Ctrl Pts',(0.291392134504392,2.79008963113125,36.5820280660433));
#93356=CARTESIAN_POINT('Ctrl Pts',(-1.92130639744127,1.86559611804953,36.723915430493));
#93357=CARTESIAN_POINT('Ctrl Pts',(-2.36567047656874,0.532908426508661,
36.8127693724468));
#93358=CARTESIAN_POINT('Ctrl Pts',(-2.36969280013257,-0.00191020411530039,
36.848589891905));
#93359=CARTESIAN_POINT('Origin',(0.,0.,-1.84858989190512));
#93360=CARTESIAN_POINT('',(-2.37358262552183,-0.00187676788449481,34.6514101080949));
#93361=CARTESIAN_POINT('',(-2.37462230926531,0.00141218416469555,34.848589891905));
#93362=CARTESIAN_POINT('',(-2.37175,1.74448693060498E-12,-1.84858989190512));
#93363=CARTESIAN_POINT('Ctrl Pts',(-2.37358262552183,-0.0018767678844951,
34.6514101080949));
#93364=CARTESIAN_POINT('Ctrl Pts',(-2.37464472099243,-0.12448352171728,
34.6596564182171));
#93365=CARTESIAN_POINT('Ctrl Pts',(-2.31018163025135,-1.0343001918437,34.7209243629547));
#93366=CARTESIAN_POINT('Ctrl Pts',(-1.13333760403503,-2.56590560328329,
34.8352139423077));
#93367=CARTESIAN_POINT('Ctrl Pts',(1.54546611079131,-2.34091012003366,34.9942788461539));
#93368=CARTESIAN_POINT('Ctrl Pts',(2.80484657580764,0.0340789650750163,
35.15334375));
#93369=CARTESIAN_POINT('Ctrl Pts',(1.48813403299161,2.37776844741717,35.3124086538462));
#93370=CARTESIAN_POINT('Ctrl Pts',(-1.1953454874454,2.53761203798461,35.4714735576924));
#93371=CARTESIAN_POINT('Ctrl Pts',(-2.32177929342658,0.99545829170247,35.5844740424419));
#93372=CARTESIAN_POINT('Ctrl Pts',(-2.37493496324691,0.105058298409406,
35.6444528925761));
#93373=CARTESIAN_POINT('Ctrl Pts',(-2.37410637778804,0.00167730819971894,
35.6514101080949));
#93374=CARTESIAN_POINT('Ctrl Pts',(-2.37462230926531,0.00141218416469564,
34.848589891905));
#93375=CARTESIAN_POINT('Ctrl Pts',(-2.36966193302837,-0.703694807005961,
34.8960683916601));
#93376=CARTESIAN_POINT('Ctrl Pts',(-1.66242402158611,-2.20504314783441,
34.9965803139111));
#93377=CARTESIAN_POINT('Ctrl Pts',(0.892578229012262,-2.65947619483432,
35.1501256586578));
#93378=CARTESIAN_POINT('Ctrl Pts',(2.71989835531262,-0.686776865193377,
35.3092259261451));
#93379=CARTESIAN_POINT('Ctrl Pts',(2.04812882046954,1.91694492893226,35.4683261936323));
#93380=CARTESIAN_POINT('Ctrl Pts',(-0.505496905774109,2.75934456058861,
35.6274264611197));
#93381=CARTESIAN_POINT('Ctrl Pts',(-2.16992769404118,1.41059069964949,35.7541810272105));
#93382=CARTESIAN_POINT('Ctrl Pts',(-2.37017738881721,0.310584307107474,
35.8279021708056));
#93383=CARTESIAN_POINT('Ctrl Pts',(-2.36858962871103,0.00134465207171076,
35.848589891905));
#93384=CARTESIAN_POINT('Origin',(0.,0.,-1.84858989190512));
#93385=CARTESIAN_POINT('',(-2.36804291379594,-0.000743081082047163,33.6514101080949));
#93386=CARTESIAN_POINT('',(-2.37300722762269,-0.00203526771887147,33.848589891905));
#93387=CARTESIAN_POINT('',(-2.37175,1.74448693060498E-12,-1.84858989190512));
#93388=CARTESIAN_POINT('Ctrl Pts',(-2.36804291379594,-0.000743081082047181,
33.6514101080949));
#93389=CARTESIAN_POINT('Ctrl Pts',(-2.36902463128789,-0.351473225448641,
33.6748599438582));
#93390=CARTESIAN_POINT('Ctrl Pts',(-2.13135450972719,-1.49396215643721,
33.7513314142368));
#93391=CARTESIAN_POINT('Ctrl Pts',(-0.361803463717808,-2.78162253789443,
33.8808245192308));
#93392=CARTESIAN_POINT('Ctrl Pts',(2.14414858133226,-1.80857749373683,34.039889423077));
#93393=CARTESIAN_POINT('Ctrl Pts',(2.68082137390367,0.825543730459955,34.1989543269231));
#93394=CARTESIAN_POINT('Ctrl Pts',(0.755311294824669,2.70144971035752,34.3580192307693));
#93395=CARTESIAN_POINT('Ctrl Pts',(-1.72812275275069,2.12760307727921,34.5088378244932));
#93396=CARTESIAN_POINT('Ctrl Pts',(-2.36781572267268,0.663846095620685,
34.6066347836017));
#93397=CARTESIAN_POINT('Ctrl Pts',(-2.37358262552183,-0.0018767678844951,
34.6514101080949));
#93398=CARTESIAN_POINT('Ctrl Pts',(-2.37300722762269,-0.00203526771887147,
33.848589891905));
#93399=CARTESIAN_POINT('Ctrl Pts',(-2.37430298792658,-0.144529249187231,
33.8581677675232));
#93400=CARTESIAN_POINT('Ctrl Pts',(-2.29764386443108,-1.07463147152998,
33.9207790656371));
#93401=CARTESIAN_POINT('Ctrl Pts',(-1.06808869572879,-2.59397302681686,
34.0364237862468));
#93402=CARTESIAN_POINT('Ctrl Pts',(1.60487192110541,-2.30084672297929,34.1955240537341));
#93403=CARTESIAN_POINT('Ctrl Pts',(2.80324845369984,0.106337352922497,34.3546243212214));
#93404=CARTESIAN_POINT('Ctrl Pts',(1.425951812856,2.41581682939948,34.5137245887086));
#93405=CARTESIAN_POINT('Ctrl Pts',(-1.26153402157907,2.50560201113339,34.672824856196));
#93406=CARTESIAN_POINT('Ctrl Pts',(-2.33380736810732,0.953419897021398,
34.784446623928));
#93407=CARTESIAN_POINT('Ctrl Pts',(-2.37520266683563,0.0839087853630068,
34.8430349691644));
#93408=CARTESIAN_POINT('Ctrl Pts',(-2.37462230926531,0.00141218416469564,
34.848589891905));
#93409=CARTESIAN_POINT('Origin',(0.,0.,-1.84858989190512));
#93410=CARTESIAN_POINT('',(-2.37084923987159,0.00215313891885895,32.6514101080949));
#93411=CARTESIAN_POINT('',(-2.36789912899606,-0.000444447102319612,32.848589891905));
#93412=CARTESIAN_POINT('',(-2.37175,1.74448693060498E-12,-1.84858989190512));
#93413=CARTESIAN_POINT('Ctrl Pts',(-2.37084923987159,0.00215313891885871,
32.6514101080949));
#93414=CARTESIAN_POINT('Ctrl Pts',(-2.36577770381593,-0.574249672426079,
32.6900634694992));
#93415=CARTESIAN_POINT('Ctrl Pts',(-1.86414833270866,-1.94922154145056,
32.7817384655188));
#93416=CARTESIAN_POINT('Ctrl Pts',(0.439242037856295,-2.77044980497037,
32.9264350961539));
#93417=CARTESIAN_POINT('Ctrl Pts',(2.56793846593204,-1.12872393651732,33.0855));
#93418=CARTESIAN_POINT('Ctrl Pts',(2.33812859149225,1.54967105520072,33.2445649038462));
#93419=CARTESIAN_POINT('Ctrl Pts',(-0.0391202080950587,2.80478079339528,
33.4036298076924));
#93420=CARTESIAN_POINT('Ctrl Pts',(-2.03527486879144,1.67859243755198,33.5392448757752));
#93421=CARTESIAN_POINT('Ctrl Pts',(-2.36680490289919,0.441550902778074,
33.6218383092428));
#93422=CARTESIAN_POINT('Ctrl Pts',(-2.36804291379594,-0.000743081082047181,
33.6514101080949));
#93423=CARTESIAN_POINT('Ctrl Pts',(-2.36789912899606,-0.000444447102319855,
32.848589891905));
#93424=CARTESIAN_POINT('Ctrl Pts',(-2.36851557196465,-0.370088276800515,
32.873300565882));
#93425=CARTESIAN_POINT('Ctrl Pts',(-2.11274503704775,-1.53224491940183,
32.9510446623547));
#93426=CARTESIAN_POINT('Ctrl Pts',(-0.295001182690674,-2.78971034840684,
33.0818221813231));
#93427=CARTESIAN_POINT('Ctrl Pts',(2.18746727921893,-1.75627344913702,33.2409224488105));
#93428=CARTESIAN_POINT('Ctrl Pts',(2.66005296337403,0.890857877465394,33.4000227162977));
#93429=CARTESIAN_POINT('Ctrl Pts',(0.688535967781046,2.71945357505306,33.559122983785));
#93430=CARTESIAN_POINT('Ctrl Pts',(-1.75884896300695,2.08970758428599,33.7086453756541));
#93431=CARTESIAN_POINT('Ctrl Pts',(-2.3671282650142,0.644470715268389,33.8051343450274));
#93432=CARTESIAN_POINT('Ctrl Pts',(-2.37300722762269,-0.00203526771887147,
33.848589891905));
#93433=CARTESIAN_POINT('Origin',(0.,0.,-1.84858989190512));
#93434=CARTESIAN_POINT('',(-2.37564494446506,-0.000232844447847634,31.6514101080949));
#93435=CARTESIAN_POINT('',(-2.37137100238912,0.00219054532625537,31.848589891905));
#93436=CARTESIAN_POINT('',(-2.37175,1.74448693060498E-12,-1.84858989190512));
#93437=CARTESIAN_POINT('Ctrl Pts',(-2.37564494446506,-0.000232844447847528,
31.6514101080949));
#93438=CARTESIAN_POINT('Ctrl Pts',(-2.37566221911256,-0.0126230839183631,
31.6522453605248));
#93439=CARTESIAN_POINT('Ctrl Pts',(-2.36995459238346,-0.811526557648796,
31.7061022475701));
#93440=CARTESIAN_POINT('Ctrl Pts',(-1.4795770558054,-2.38310247904171,31.8129807692308));
#93441=CARTESIAN_POINT('Ctrl Pts',(1.20445971643178,-2.53329873508307,31.972045673077));
#93442=CARTESIAN_POINT('Ctrl Pts',(2.78226833327609,-0.356803323035994,
32.1311105769231));
#93443=CARTESIAN_POINT('Ctrl Pts',(1.80472078159196,2.14739576933795,32.2901754807693));
#93444=CARTESIAN_POINT('Ctrl Pts',(-0.83036077806552,2.67933325062988,32.4492403846154));
#93445=CARTESIAN_POINT('Ctrl Pts',(-2.24779252756098,1.21917927701057,32.5696519270573));
#93446=CARTESIAN_POINT('Ctrl Pts',(-2.3727344372516,0.216414273582911,32.6370418348838));
#93447=CARTESIAN_POINT('Ctrl Pts',(-2.37084923987159,0.00215313891885871,
32.6514101080949));
#93448=CARTESIAN_POINT('Ctrl Pts',(-2.37137100238912,0.00219054532625535,
31.848589891905));
#93449=CARTESIAN_POINT('Ctrl Pts',(-2.36595764621499,-0.591626673288607,
31.8884333642407));
#93450=CARTESIAN_POINT('Ctrl Pts',(-1.83899320124287,-1.98440542455834,
31.9813102590722));
#93451=CARTESIAN_POINT('Ctrl Pts',(0.501926962994743,-2.75999616840604,
32.1272205763995));
#93452=CARTESIAN_POINT('Ctrl Pts',(2.59328163816445,-1.06976626931127,32.2863208438868));
#93453=CARTESIAN_POINT('Ctrl Pts',(2.30188428228449,1.60338338421251,32.445421111374));
#93454=CARTESIAN_POINT('Ctrl Pts',(-0.104524173098342,2.80331664694433,
32.6045213788614));
#93455=CARTESIAN_POINT('Ctrl Pts',(-2.05605868746136,1.64119699270093,32.7389109723716));
#93456=CARTESIAN_POINT('Ctrl Pts',(-2.36719257768177,0.423231946338964,
32.8202671433862));
#93457=CARTESIAN_POINT('Ctrl Pts',(-2.36789912899606,-0.000444447102319855,
32.848589891905));
#93458=CARTESIAN_POINT('Origin',(0.,0.,-1.84858989190512));
#93459=CARTESIAN_POINT('',(-2.3701487589333,-0.00203535903446658,30.6514101080949));
#93460=CARTESIAN_POINT('',(-2.37553023271479,-0.000536704938520205,30.848589891905));
#93461=CARTESIAN_POINT('',(-2.37175,1.74448693060498E-12,-1.84858989190512));
#93462=CARTESIAN_POINT('Ctrl Pts',(-2.3701487589333,-0.00203535903446656,
30.6514101080949));
#93463=CARTESIAN_POINT('Ctrl Pts',(-2.37209433753784,-0.241386337143971,
30.6674488861659));
#93464=CARTESIAN_POINT('Ctrl Pts',(-2.22858721340341,-1.26971431685246,
30.7365092988522));
#93465=CARTESIAN_POINT('Ctrl Pts',(-0.74559551558228,-2.70414737335524,
30.8585913461539));
#93466=CARTESIAN_POINT('Ctrl Pts',(1.87143276947021,-2.08951312009126,31.01765625));
#93467=CARTESIAN_POINT('Ctrl Pts',(2.76965585724649,0.444220803318177,31.1767211538462));
#93468=CARTESIAN_POINT('Ctrl Pts',(1.12410662268099,2.56996303291023,31.3357860576923));
#93469=CARTESIAN_POINT('Ctrl Pts',(-1.53980888886202,2.33657152166105,31.4940157091086));
#93470=CARTESIAN_POINT('Ctrl Pts',(-2.3745656284112,0.773906504598037,31.5992237259095));
#93471=CARTESIAN_POINT('Ctrl Pts',(-2.37564494446506,-0.000232844447847528,
31.6514101080949));
#93472=CARTESIAN_POINT('Ctrl Pts',(-2.37553023271479,-0.000536704938520552,
30.848589891905));
#93473=CARTESIAN_POINT('Ctrl Pts',(-2.37561831176314,-0.0293608987698828,
30.8505327401037));
#93474=CARTESIAN_POINT('Ctrl Pts',(-2.36206334805178,-0.844906819600521,
30.9055090107983));
#93475=CARTESIAN_POINT('Ctrl Pts',(-1.42907574814251,-2.41397018040158,
31.0135187039885));
#93476=CARTESIAN_POINT('Ctrl Pts',(1.25829169048848,-2.50723184955934,31.1726189714758));
#93477=CARTESIAN_POINT('Ctrl Pts',(2.78951895635884,-0.296805522037135,
31.3317192389631));
#93478=CARTESIAN_POINT('Ctrl Pts',(1.75768794845828,2.18633085365451,31.4908195064504));
#93479=CARTESIAN_POINT('Ctrl Pts',(-0.889137153221077,2.66062861905961,
31.6499197739376));
#93480=CARTESIAN_POINT('Ctrl Pts',(-2.26075327480318,1.18372539029748,31.7691765690892));
#93481=CARTESIAN_POINT('Ctrl Pts',(-2.37316306251715,0.198770287465469,
31.835399941745));
#93482=CARTESIAN_POINT('Ctrl Pts',(-2.37137100238912,0.00219054532625535,
31.848589891905));
#93483=CARTESIAN_POINT('Origin',(0.,0.,-1.84858989190512));
#93484=CARTESIAN_POINT('',(-2.36833667409033,0.00111765679201713,29.6514101080949));
#93485=CARTESIAN_POINT('',(-2.36974424005732,-0.00192697225866761,29.848589891905));
#93486=CARTESIAN_POINT('',(-2.37175,1.74448693060498E-12,-1.84858989190512));
#93487=CARTESIAN_POINT('Ctrl Pts',(-2.36833667409033,0.00111765679201677,
29.6514101080949));
#93488=CARTESIAN_POINT('Ctrl Pts',(-2.36635541735129,-0.466016676365621,
29.6826524118069));
#93489=CARTESIAN_POINT('Ctrl Pts',(-2.00643187356775,-1.72874566519355,
29.7669163501342));
#93490=CARTESIAN_POINT('Ctrl Pts',(0.0492022987188458,-2.80462204645853,
29.9042019230769));
#93491=CARTESIAN_POINT('Ctrl Pts',(2.38575795131293,-1.47529139068443,30.0632668269231));
#93492=CARTESIAN_POINT('Ctrl Pts',(2.53112980449082,1.20901100181045,30.2223317307692));
#93493=CARTESIAN_POINT('Ctrl Pts',(0.351802029708706,2.78290514059918,30.3813966346154));
#93494=CARTESIAN_POINT('Ctrl Pts',(-1.89831104124899,1.89987965715743,30.5244227603906));
#93495=CARTESIAN_POINT('Ctrl Pts',(-2.36566256590104,0.54986970805048,30.6144272515505));
#93496=CARTESIAN_POINT('Ctrl Pts',(-2.3701487589333,-0.00203535903446656,
30.6514101080949));
#93497=CARTESIAN_POINT('Ctrl Pts',(-2.36974424005732,-0.00192697225866751,
29.848589891905));
#93498=CARTESIAN_POINT('Ctrl Pts',(-2.37168135840376,-0.256861139499681,
29.8656655384625));
#93499=CARTESIAN_POINT('Ctrl Pts',(-2.21616148860617,-1.30126756262755,
29.9357746075158));
#93500=CARTESIAN_POINT('Ctrl Pts',(-0.692053308057238,-2.71856060160596,
30.0589170990649));
#93501=CARTESIAN_POINT('Ctrl Pts',(1.91296709700241,-2.05184463631711,30.2180173665521));
#93502=CARTESIAN_POINT('Ctrl Pts',(2.76032024038351,0.500141676254002,30.3771176340394));
#93503=CARTESIAN_POINT('Ctrl Pts',(1.07144339534857,2.59258916459223,30.5362179015267));
#93504=CARTESIAN_POINT('Ctrl Pts',(-1.56924879404274,2.30645815426358,30.6933753208152));
#93505=CARTESIAN_POINT('Ctrl Pts',(-2.37321404086479,0.757445631218895,
30.797499317608));
#93506=CARTESIAN_POINT('Ctrl Pts',(-2.37553023271479,-0.000536704938520552,
30.848589891905));
#93507=CARTESIAN_POINT('Origin',(0.,0.,-1.84858989190512));
#93508=CARTESIAN_POINT('',(-2.37425246554842,0.00160971056243236,28.6514101080949));
#93509=CARTESIAN_POINT('',(-2.36855491481223,0.00131744329006256,28.848589891905));
#93510=CARTESIAN_POINT('',(-2.37175,1.74448693060498E-12,-1.84858989190512));
#93511=CARTESIAN_POINT('Ctrl Pts',(-2.37425246554842,0.00160971056243232,
28.6514101080949));
#93512=CARTESIAN_POINT('Ctrl Pts',(-2.36888615690045,-0.688442751284159,
28.6978559374479));
#93513=CARTESIAN_POINT('Ctrl Pts',(-1.6879762329752,-2.17546809508341,28.7973234014163));
#93514=CARTESIAN_POINT('Ctrl Pts',(0.839986810335585,-2.67633104233065,
28.9498125000001));
#93515=CARTESIAN_POINT('Ctrl Pts',(2.70548310349,-0.740734005166865,29.1088774038461));
#93516=CARTESIAN_POINT('Ctrl Pts',(2.08614612062029,1.87518533833364,29.2679423076924));
#93517=CARTESIAN_POINT('Ctrl Pts',(-0.449198133734217,2.7688529622084,29.4270072115385));
#93518=CARTESIAN_POINT('Ctrl Pts',(-2.15503896555959,1.44344170040664,29.5548298116727));
#93519=CARTESIAN_POINT('Ctrl Pts',(-2.3697178285187,0.32676179981013,29.6296307771915));
#93520=CARTESIAN_POINT('Ctrl Pts',(-2.36833667409033,0.00111765679201677,
29.6514101080949));
#93521=CARTESIAN_POINT('Ctrl Pts',(-2.36855491481223,0.00131744329006263,
28.848589891905));
#93522=CARTESIAN_POINT('Ctrl Pts',(-2.3661350789471,-0.480151430218069,
28.8807983368213));
#93523=CARTESIAN_POINT('Ctrl Pts',(-1.98917995276845,-1.75787348496187,
28.9660402042334));
#93524=CARTESIAN_POINT('Ctrl Pts',(0.10089768302309,-2.80344951503636,29.1043154941412));
#93525=CARTESIAN_POINT('Ctrl Pts',(2.41304534085417,-1.43063681931478,29.2634157616285));
#93526=CARTESIAN_POINT('Ctrl Pts',(2.50804519556235,1.25666973497962,29.4225160291157));
#93527=CARTESIAN_POINT('Ctrl Pts',(0.298609737212693,2.78932639729359,29.581616296603));
#93528=CARTESIAN_POINT('Ctrl Pts',(-1.91861604566399,1.86967193881861,29.7236409175328));
#93529=CARTESIAN_POINT('Ctrl Pts',(-2.36566506992268,0.534911596855939,
29.8126321159668));
#93530=CARTESIAN_POINT('Ctrl Pts',(-2.36974424005732,-0.00192697225866751,
29.848589891905));
#93531=CARTESIAN_POINT('Origin',(0.,0.,-1.84858989190512));
#93532=CARTESIAN_POINT('',(-2.37342029013076,-0.00192684023212259,27.6514101080949));
#93533=CARTESIAN_POINT('',(-2.37457526090586,0.00144042296748297,27.848589891905));
#93534=CARTESIAN_POINT('',(-2.37175,1.74448693060498E-12,-1.84858989190512));
#93535=CARTESIAN_POINT('Ctrl Pts',(-2.37342029013076,-0.00192684023212316,
27.6514101080949));
#93536=CARTESIAN_POINT('Ctrl Pts',(-2.37455049002191,-0.130227195499285,
27.6600378284736));
#93537=CARTESIAN_POINT('Ctrl Pts',(-2.30665001943632,-1.04579922342617,
27.7216871834676));
#93538=CARTESIAN_POINT('Ctrl Pts',(-1.1148611157287,-2.57398725372069,27.8363581730769));
#93539=CARTESIAN_POINT('Ctrl Pts',(1.56225579709783,-2.32973872228513,27.9954230769231));
#93540=CARTESIAN_POINT('Ctrl Pts',(2.80452908244698,0.0542431137526706,
28.1544879807693));
#93541=CARTESIAN_POINT('Ctrl Pts',(1.47100095966601,2.38840571644395,28.3135528846154));
#93542=CARTESIAN_POINT('Ctrl Pts',(-1.21355838150491,2.52895269713762,28.4726177884615));
#93543=CARTESIAN_POINT('Ctrl Pts',(-2.3251114613213,0.98397290416047,28.5852368629547));
#93544=CARTESIAN_POINT('Ctrl Pts',(-2.37501222807476,0.0993074085722678,
28.6448343028325));
#93545=CARTESIAN_POINT('Ctrl Pts',(-2.37425246554842,0.00160971056243232,
28.6514101080949));
#93546=CARTESIAN_POINT('Ctrl Pts',(-2.37457526090586,0.0014404229674831,
27.848589891905));
#93547=CARTESIAN_POINT('Ctrl Pts',(-2.36955185362383,-0.701664761427417,
27.8959311351801));
#93548=CARTESIAN_POINT('Ctrl Pts',(-1.665840495116,-2.20114684206871,27.9963058009509));
#93549=CARTESIAN_POINT('Ctrl Pts',(0.885694589519864,-2.66177659090546,
28.1497138892175));
#93550=CARTESIAN_POINT('Ctrl Pts',(2.71811240879197,-0.693811544274251,
28.3088141567048));
#93551=CARTESIAN_POINT('Ctrl Pts',(2.05308152547941,1.91163955167607,28.4679144241921));
#93552=CARTESIAN_POINT('Ctrl Pts',(-0.498356180275029,2.76064315755925,
28.6270146916793));
#93553=CARTESIAN_POINT('Ctrl Pts',(-2.16807702738258,1.41474422731526,28.7539065142503));
#93554=CARTESIAN_POINT('Ctrl Pts',(-2.37011950533401,0.312620224969389,
28.8277649143255));
#93555=CARTESIAN_POINT('Ctrl Pts',(-2.36855491481223,0.00131744329006263,
28.848589891905));
#93556=CARTESIAN_POINT('Origin',(0.,0.,-1.84858989190512));
#93557=CARTESIAN_POINT('',(-2.36799289882491,-0.000653459418386054,26.6514101080949));
#93558=CARTESIAN_POINT('',(-2.37306808171561,-0.00202154815997113,26.848589891905));
#93559=CARTESIAN_POINT('',(-2.37175,1.74448693060498E-12,-1.84858989190512));
#93560=CARTESIAN_POINT('Ctrl Pts',(-2.36799289882491,-0.000653459418386224,
26.6514101080949));
#93561=CARTESIAN_POINT('Ctrl Pts',(-2.36886921458804,-0.357106994699224,
26.6752413541146));
#93562=CARTESIAN_POINT('Ctrl Pts',(-2.12579799293791,-1.50549148658124,
26.7520942347496));
#93563=CARTESIAN_POINT('Ctrl Pts',(-0.34179604974745,-2.78415178286989,
26.8819687500001));
#93564=CARTESIAN_POINT('Ctrl Pts',(2.15709566880955,-1.79311571441545,27.0410336538462));
#93565=CARTESIAN_POINT('Ctrl Pts',(2.67481696700378,0.844795763903405,27.2000985576923));
#93566=CARTESIAN_POINT('Ctrl Pts',(0.73587010182595,2.70681009361926,27.3591634615385));
#93567=CARTESIAN_POINT('Ctrl Pts',(-1.73710433416866,2.11662034428545,27.509600645006));
#93568=CARTESIAN_POINT('Ctrl Pts',(-2.36760484933805,0.65824232593481,27.6070161938582));
#93569=CARTESIAN_POINT('Ctrl Pts',(-2.37342029013076,-0.00192684023212316,
27.6514101080949));
#93570=CARTESIAN_POINT('Ctrl Pts',(-2.37306808171561,-0.00202154815997103,
26.848589891905));
#93571=CARTESIAN_POINT('Ctrl Pts',(-2.37434058588056,-0.142464205890787,
26.8580305110431));
#93572=CARTESIAN_POINT('Ctrl Pts',(-2.29896181857628,-1.07049040953162,
26.920504552677));
#93573=CARTESIAN_POINT('Ctrl Pts',(-1.07479630198138,-2.59120096384751,
27.0360120168066));
#93574=CARTESIAN_POINT('Ctrl Pts',(1.59891375129768,-2.30499118039708,27.1951122842938));
#93575=CARTESIAN_POINT('Ctrl Pts',(2.80351418982834,0.0990843742891699,
27.3542125517811));
#93576=CARTESIAN_POINT('Ctrl Pts',(1.43219729196881,2.41211949179022,27.5133128192684));
#93577=CARTESIAN_POINT('Ctrl Pts',(-1.25504725373308,2.50885749230484,27.6724130867557));
#93578=CARTESIAN_POINT('Ctrl Pts',(-2.33265631141876,0.957549547268701,
27.7841721109679));
#93579=CARTESIAN_POINT('Ctrl Pts',(-2.37517926140458,0.085979831814631,
27.8428977126843));
#93580=CARTESIAN_POINT('Ctrl Pts',(-2.37457526090586,0.0014404229674831,
27.848589891905));
#93581=CARTESIAN_POINT('Origin',(0.,0.,-1.84858989190512));
#93582=CARTESIAN_POINT('',(-2.37101590433324,0.00216888848020844,25.6514101080949));
#93583=CARTESIAN_POINT('',(-2.36791098026206,-0.000477715941999413,25.848589891905));
#93584=CARTESIAN_POINT('',(-2.37175,1.74448693060498E-12,-1.84858989190512));
#93585=CARTESIAN_POINT('Ctrl Pts',(-2.37101590433324,0.00216888848020831,
25.6514101080949));
#93586=CARTESIAN_POINT('Ctrl Pts',(-2.36582777414831,-0.579817597934016,
25.6904448797556));
#93587=CARTESIAN_POINT('Ctrl Pts',(-1.85617349906383,-1.96045219094367,
25.7825012860316));
#93588=CARTESIAN_POINT('Ctrl Pts',(0.459148425116812,-2.76722034059328,
25.9275793269231));
#93589=CARTESIAN_POINT('Ctrl Pts',(2.57598689455279,-1.11023295248012,26.0866442307693));
#93590=CARTESIAN_POINT('Ctrl Pts',(2.32692703480318,1.56644063544793,26.2457091346154));
#93591=CARTESIAN_POINT('Ctrl Pts',(-0.0592837535552358,2.80442705846396,
26.4047740384616));
#93592=CARTESIAN_POINT('Ctrl Pts',(-2.04169909775158,1.66712437431943,26.5400076962881));
#93593=CARTESIAN_POINT('Ctrl Pts',(-2.36691951820364,0.435958927638278,
26.6222197194992));
#93594=CARTESIAN_POINT('Ctrl Pts',(-2.36799289882491,-0.000653459418386224,
26.6514101080949));
#93595=CARTESIAN_POINT('Ctrl Pts',(-2.36791098026206,-0.000477715941999204,
25.848589891905));
#93596=CARTESIAN_POINT('Ctrl Pts',(-2.36857006946863,-0.36806375603213,
25.8731633094019));
#93597=CARTESIAN_POINT('Ctrl Pts',(-2.11479784456769,-1.52809834734262,
25.9507701493945));
#93598=CARTESIAN_POINT('Ctrl Pts',(-0.302217792031812,-2.78893777843403,
26.0814104118829));
#93599=CARTESIAN_POINT('Ctrl Pts',(2.18291609085233,-1.76192703200078,26.2405106793702));
#93600=CARTESIAN_POINT('Ctrl Pts',(2.66234890658549,0.883972751503175,26.3996109468574));
#93601=CARTESIAN_POINT('Ctrl Pts',(0.695569490229732,2.71766307883422,26.5587112143448));
#93602=CARTESIAN_POINT('Ctrl Pts',(-1.75568464583691,2.09367884994919,26.7083708626939));
#93603=CARTESIAN_POINT('Ctrl Pts',(-2.3671921933842,0.646483499224386,26.8049970885473));
#93604=CARTESIAN_POINT('Ctrl Pts',(-2.37306808171561,-0.00202154815997103,
26.848589891905));
#93605=CARTESIAN_POINT('Origin',(0.,0.,-1.84858989190512));
#93606=CARTESIAN_POINT('',(-2.37561413348328,-0.000338293417154348,24.6514101080949));
#93607=CARTESIAN_POINT('',(-2.3713094773117,0.00218862049173575,24.848589891905));
#93608=CARTESIAN_POINT('',(-2.37175,1.74448693060498E-12,-1.84858989190512));
#93609=CARTESIAN_POINT('Ctrl Pts',(-2.37561413348328,-0.00033829341715417,
24.6514101080949));
#93610=CARTESIAN_POINT('Ctrl Pts',(-2.37565004965548,-0.0183870501238682,
24.6526267707812));
#93611=CARTESIAN_POINT('Ctrl Pts',(-2.36727666328559,-0.822958632995309,
24.7068650680829));
#93612=CARTESIAN_POINT('Ctrl Pts',(-1.46240585539294,-2.39367809109597,
24.8141250000001));
#93613=CARTESIAN_POINT('Ctrl Pts',(1.2226413650927,-2.52457398030731,24.9731899038461));
#93614=CARTESIAN_POINT('Ctrl Pts',(2.78476161379025,-0.336791395437584,
25.1322548076924));
#93615=CARTESIAN_POINT('Ctrl Pts',(1.78923575676476,2.16031504563452,25.2913197115385));
#93616=CARTESIAN_POINT('Ctrl Pts',(-0.849601988376427,2.6732942507377,25.4503846153846));
#93617=CARTESIAN_POINT('Ctrl Pts',(-2.25204311898601,1.2076448752048,25.5704147475701));
#93618=CARTESIAN_POINT('Ctrl Pts',(-2.37287490498319,0.21070514681249,25.6374232451402));
#93619=CARTESIAN_POINT('Ctrl Pts',(-2.37101590433324,0.00216888848020831,
25.6514101080949));
#93620=CARTESIAN_POINT('Ctrl Pts',(-2.3713094773117,0.00218862049173589,
24.848589891905));
#93621=CARTESIAN_POINT('Ctrl Pts',(-2.36593141354757,-0.589622083083144,
24.8882961077606));
#93622=CARTESIAN_POINT('Ctrl Pts',(-1.84192095452906,-1.98037618738568,
24.981035746112));
#93623=CARTESIAN_POINT('Ctrl Pts',(0.494784563590454,-2.76128552696561,
25.1268088069592));
#93624=CARTESIAN_POINT('Ctrl Pts',(2.59050523725581,-1.07647208117411,25.2859090744465));
#93625=CARTESIAN_POINT('Ctrl Pts',(2.30602488505606,1.59742253499168,25.4450093419338));
#93626=CARTESIAN_POINT('Ctrl Pts',(-0.0972710241024927,2.80357769174802,
25.6041096094211));
#93627=CARTESIAN_POINT('Ctrl Pts',(-2.05380189715669,1.64532922764933,25.7386364594115));
#93628=CARTESIAN_POINT('Ctrl Pts',(-2.3671476480102,0.425246566804615,25.8201298869061));
#93629=CARTESIAN_POINT('Ctrl Pts',(-2.36791098026206,-0.000477715941999204,
25.848589891905));
#93630=CARTESIAN_POINT('Origin',(0.,0.,-1.84858989190512));
#93631=CARTESIAN_POINT('',(-2.3699970317438,-0.0019977438217458,23.6514101080949));
#93632=CARTESIAN_POINT('',(-2.37554964903122,-0.000499616039387474,23.848589891905));
#93633=CARTESIAN_POINT('',(-2.37175,1.74448693060498E-12,-1.84858989190512));
#93634=CARTESIAN_POINT('Ctrl Pts',(-2.3699970317438,-0.00199774382174632,
23.6514101080949));
#93635=CARTESIAN_POINT('Ctrl Pts',(-2.37194321588891,-0.247080240897932,
23.6678302964223));
#93636=CARTESIAN_POINT('Ctrl Pts',(-2.22406647554583,-1.28125555242059,
23.737272119365));
#93637=CARTESIAN_POINT('Ctrl Pts',(-0.726135179226555,-2.70943783674216,
23.8597355769231));
#93638=CARTESIAN_POINT('Ctrl Pts',(1.88640665005374,-2.07600473032059,24.0188004807692));
#93639=CARTESIAN_POINT('Ctrl Pts',(2.76639061929044,0.464121353939118,24.1778653846154));
#93640=CARTESIAN_POINT('Ctrl Pts',(1.10560120264771,2.57797821371406,24.3369302884615));
#93641=CARTESIAN_POINT('Ctrl Pts',(-1.55015041093734,2.32604964527379,24.4947785296214));
#93642=CARTESIAN_POINT('Ctrl Pts',(-2.3740848383765,0.768169975198311,24.5996051361658));
#93643=CARTESIAN_POINT('Ctrl Pts',(-2.37561413348328,-0.00033829341715417,
24.6514101080949));
#93644=CARTESIAN_POINT('Ctrl Pts',(-2.37554964903122,-0.000499616039387678,
23.848589891905));
#93645=CARTESIAN_POINT('Ctrl Pts',(-2.3756263002611,-0.02728687960757,23.8503954836237));
#93646=CARTESIAN_POINT('Ctrl Pts',(-2.36306094446354,-0.840789806362212,
23.9052344978381));
#93647=CARTESIAN_POINT('Ctrl Pts',(-1.43531643911124,-2.4102647666624,24.0131069345482));
#93648=CARTESIAN_POINT('Ctrl Pts',(1.2518007167422,-2.51047893664949,24.1722072020356));
#93649=CARTESIAN_POINT('Ctrl Pts',(2.78874171880229,-0.304021630165937,
24.3313074695228));
#93650=CARTESIAN_POINT('Ctrl Pts',(1.76333858640404,2.18177600946929,24.4904077370101));
#93651=CARTESIAN_POINT('Ctrl Pts',(-0.882250543669541,2.66292010845086,
24.6495080044974));
#93652=CARTESIAN_POINT('Ctrl Pts',(-2.25926617902281,1.18787477101089,24.768902056129));
#93653=CARTESIAN_POINT('Ctrl Pts',(-2.37311459939558,0.200827130065391,
24.8352626852649));
#93654=CARTESIAN_POINT('Ctrl Pts',(-2.3713094773117,0.00218862049173589,
24.848589891905));
#93655=CARTESIAN_POINT('Origin',(0.,0.,-1.84858989190512));
#93656=CARTESIAN_POINT('',(-2.36842026495236,0.00119817809484571,22.6514101080949));
#93657=CARTESIAN_POINT('',(-2.36979619273569,-0.00194326858727306,22.848589891905));
#93658=CARTESIAN_POINT('',(-2.37175,1.74448693060498E-12,-1.84858989190512));
#93659=CARTESIAN_POINT('Ctrl Pts',(-2.36842026495236,0.00119817809484543,
22.6514101080949));
#93660=CARTESIAN_POINT('Ctrl Pts',(-2.36626591411704,-0.471597269374344,
22.6830338220633));
#93661=CARTESIAN_POINT('Ctrl Pts',(-1.99968381525113,-1.74017804174392,
22.767679170647));
#93662=CARTESIAN_POINT('Ctrl Pts',(0.0693644423326341,-2.8041958319312,
22.9053461538462));
#93663=CARTESIAN_POINT('Ctrl Pts',(2.39630268358469,-1.45810120990461,23.0644110576923));
#93664=CARTESIAN_POINT('Ctrl Pts',(2.52237238497556,1.22717693964369,23.2234759615385));
#93665=CARTESIAN_POINT('Ctrl Pts',(0.331785653130296,2.78536244859756,23.3825408653846));
#93666=CARTESIAN_POINT('Ctrl Pts',(-1.90593755423956,1.88858078851823,23.5251855809035));
#93667=CARTESIAN_POINT('Ctrl Pts',(-2.36565888695313,0.544303776846138,
23.6148086618069));
#93668=CARTESIAN_POINT('Ctrl Pts',(-2.3699970317438,-0.00199774382174632,
23.6514101080949));
#93669=CARTESIAN_POINT('Ctrl Pts',(-2.36979619273569,-0.00194326858727323,
22.848589891905));
#93670=CARTESIAN_POINT('Ctrl Pts',(-2.37173688724524,-0.254814261784281,
22.8655282819824));
#93671=CARTESIAN_POINT('Ctrl Pts',(-2.21782603676459,-1.29711363442759,
22.9355000945556));
#93672=CARTESIAN_POINT('Ctrl Pts',(-0.699084508414374,-2.7167610082398,
23.0585053296246));
#93673=CARTESIAN_POINT('Ctrl Pts',(1.90765211942334,-2.05678703736111,23.2176055971119));
#93674=CARTESIAN_POINT('Ctrl Pts',(2.76160497892747,0.49299844437904,23.3767058645991));
#93675=CARTESIAN_POINT('Ctrl Pts',(1.07814741001629,2.5898084269058,23.5358061320864));
#93676=CARTESIAN_POINT('Ctrl Pts',(-1.56558316400954,2.31026649768087,23.693100807855));
#93677=CARTESIAN_POINT('Ctrl Pts',(-2.37337491805917,0.759502432526167,
23.7973620611279));
#93678=CARTESIAN_POINT('Ctrl Pts',(-2.37554964903122,-0.000499616039387678,
23.848589891905));
#93679=CARTESIAN_POINT('Origin',(0.,0.,-1.84858989190512));
#93680=CARTESIAN_POINT('',(-2.37439379830995,0.00153838718516934,21.6514101080949));
#93681=CARTESIAN_POINT('',(-2.36852094091456,0.00128992227662758,21.848589891905));
#93682=CARTESIAN_POINT('',(-2.37175,1.74448693060498E-12,-1.84858989190512));
#93683=CARTESIAN_POINT('Ctrl Pts',(-2.37439379830994,0.00153838718516921,
21.6514101080949));
#93684=CARTESIAN_POINT('Ctrl Pts',(-2.36916514996087,-0.694072325068264,
21.6982373477043));
#93685=CARTESIAN_POINT('Ctrl Pts',(-1.67862426279434,-2.18634004573506,
21.7980862219291));
#93686=CARTESIAN_POINT('Ctrl Pts',(0.859206187941647,-2.67022291509215,
21.9509567307692));
#93687=CARTESIAN_POINT('Ctrl Pts',(2.71073858124696,-0.721264191416516,
22.1100216346154));
#93688=CARTESIAN_POINT('Ctrl Pts',(2.07261083932685,1.89013491539238,22.2690865384616));
#93689=CARTESIAN_POINT('Ctrl Pts',(-0.469092783427355,2.76555196122163,
22.4281514423077));
#93690=CARTESIAN_POINT('Ctrl Pts',(-2.16029918274576,1.43190245360995,22.5555926321855));
#93691=CARTESIAN_POINT('Ctrl Pts',(-2.36987798836417,0.321111249574778,
22.6300121874479));
#93692=CARTESIAN_POINT('Ctrl Pts',(-2.36842026495236,0.00119817809484543,
22.6514101080949));
#93693=CARTESIAN_POINT('Ctrl Pts',(-2.36852094091456,0.00128992227662748,
21.848589891905));
#93694=CARTESIAN_POINT('Ctrl Pts',(-2.36616375344373,-0.478144377631666,
21.8806610803412));
#93695=CARTESIAN_POINT('Ctrl Pts',(-1.99164931628814,-1.75376439025444,
21.9657656912732));
#93696=CARTESIAN_POINT('Ctrl Pts',(0.0936442024055214,-2.80370117686478,
22.1039037247009));
#93697=CARTESIAN_POINT('Ctrl Pts',(2.40933589137447,-1.43687511229467,22.2630039921882));
#93698=CARTESIAN_POINT('Ctrl Pts',(2.51128808357329,1.25017666235613,22.4221042596755));
#93699=CARTESIAN_POINT('Ctrl Pts',(0.305825341110179,2.78854449247846,22.5812045271628));
#93700=CARTESIAN_POINT('Ctrl Pts',(-1.91591745013914,1.87374633225182,22.7233664045726));
#93701=CARTESIAN_POINT('Ctrl Pts',(-2.36566065028352,0.536914713509884,
22.8124948594867));
#93702=CARTESIAN_POINT('Ctrl Pts',(-2.36979619273569,-0.00194326858727323,
22.848589891905));
#93703=CARTESIAN_POINT('Origin',(0.,0.,-1.84858989190512));
#93704=CARTESIAN_POINT('',(-2.37325526314324,-0.00197269285830692,20.6514101080949));
#93705=CARTESIAN_POINT('',(-2.37452747597515,0.00146821833409135,20.848589891905));
#93706=CARTESIAN_POINT('',(-2.37175,1.74448693060498E-12,-1.84858989190512));
#93707=CARTESIAN_POINT('Ctrl Pts',(-2.37325526314324,-0.00197269285830694,
20.6514101080949));
#93708=CARTESIAN_POINT('Ctrl Pts',(-2.37445256882395,-0.135969023876453,
20.66041923873));
#93709=CARTESIAN_POINT('Ctrl Pts',(-2.30307226995662,-1.05730119808642,
20.7224500039804));
#93710=CARTESIAN_POINT('Ctrl Pts',(-1.09632700309372,-2.58193586131958,
20.8375024038462));
#93711=CARTESIAN_POINT('Ctrl Pts',(1.5789647343853,-2.31844690628189,20.9965673076923));
#93712=CARTESIAN_POINT('Ctrl Pts',(2.80406663012842,0.0744044587420362,
21.1556322115385));
#93713=CARTESIAN_POINT('Ctrl Pts',(1.4537918540513,2.39891953486867,21.3146971153846));
#93714=CARTESIAN_POINT('Ctrl Pts',(-1.23170854982573,2.52016264117351,21.4737620192308));
#93715=CARTESIAN_POINT('Ctrl Pts',(-2.32839868565871,0.972490786612713,
21.5859996834675));
#93716=CARTESIAN_POINT('Ctrl Pts',(-2.37508545371163,0.0935550757204803,
21.6452157130889));
#93717=CARTESIAN_POINT('Ctrl Pts',(-2.37439379830994,0.00153838718516921,
21.6514101080949));
#93718=CARTESIAN_POINT('Ctrl Pts',(-2.37452747597515,0.00146821833409142,
20.848589891905));
#93719=CARTESIAN_POINT('Ctrl Pts',(-2.36944352129783,-0.699635497062075,
20.8957938787));
#93720=CARTESIAN_POINT('Ctrl Pts',(-1.66924795052569,-2.19724761514887,
20.9960312879907));
#93721=CARTESIAN_POINT('Ctrl Pts',(0.878805021433445,-2.66405916978217,
21.1493021197773));
#93722=CARTESIAN_POINT('Ctrl Pts',(2.71630826798053,-0.70084157917304,21.3084023872645));
#93723=CARTESIAN_POINT('Ctrl Pts',(2.05802048773081,1.90632137843475,21.4675026547518));
#93724=CARTESIAN_POINT('Ctrl Pts',(-0.491212118917867,2.76192327555009,
21.6266029222391));
#93725=CARTESIAN_POINT('Ctrl Pts',(-2.16621938134231,1.41889763066239,21.7536320012902));
#93726=CARTESIAN_POINT('Ctrl Pts',(-2.37006163578416,0.31465573442438,21.8276276578455));
#93727=CARTESIAN_POINT('Ctrl Pts',(-2.36852094091456,0.00128992227662748,
21.848589891905));
#93728=CARTESIAN_POINT('Origin',(0.,0.,-1.84858989190512));
#93729=CARTESIAN_POINT('',(-2.3679493887729,-0.000562658222058198,19.651410108095));
#93730=CARTESIAN_POINT('',(-2.37312868751824,-0.00200726644127208,19.848589891905));
#93731=CARTESIAN_POINT('',(-2.37175,1.74448693060498E-12,-1.84858989190512));
#93732=CARTESIAN_POINT('Ctrl Pts',(-2.3679493887729,-0.000562658222058171,
19.651410108095));
#93733=CARTESIAN_POINT('Ctrl Pts',(-2.36871522544106,-0.362737700238317,
19.675622764371));
#93734=CARTESIAN_POINT('Ctrl Pts',(-2.12018559280303,-1.5170183344022,19.7528570552624));
#93735=CARTESIAN_POINT('Ctrl Pts',(-0.321770969210761,-2.78653712213808,
19.8831129807692));
#93736=CARTESIAN_POINT('Ctrl Pts',(2.16993126151137,-1.77756125351454,20.0421778846154));
#93737=CARTESIAN_POINT('Ctrl Pts',(2.66867430563458,0.864004132007661,20.2012427884615));
#93738=CARTESIAN_POINT('Ctrl Pts',(0.716390873577828,2.7120305687685,20.3603076923077));
#93739=CARTESIAN_POINT('Ctrl Pts',(-1.7460176444507,2.10561836082741,20.5103634655188));
#93740=CARTESIAN_POINT('Ctrl Pts',(-2.36740603937537,0.652642529321267,
20.6073976041146));
#93741=CARTESIAN_POINT('Ctrl Pts',(-2.37325526314324,-0.00197269285830694,
20.6514101080949));
#93742=CARTESIAN_POINT('Ctrl Pts',(-2.37312868751824,-0.00200726644127234,
19.848589891905));
#93743=CARTESIAN_POINT('Ctrl Pts',(-2.37437772673991,-0.140398904122633,
19.857893254563));
#93744=CARTESIAN_POINT('Ctrl Pts',(-2.300273734566,-1.0663497090457,19.9202300397168));
#93745=CARTESIAN_POINT('Ctrl Pts',(-1.08149671384552,-2.58841155609738,
20.0356002473663));
#93746=CARTESIAN_POINT('Ctrl Pts',(1.59294487880464,-2.30912020884302,20.1947005148536));
#93747=CARTESIAN_POINT('Ctrl Pts',(2.80376116001019,0.0918307324124995,
20.3538007823408));
#93748=CARTESIAN_POINT('Ctrl Pts',(1.43843318435008,2.40840600812187,20.5129010498282));
#93749=CARTESIAN_POINT('Ctrl Pts',(-1.24855208494876,2.51209617987991,20.6720013173154));
#93750=CARTESIAN_POINT('Ctrl Pts',(-2.33149949909663,0.961679636121884,
20.7838975980077));
#93751=CARTESIAN_POINT('Ctrl Pts',(-2.37515531673415,0.0880507149826994,
20.8427604562042));
#93752=CARTESIAN_POINT('Ctrl Pts',(-2.37452747597515,0.00146821833409142,
20.848589891905));
#93753=CARTESIAN_POINT('Origin',(0.,0.,-1.84858989190512));
#93754=CARTESIAN_POINT('',(-2.37118449249719,0.00218036612316423,18.651410108095));
#93755=CARTESIAN_POINT('',(-2.36792368850356,-0.000510873358860464,18.848589891905));
#93756=CARTESIAN_POINT('',(-2.37175,1.74448693060498E-12,-1.84858989190512));
#93757=CARTESIAN_POINT('Ctrl Pts',(-2.37118449249719,0.00218036612316402,
18.651410108095));
#93758=CARTESIAN_POINT('Ctrl Pts',(-2.36588712038017,-0.585386454121441,
18.690826290012));
#93759=CARTESIAN_POINT('Ctrl Pts',(-1.84813322168764,-1.97166903258445,
18.7832641065445));
#93760=CARTESIAN_POINT('Ctrl Pts',(0.479031080165797,-2.76384784565209,
18.9287235576923));
#93761=CARTESIAN_POINT('Ctrl Pts',(2.58390217697866,-1.09168458333227,19.0877884615385));
#93762=CARTESIAN_POINT('Ctrl Pts',(2.31560520518838,1.58312925037248,19.2468533653847));
#93763=CARTESIAN_POINT('Ctrl Pts',(-0.0794442347893398,2.80392836984813,
19.4059182692308));
#93764=CARTESIAN_POINT('Ctrl Pts',(-2.04806391798638,1.65565053536932,19.5407705168009));
#93765=CARTESIAN_POINT('Ctrl Pts',(-2.36703817226971,0.430364573451299,
19.6226011297556));
#93766=CARTESIAN_POINT('Ctrl Pts',(-2.3679493887729,-0.000562658222058171,
19.651410108095));
#93767=CARTESIAN_POINT('Ctrl Pts',(-2.36792368850356,-0.000510873358860013,
18.848589891905));
#93768=CARTESIAN_POINT('Ctrl Pts',(-2.3686247961319,-0.366038844975643,
18.8730260529218));
#93769=CARTESIAN_POINT('Ctrl Pts',(-2.11684335076948,-1.52395140070622,
18.9504956364343));
#93770=CARTESIAN_POINT('Ctrl Pts',(-0.309432378410861,-2.78814654008503,
19.0809986424426));
#93771=CARTESIAN_POINT('Ctrl Pts',(2.17835029065068,-1.76756882101353,19.2400989099299));
#93772=CARTESIAN_POINT('Ctrl Pts',(2.66462702877159,0.877081708472472,19.3991991774172));
#93773=CARTESIAN_POINT('Ctrl Pts',(0.702598356729098,2.71585439133226,19.5582994449045));
#93774=CARTESIAN_POINT('Ctrl Pts',(-1.75251153778358,2.09764773379169,19.7080963497337));
#93775=CARTESIAN_POINT('Ctrl Pts',(-2.3672576318676,0.648496730804293,19.8048598320673));
#93776=CARTESIAN_POINT('Ctrl Pts',(-2.37312868751824,-0.00200726644127234,
19.848589891905));
#93777=CARTESIAN_POINT('Origin',(0.,0.,-1.84858989190512));
#93778=CARTESIAN_POINT('',(-2.37557266989979,-0.000442787889473553,17.651410108095));
#93779=CARTESIAN_POINT('',(-2.37124813668935,0.00218613168039616,17.848589891905));
#93780=CARTESIAN_POINT('',(-2.37175,1.74448693060498E-12,-1.84858989190512));
#93781=CARTESIAN_POINT('Ctrl Pts',(-2.37557266989979,-0.000442787889474178,
17.651410108095));
#93782=CARTESIAN_POINT('Ctrl Pts',(-2.37563336905613,-0.0241507402655156,
17.6530081810377));
#93783=CARTESIAN_POINT('Ctrl Pts',(-2.36455668635702,-0.834394437625102,
17.7076278885958));
#93784=CARTESIAN_POINT('Ctrl Pts',(-1.44515906695039,-2.4041299800326,17.8152692307692));
#93785=CARTESIAN_POINT('Ctrl Pts',(1.24075981853869,-2.51571873673912,17.9743341346154));
#93786=CARTESIAN_POINT('Ctrl Pts',(2.78711095707658,-0.316762059950613,
18.1333990384615));
#93787=CARTESIAN_POINT('Ctrl Pts',(1.77365825090308,2.17312266075431,18.2924639423077));
#93788=CARTESIAN_POINT('Ctrl Pts',(-0.868799284926716,2.66711707508149,
18.4515288461538));
#93789=CARTESIAN_POINT('Ctrl Pts',(-2.25624427366724,1.19611213094849,18.5711775680829));
#93790=CARTESIAN_POINT('Ctrl Pts',(-2.37301300916873,0.204993327478883,
18.6378046553966));
#93791=CARTESIAN_POINT('Ctrl Pts',(-2.37118449249719,0.00218036612316402,
18.651410108095));
#93792=CARTESIAN_POINT('Ctrl Pts',(-2.37124813668935,0.00218613168039603,
17.848589891905));
#93793=CARTESIAN_POINT('Ctrl Pts',(-2.36590642856635,-0.587617655854367,
17.8881588512806));
#93794=CARTESIAN_POINT('Ctrl Pts',(-1.8448401832008,-1.97634507886242,17.9807612331519));
#93795=CARTESIAN_POINT('Ctrl Pts',(0.487638852235446,-2.7625564022455,18.1263970375189));
#93796=CARTESIAN_POINT('Ctrl Pts',(2.58771149622336,-1.08317068743137,18.2854973050062));
#93797=CARTESIAN_POINT('Ctrl Pts',(2.3101500519365,1.5914509930673,18.4445975724935));
#93798=CARTESIAN_POINT('Ctrl Pts',(-0.0900172240013499,2.80381997018001,
18.6036978399808));
#93799=CARTESIAN_POINT('Ctrl Pts',(-2.051537474168,1.649460778596,18.7383619464513));
#93800=CARTESIAN_POINT('Ctrl Pts',(-2.36710319308455,0.427260861122469,
18.819992630426));
#93801=CARTESIAN_POINT('Ctrl Pts',(-2.36792368850356,-0.000510873358860013,
18.848589891905));
#93802=CARTESIAN_POINT('Origin',(0.,0.,-1.84858989190512));
#93803=CARTESIAN_POINT('',(-2.36984887420079,-0.00195632190991676,16.651410108095));
#93804=CARTESIAN_POINT('',(-2.37556777218862,-0.000462349284400809,16.848589891905));
#93805=CARTESIAN_POINT('',(-2.37175,1.74448693060498E-12,-1.84858989190512));
#93806=CARTESIAN_POINT('Ctrl Pts',(-2.36984887420079,-0.00195632190991717,
16.651410108095));
#93807=CARTESIAN_POINT('Ctrl Pts',(-2.37179051810406,-0.252771195777155,
16.6682117066787));
#93808=CARTESIAN_POINT('Ctrl Pts',(-2.21949473853235,-1.29279764384103,
16.7380349398778));
#93809=CARTESIAN_POINT('Ctrl Pts',(-0.706637310794764,-2.71458825619525,
16.8608798076923));
#93810=CARTESIAN_POINT('Ctrl Pts',(1.9012830270871,-2.06238903715836,17.0199447115385));
#93811=CARTESIAN_POINT('Ctrl Pts',(2.76298239365644,0.483997915310618,17.1790096153846));
#93812=CARTESIAN_POINT('Ctrl Pts',(1.08703863690706,2.58586014539682,17.3380745192308));
#93813=CARTESIAN_POINT('Ctrl Pts',(-1.5604205625462,2.31549981116177,17.4955413501342));
#93814=CARTESIAN_POINT('Ctrl Pts',(-2.3736194631805,0.762443134622733,17.5999865464223));
#93815=CARTESIAN_POINT('Ctrl Pts',(-2.37557266989979,-0.000442787889474178,
17.651410108095));
#93816=CARTESIAN_POINT('Ctrl Pts',(-2.37556777218862,-0.000462349284400653,
16.848589891905));
#93817=CARTESIAN_POINT('Ctrl Pts',(-2.37563370680816,-0.0252128074327879,
16.8502582271436));
#93818=CARTESIAN_POINT('Ctrl Pts',(-2.36405305652946,-0.836673273324087,
16.9049599848779));
#93819=CARTESIAN_POINT('Ctrl Pts',(-1.44154752246972,-2.40654321927916,
17.012695165108));
#93820=CARTESIAN_POINT('Ctrl Pts',(1.24530136378902,-2.51370921928975,17.1717954325953));
#93821=CARTESIAN_POINT('Ctrl Pts',(2.78794581418191,-0.311235703258245,
17.3308957000825));
#93822=CARTESIAN_POINT('Ctrl Pts',(1.76897742105025,2.17720656108039,17.4899959675698));
#93823=CARTESIAN_POINT('Ctrl Pts',(-0.875358028577435,2.66519377299328,
17.6490962350571));
#93824=CARTESIAN_POINT('Ctrl Pts',(-2.25777273477332,1.19202439171433,17.7686275431688));
#93825=CARTESIAN_POINT('Ctrl Pts',(-2.37306580470883,0.202883634742145,
17.8351254287848));
#93826=CARTESIAN_POINT('Ctrl Pts',(-2.37124813668935,0.00218613168039603,
17.848589891905));
#93827=CARTESIAN_POINT('Origin',(0.,0.,-1.84858989190512));
#93828=CARTESIAN_POINT('',(-2.36850976199849,0.00127651360681889,15.651410108095));
#93829=CARTESIAN_POINT('',(-2.36984864786026,-0.00195908838300035,15.848589891905));
#93830=CARTESIAN_POINT('',(-2.37175,1.74448693060498E-12,-1.84858989190512));
#93831=CARTESIAN_POINT('Ctrl Pts',(-2.36850976199849,0.00127651360681887,
15.651410108095));
#93832=CARTESIAN_POINT('Ctrl Pts',(-2.3661817149612,-0.477176041303263,
15.6834152323197));
#93833=CARTESIAN_POINT('Ctrl Pts',(-1.99287478523265,-1.75160289678569,
15.7684419911599));
#93834=CARTESIAN_POINT('Ctrl Pts',(0.0895230006752742,-2.80362467567087,
15.9064903846154));
#93835=CARTESIAN_POINT('Ctrl Pts',(2.40672355708034,-1.44083566359076,16.0655552884616));
#93836=CARTESIAN_POINT('Ctrl Pts',(2.5134845904627,1.24527944782968,16.2246201923077));
#93837=CARTESIAN_POINT('Ctrl Pts',(0.311752127397432,2.78767578831249,16.3836850961539));
#93838=CARTESIAN_POINT('Ctrl Pts',(-1.91350003226281,1.8772703365023,16.5259484014163));
#93839=CARTESIAN_POINT('Ctrl Pts',(-2.36566317652526,0.538737691428593,
16.6151900720633));
#93840=CARTESIAN_POINT('Ctrl Pts',(-2.36984887420079,-0.00195632190991717,
16.651410108095));
#93841=CARTESIAN_POINT('Ctrl Pts',(-2.36984864786026,-0.00195908838300039,
15.848589891905));
#93842=CARTESIAN_POINT('Ctrl Pts',(-2.37179223519786,-0.252766996446055,
15.8653910255024));
#93843=CARTESIAN_POINT('Ctrl Pts',(-2.21948393637844,-1.29295979284088,
15.9352255815954));
#93844=CARTESIAN_POINT('Ctrl Pts',(-0.706111029293687,-2.71494322962874,
16.0580935601843));
#93845=CARTESIAN_POINT('Ctrl Pts',(1.90232437254992,-2.06171567084302,16.2171938276716));
#93846=CARTESIAN_POINT('Ctrl Pts',(2.7628712320534,0.485851912509174,16.3762940951588));
#93847=CARTESIAN_POINT('Ctrl Pts',(1.08484420786421,2.58701035375983,16.5353943626462));
#93848=CARTESIAN_POINT('Ctrl Pts',(-1.56190831659987,2.31407131393373,16.6928262948949));
#93849=CARTESIAN_POINT('Ctrl Pts',(-2.37353776202774,0.761560422315232,
16.7972248046478));
#93850=CARTESIAN_POINT('Ctrl Pts',(-2.37556777218862,-0.000462349284400653,
16.848589891905));
#93851=CARTESIAN_POINT('Origin',(0.,0.,-1.84858989190512));
#93852=CARTESIAN_POINT('',(-2.37452997801752,0.00146346246222767,14.651410108095));
#93853=CARTESIAN_POINT('',(-2.36848771328686,0.00126209581994427,14.848589891905));
#93854=CARTESIAN_POINT('',(-2.37175,1.74448693060498E-12,-1.84858989190512));
#93855=CARTESIAN_POINT('Ctrl Pts',(-2.37452997801752,0.00146346246222774,
14.651410108095));
#93856=CARTESIAN_POINT('Ctrl Pts',(-2.36945739098401,-0.699707555274035,
14.6986187579608));
#93857=CARTESIAN_POINT('Ctrl Pts',(-1.66920288796294,-2.19719003397587,
14.7988490424419));
#93858=CARTESIAN_POINT('Ctrl Pts',(0.878381155370515,-2.66397677083911,
14.9521009615385));
#93859=CARTESIAN_POINT('Ctrl Pts',(2.7158539478379,-0.701757097359029,15.1111658653846));
#93860=CARTESIAN_POINT('Ctrl Pts',(2.05896843006344,1.90498679619639,15.2702307692308));
#93861=CARTESIAN_POINT('Ctrl Pts',(-0.488963186910485,2.76210801590502,
15.429295673077));
#93862=CARTESIAN_POINT('Ctrl Pts',(-2.16550513060297,1.42036197322363,15.5563554526983));
#93863=CARTESIAN_POINT('Ctrl Pts',(-2.37003849922212,0.315457549776884,
15.6303935977043));
#93864=CARTESIAN_POINT('Ctrl Pts',(-2.36850976199849,0.00127651360681887,
15.651410108095));
#93865=CARTESIAN_POINT('Ctrl Pts',(-2.36848771328686,0.00126209581994444,
14.848589891905));
#93866=CARTESIAN_POINT('Ctrl Pts',(-2.36619314536369,-0.476137104368745,
14.8805238238611));
#93867=CARTESIAN_POINT('Ctrl Pts',(-1.99411074642562,-1.74965427770411,
14.965491178313));
#93868=CARTESIAN_POINT('Ctrl Pts',(0.0863900949595627,-2.8039340714949,
15.1034919552607));
#93869=CARTESIAN_POINT('Ctrl Pts',(2.40561031446837,-1.44310378723102,15.2625922227479));
#93870=CARTESIAN_POINT('Ctrl Pts',(2.51451416171814,1.24367522139665,15.4216924902352));
#93871=CARTESIAN_POINT('Ctrl Pts',(0.313038897897693,2.78774392191968,15.5807927577225));
#93872=CARTESIAN_POINT('Ctrl Pts',(-1.91321060022851,1.87781928293776,15.7230918916124));
#93873=CARTESIAN_POINT('Ctrl Pts',(-2.36565722723337,0.53891778342454,15.8123576030066));
#93874=CARTESIAN_POINT('Ctrl Pts',(-2.36984864786026,-0.00195908838300039,
15.848589891905));
#93875=CARTESIAN_POINT('Origin',(0.,0.,-1.84858989190512));
#93876=CARTESIAN_POINT('',(-2.37308791222507,-0.00201426525716621,13.651410108095));
#93877=CARTESIAN_POINT('',(-2.37447897333966,0.00149556365171458,13.848589891905));
#93878=CARTESIAN_POINT('',(-2.37175,1.74448693060498E-12,-1.84858989190512));
#93879=CARTESIAN_POINT('Ctrl Pts',(-2.37308791222507,-0.00201426525716633,
13.651410108095));
#93880=CARTESIAN_POINT('Ctrl Pts',(-2.37435103224372,-0.141708936028309,
13.6608006489864));
#93881=CARTESIAN_POINT('Ctrl Pts',(-2.29944815507118,-1.06880604528595,
13.7232128244932));
#93882=CARTESIAN_POINT('Ctrl Pts',(-1.07773622411112,-2.58975101523663,
13.8386466346154));
#93883=CARTESIAN_POINT('Ctrl Pts',(1.59559205901132,-2.30703525566917,13.9977115384616));
#93884=CARTESIAN_POINT('Ctrl Pts',(2.80345924275497,0.094561957954597,14.1567764423077));
#93885=CARTESIAN_POINT('Ctrl Pts',(1.43650760564222,2.40930935925889,14.3158413461539));
#93886=CARTESIAN_POINT('Ctrl Pts',(-1.24979505427195,2.51124232442785,14.47490625));
#93887=CARTESIAN_POINT('Ctrl Pts',(-2.33164118373885,0.961011990247127,
14.5867625039804));
#93888=CARTESIAN_POINT('Ctrl Pts',(-2.37515458539669,0.0878013781735994,
14.6455971233454));
#93889=CARTESIAN_POINT('Ctrl Pts',(-2.37452997801752,0.00146346246222774,
14.651410108095));
#93890=CARTESIAN_POINT('Ctrl Pts',(-2.37447897333966,0.00149556365171451,
13.848589891905));
#93891=CARTESIAN_POINT('Ctrl Pts',(-2.36933692775314,-0.69760700066698,
13.8956566222199));
#93892=CARTESIAN_POINT('Ctrl Pts',(-1.67264639556168,-2.19334548761835,
13.9957567750306));
#93893=CARTESIAN_POINT('Ctrl Pts',(0.87190957086987,-2.66632391618547,14.148890350337));
#93894=CARTESIAN_POINT('Ctrl Pts',(2.71448594495469,-0.707866922832642,
14.3079906178242));
#93895=CARTESIAN_POINT('Ctrl Pts',(2.06294567416375,1.90099044480665,14.4670908853115));
#93896=CARTESIAN_POINT('Ctrl Pts',(-0.484064769522908,2.76318490599233,
14.6261911527988));
#93897=CARTESIAN_POINT('Ctrl Pts',(-2.16435474415049,1.42305090134789,14.75335748833));
#93898=CARTESIAN_POINT('Ctrl Pts',(-2.37000378760724,0.31669083543954,14.8274904013654));
#93899=CARTESIAN_POINT('Ctrl Pts',(-2.36848771328686,0.00126209581994444,
14.848589891905));
#93900=CARTESIAN_POINT('Origin',(0.,0.,-1.84858989190512));
#93901=CARTESIAN_POINT('',(-2.36791244388392,-0.000470842462512318,12.651410108095));
#93902=CARTESIAN_POINT('',(-2.3731890282555,-0.00199242475106415,12.848589891905));
#93903=CARTESIAN_POINT('',(-2.37175,1.74448693060498E-12,-1.84858989190512));
#93904=CARTESIAN_POINT('Ctrl Pts',(-2.36791244388392,-0.000470842462512201,
12.651410108095));
#93905=CARTESIAN_POINT('Ctrl Pts',(-2.36856283952937,-0.368365367608508,
12.6760041746274));
#93906=CARTESIAN_POINT('Ctrl Pts',(-2.11451705642467,-1.52854249033973,
12.7536198757752));
#93907=CARTESIAN_POINT('Ctrl Pts',(-0.301729257152967,-2.78877843240699,
12.8842572115385));
#93908=CARTESIAN_POINT('Ctrl Pts',(2.18265469599876,-1.76191491500441,13.0433221153847));
#93909=CARTESIAN_POINT('Ctrl Pts',(2.66239370729449,0.88316784194122,13.2023870192308));
#93910=CARTESIAN_POINT('Ctrl Pts',(0.696874616911946,2.71711086597222,13.361451923077));
#93911=CARTESIAN_POINT('Ctrl Pts',(-1.75486287047061,2.09459753855825,13.5111262860316));
#93912=CARTESIAN_POINT('Ctrl Pts',(-2.36721910141259,0.647046459105955,
13.607779014371));
#93913=CARTESIAN_POINT('Ctrl Pts',(-2.37308791222507,-0.00201426525716633,
13.651410108095));
#93914=CARTESIAN_POINT('Ctrl Pts',(-2.3731890282555,-0.00199242475106441,
12.848589891905));
#93915=CARTESIAN_POINT('Ctrl Pts',(-2.37441440680738,-0.138333347090684,
12.8577559980829));
#93916=CARTESIAN_POINT('Ctrl Pts',(-2.30157962306162,-1.06220937357195,
12.9199555267566));
#93917=CARTESIAN_POINT('Ctrl Pts',(-1.08818988647055,-2.58560482223799,
13.035188477926));
#93918=CARTESIAN_POINT('Ctrl Pts',(1.58696534358022,-2.31323378067855,13.1942887454133));
#93919=CARTESIAN_POINT('Ctrl Pts',(2.80398936259225,0.0845764758463313,
13.3533890129006));
#93920=CARTESIAN_POINT('Ctrl Pts',(1.44465944825848,2.40467640325151,13.5124892803878));
#93921=CARTESIAN_POINT('Ctrl Pts',(-1.24204855870295,2.51531805217969,13.6715895478751));
#93922=CARTESIAN_POINT('Ctrl Pts',(-2.33033692113347,0.965810161418643,
13.7836230850475));
#93923=CARTESIAN_POINT('Ctrl Pts',(-2.37513083513226,0.0901214311432274,
13.8426231997242));
#93924=CARTESIAN_POINT('Ctrl Pts',(-2.37447897333966,0.00149556365171451,
13.848589891905));
#93925=CARTESIAN_POINT('Origin',(0.,0.,-1.84858989190512));
#93926=CARTESIAN_POINT('',(-2.37135471886199,0.00218752354069527,11.651410108095));
#93927=CARTESIAN_POINT('',(-2.36793725144823,-0.00054391158261724,11.848589891905));
#93928=CARTESIAN_POINT('',(-2.37175,1.74448693060498E-12,-1.84858989190512));
#93929=CARTESIAN_POINT('Ctrl Pts',(-2.37135471886199,0.0021875235406953,
11.651410108095));
#93930=CARTESIAN_POINT('Ctrl Pts',(-2.36595594613634,-0.590956427613617,
11.6912077002684));
#93931=CARTESIAN_POINT('Ctrl Pts',(-1.8400272861403,-1.98287170359581,11.7840269270573));
#93932=CARTESIAN_POINT('Ctrl Pts',(0.498888975319622,-2.76033249446239,
11.9298677884616));
#93933=CARTESIAN_POINT('Ctrl Pts',(2.59168390408889,-1.07307978779166,12.0889326923077));
#93934=CARTESIAN_POINT('Ctrl Pts',(2.30416368784436,1.59973603738241,12.2479975961539));
#93935=CARTESIAN_POINT('Ctrl Pts',(-0.0996006097535288,2.80328475332372,
12.4070625));
#93936=CARTESIAN_POINT('Ctrl Pts',(-2.054369577301,1.64417118009386,12.5415333373137));
#93937=CARTESIAN_POINT('Ctrl Pts',(-2.36716067042395,0.424767767310423,
12.622982540012));
#93938=CARTESIAN_POINT('Ctrl Pts',(-2.36791244388392,-0.000470842462512201,
12.651410108095));
#93939=CARTESIAN_POINT('Ctrl Pts',(-2.36793725144823,-0.000543911582617518,
11.848589891905));
#93940=CARTESIAN_POINT('Ctrl Pts',(-2.36867974366206,-0.364013542241654,
11.8728887964417));
#93941=CARTESIAN_POINT('Ctrl Pts',(-2.11888156743286,-1.51980408948385,
11.9502211234741));
#93942=CARTESIAN_POINT('Ctrl Pts',(-0.316644893535377,-2.78733663865617,
12.0805868730024));
#93943=CARTESIAN_POINT('Ctrl Pts',(2.17376990917619,-1.7731987784107,12.2396871404896));
#93944=CARTESIAN_POINT('Ctrl Pts',(2.66688731468318,0.870184794500003,12.3987874079769));
#93945=CARTESIAN_POINT('Ctrl Pts',(0.709622520229888,2.71402752465403,12.5578876754642));
#93946=CARTESIAN_POINT('Ctrl Pts',(-1.74932962998056,2.10161421686923,12.7078218367736));
#93947=CARTESIAN_POINT('Ctrl Pts',(-2.3673245894741,0.650510421196307,12.8047225755872));
#93948=CARTESIAN_POINT('Ctrl Pts',(-2.3731890282555,-0.00199242475106441,
12.848589891905));
#93949=CARTESIAN_POINT('Origin',(0.,0.,-1.84858989190512));
#93950=CARTESIAN_POINT('',(-2.37552098982677,-0.000546054288011158,10.651410108095));
#93951=CARTESIAN_POINT('',(-2.37118699418392,0.00218308078960436,10.848589891905));
#93952=CARTESIAN_POINT('',(-2.37175,1.74448693060498E-12,-1.84858989190512));
#93953=CARTESIAN_POINT('Ctrl Pts',(-2.37552098982677,-0.000546054288011466,
10.651410108095));
#93954=CARTESIAN_POINT('Ctrl Pts',(-2.3756121895163,-0.0299140681072457,
10.6533895912941));
#93955=CARTESIAN_POINT('Ctrl Pts',(-2.36179446748901,-0.845833956636457,
10.7083907091086));
#93956=CARTESIAN_POINT('Ctrl Pts',(-1.4278375819202,-2.4144576056201,10.8164134615385));
#93957=CARTESIAN_POINT('Ctrl Pts',(1.25881414027309,-2.50673346208347,10.9754783653846));
#93958=CARTESIAN_POINT('Ctrl Pts',(2.78931624170351,-0.296716351840369,
11.1345432692308));
#93959=CARTESIAN_POINT('Ctrl Pts',(1.75798906916851,2.18581795270431,11.2936081730769));
#93960=CARTESIAN_POINT('Ctrl Pts',(-0.887951675457031,2.66080204294372,
11.4526730769231));
#93961=CARTESIAN_POINT('Ctrl Pts',(-2.26039623340362,1.18458115724447,11.5719403885958));
#93962=CARTESIAN_POINT('Ctrl Pts',(-2.37314863642732,0.199278863891932,
11.638186065653));
#93963=CARTESIAN_POINT('Ctrl Pts',(-2.37135471886199,0.0021875235406953,
11.651410108095));
#93964=CARTESIAN_POINT('Ctrl Pts',(-2.37118699418392,0.00218308078960424,
10.848589891905));
#93965=CARTESIAN_POINT('Ctrl Pts',(-2.36588268180612,-0.585613382676844,
10.8880215948005));
#93966=CARTESIAN_POINT('Ctrl Pts',(-1.84775089715974,-1.97231211609,10.9804867201917));
#93967=CARTESIAN_POINT('Ctrl Pts',(0.480489876761207,-2.76380878573882,
11.1259852680787));
#93968=CARTESIAN_POINT('Ctrl Pts',(2.58490043376768,-1.08986204324435,11.2850855355659));
#93969=CARTESIAN_POINT('Ctrl Pts',(2.31425975531301,1.58546879841127,11.4441858030532));
#93970=CARTESIAN_POINT('Ctrl Pts',(-0.0827628213498791,2.80404348061853,
11.6032860705405));
#93971=CARTESIAN_POINT('Ctrl Pts',(-2.04926540690783,1.65359163367153,11.7380874334911));
#93972=CARTESIAN_POINT('Ctrl Pts',(-2.36705922191318,0.429274832467547,
11.8198553739459));
#93973=CARTESIAN_POINT('Ctrl Pts',(-2.36793725144823,-0.000543911582617518,
11.848589891905));
#93974=CARTESIAN_POINT('Origin',(0.,0.,-1.84858989190512));
#93975=CARTESIAN_POINT('',(-2.36970451566036,-0.00191118876816796,9.65141010809495));
#93976=CARTESIAN_POINT('',(-2.37558458192292,-0.000424916937384612,9.84858989190501));
#93977=CARTESIAN_POINT('',(-2.37175,1.74448693060498E-12,-1.84858989190512));
#93978=CARTESIAN_POINT('Ctrl Pts',(-2.36970451566036,-0.00191118876816797,
9.65141010809495));
#93979=CARTESIAN_POINT('Ctrl Pts',(-2.37163637732688,-0.25845917027921,
9.6685931169351));
#93980=CARTESIAN_POINT('Ctrl Pts',(-2.21487175474487,-1.30434045260947,
9.73879776039063));
#93981=CARTESIAN_POINT('Ctrl Pts',(-0.687102918082009,-2.71959836550246,
9.86202403846154));
#93982=CARTESIAN_POINT('Ctrl Pts',(1.91606113164826,-2.04866674436504,10.0210889423077));
#93983=CARTESIAN_POINT('Ctrl Pts',(2.75943135650696,0.503849460063841,10.1801538461539));
#93984=CARTESIAN_POINT('Ctrl Pts',(1.06841988491078,2.59360842056154,10.33921875));
#93985=CARTESIAN_POINT('Ctrl Pts',(-1.57061947598469,2.30492249930711,10.496304170647));
#93986=CARTESIAN_POINT('Ctrl Pts',(-2.37316935159884,0.756725646134099,
10.6003679566787));
#93987=CARTESIAN_POINT('Ctrl Pts',(-2.37552098982677,-0.000546054288011466,
10.651410108095));
#93988=CARTESIAN_POINT('Ctrl Pts',(-2.37558458192292,-0.000424916937384534,
9.84858989190501));
#93989=CARTESIAN_POINT('Ctrl Pts',(-2.37564053070254,-0.0231386862569469,
9.85012097066349));
#93990=CARTESIAN_POINT('Ctrl Pts',(-2.36503969337732,-0.832557221286051,
9.90468547191772));
#93991=CARTESIAN_POINT('Ctrl Pts',(-1.44776895650877,-2.4028055631629,10.0122833956677));
#93992=CARTESIAN_POINT('Ctrl Pts',(1.23879367513383,-2.51692267585747,10.171383663155));
#93993=CARTESIAN_POINT('Ctrl Pts',(2.78713124782529,-0.318447693025035,
10.3304839306423));
#93994=CARTESIAN_POINT('Ctrl Pts',(1.77460441465207,2.1726225390745,10.4895841981295));
#93995=CARTESIAN_POINT('Ctrl Pts',(-0.868459654081467,2.66744959746755,
10.6486844656168));
#93996=CARTESIAN_POINT('Ctrl Pts',(-2.25627293082936,1.19617424730534,10.7683530302087));
#93997=CARTESIAN_POINT('Ctrl Pts',(-2.3730166836048,0.204939799141744,10.8349881723047));
#93998=CARTESIAN_POINT('Ctrl Pts',(-2.37118699418392,0.00218308078960424,
10.848589891905));
#93999=CARTESIAN_POINT('Origin',(0.,0.,-1.84858989190512));
#94000=CARTESIAN_POINT('',(-2.36860503817343,0.00135251512067538,8.65141010809494));
#94001=CARTESIAN_POINT('',(-2.36990159498818,-0.00197442701926287,8.84858989190502));
#94002=CARTESIAN_POINT('',(-2.37175,1.74448693060498E-12,-1.84858989190512));
#94003=CARTESIAN_POINT('Ctrl Pts',(-2.36860503817343,0.00135251512067523,
8.65141010809494));
#94004=CARTESIAN_POINT('Ctrl Pts',(-2.36610302129555,-0.482753094486701,
8.68379664257612));
#94005=CARTESIAN_POINT('Ctrl Pts',(-1.98600454178426,-1.76301994240106,
8.76920481167267));
#94006=CARTESIAN_POINT('Ctrl Pts',(0.109676931802227,-2.80290860719912,
8.90763461538463));
#94007=CARTESIAN_POINT('Ctrl Pts',(2.41702003317145,-1.42349564415503,9.06669951923077));
#94008=CARTESIAN_POINT('Ctrl Pts',(2.50446688033972,1.26331759069596,9.22576442307694));
#94009=CARTESIAN_POINT('Ctrl Pts',(0.291702487991934,2.78984504017334,9.38482932692308));
#94010=CARTESIAN_POINT('Ctrl Pts',(-1.92099870206075,1.86594863561955,9.52671122192909));
#94011=CARTESIAN_POINT('Ctrl Pts',(-2.36567522905754,0.53317129814093,9.61557148231971));
#94012=CARTESIAN_POINT('Ctrl Pts',(-2.36970451566036,-0.00191118876816797,
9.65141010809495));
#94013=CARTESIAN_POINT('Ctrl Pts',(-2.36990159498818,-0.00197442701926287,
8.84858989190501));
#94014=CARTESIAN_POINT('Ctrl Pts',(-2.37184739597465,-0.250719344876404,
8.86525376902227));
#94015=CARTESIAN_POINT('Ctrl Pts',(-2.2211351990105,-1.28880604443534,8.93495106863528));
#94016=CARTESIAN_POINT('Ctrl Pts',(-0.713132823661497,-2.71310727794049,
9.05768179074405));
#94017=CARTESIAN_POINT('Ctrl Pts',(1.89698389204465,-2.06663050377184,9.21678205823132));
#94018=CARTESIAN_POINT('Ctrl Pts',(2.76411899128539,0.478702128481346,9.37588232571861));
#94019=CARTESIAN_POINT('Ctrl Pts',(1.09153374406576,2.5841949638839,9.53498259320587));
#94020=CARTESIAN_POINT('Ctrl Pts',(-1.558224245524,2.31787258077939,9.6925517819347));
#94021=CARTESIAN_POINT('Ctrl Pts',(-2.37370257992687,0.763619616102294,
9.79708754816773));
#94022=CARTESIAN_POINT('Ctrl Pts',(-2.37558458192292,-0.000424916937384534,
9.84858989190501));
#94023=CARTESIAN_POINT('Origin',(0.,0.,-1.84858989190512));
#94024=CARTESIAN_POINT('',(-2.37466060251227,0.00138507137951498,7.65141010809495));
#94025=CARTESIAN_POINT('',(-2.3684552380494,0.00123397076206691,7.84858989190501));
#94026=CARTESIAN_POINT('',(-2.37175,1.74448693060498E-12,-1.84858989190512));
#94027=CARTESIAN_POINT('Ctrl Pts',(-2.37466060251227,0.00138507137951483,
7.65141010809495));
#94028=CARTESIAN_POINT('Ctrl Pts',(-2.36976305923354,-0.705348722947108,
7.69900016821715));
#94029=CARTESIAN_POINT('Ctrl Pts',(-1.65971194045233,-2.20801762144576,
7.79961186295472));
#94030=CARTESIAN_POINT('Ctrl Pts',(0.897510721516925,-2.65759293241885,
7.9532451923077));
#94031=CARTESIAN_POINT('Ctrl Pts',(2.72082893886257,-0.682213731266401,
8.11231009615385));
#94032=CARTESIAN_POINT('Ctrl Pts',(2.04521959797142,1.91974021308981,8.27137500000001));
#94033=CARTESIAN_POINT('Ctrl Pts',(-0.508808317133133,2.75852130426731,
8.43043990384615));
#94034=CARTESIAN_POINT('Ctrl Pts',(-2.17065706179093,1.40882044126061,8.55711827321115));
#94035=CARTESIAN_POINT('Ctrl Pts',(-2.37019919974828,0.309800698596051,
8.63077500796074));
#94036=CARTESIAN_POINT('Ctrl Pts',(-2.36860503817343,0.00135251512067523,
8.65141010809494));
#94037=CARTESIAN_POINT('Ctrl Pts',(-2.3684552380494,0.00123397076206695,
7.84858989190502));
#94038=CARTESIAN_POINT('Ctrl Pts',(-2.36622324530222,-0.474129605566998,
7.88038656738104));
#94039=CARTESIAN_POINT('Ctrl Pts',(-1.99656425442517,-1.7455431608208,7.96521666535284));
#94040=CARTESIAN_POINT('Ctrl Pts',(0.0791354092423232,-2.80414819736781,
8.10308018582037));
#94041=CARTESIAN_POINT('Ctrl Pts',(2.40186863507383,-1.44932280243071,8.26218045330766));
#94042=CARTESIAN_POINT('Ctrl Pts',(2.51772340840239,1.23716545562014,8.42128072079493));
#94043=CARTESIAN_POINT('Ctrl Pts',(0.320250359289559,2.78692469097606,8.58038098828221));
#94044=CARTESIAN_POINT('Ctrl Pts',(-1.9104954853186,1.8818907754002,8.72281737865224));
#94045=CARTESIAN_POINT('Ctrl Pts',(-2.36565481035475,0.54092081362753,8.81222034652651));
#94046=CARTESIAN_POINT('Ctrl Pts',(-2.36990159498818,-0.00197442701926287,
8.84858989190501));
#94047=CARTESIAN_POINT('Origin',(0.,0.,-1.84858989190512));
#94048=CARTESIAN_POINT('',(-2.37291859965002,-0.00205150633385966,6.65141010809495));
#94049=CARTESIAN_POINT('',(-2.3744297718001,0.00152245248726483,6.84858989190502));
#94050=CARTESIAN_POINT('',(-2.37175,1.74448693060498E-12,-1.84858989190512));
#94051=CARTESIAN_POINT('Ctrl Pts',(-2.37291859965002,-0.00205150633385984,
6.65141010809495));
#94052=CARTESIAN_POINT('Ctrl Pts',(-2.3742459582117,-0.147446862522116,
6.66118205924279));
#94053=CARTESIAN_POINT('Ctrl Pts',(-2.29577744667903,-1.08031369136468,
6.72397564500602));
#94054=CARTESIAN_POINT('Ctrl Pts',(-1.05908973969091,-2.5974323115265,6.83979086538461));
#94055=CARTESIAN_POINT('Ctrl Pts',(1.61213691155191,-2.29550436028606,6.99885576923078));
#94056=CARTESIAN_POINT('Ctrl Pts',(2.80270695172092,0.114714569500639,7.15792067307693));
#94057=CARTESIAN_POINT('Ctrl Pts',(1.41914910781753,2.41957465259107,7.31698557692308));
#94058=CARTESIAN_POINT('Ctrl Pts',(-1.26781695999829,2.50219220796908,7.47605048076923));
#94059=CARTESIAN_POINT('Ctrl Pts',(-2.33483917126496,0.949536563310053,
7.5875253244932));
#94060=CARTESIAN_POINT('Ctrl Pts',(-2.37521957157186,0.0820463952122587,
7.64597853360177));
#94061=CARTESIAN_POINT('Ctrl Pts',(-2.37466060251227,0.00138507137951483,
7.65141010809495));
#94062=CARTESIAN_POINT('Ctrl Pts',(-2.3744297718001,0.00152245248726472,
6.84858989190502));
#94063=CARTESIAN_POINT('Ctrl Pts',(-2.36923206465993,-0.695579259077515,
6.89551936573982));
#94064=CARTESIAN_POINT('Ctrl Pts',(-1.67603583801615,-2.18944047996094,
6.99548226207037));
#94065=CARTESIAN_POINT('Ctrl Pts',(0.865008283985421,-2.66857081495577,
7.14847858089671));
#94066=CARTESIAN_POINT('Ctrl Pts',(2.71264545191261,-0.714887528227297,
7.30757884838397));
#94067=CARTESIAN_POINT('Ctrl Pts',(2.0678570518103,1.89564678647566,7.46667911587126));
#94068=CARTESIAN_POINT('Ctrl Pts',(-0.476914179932666,2.76442804044096,
7.62577938335854));
#94069=CARTESIAN_POINT('Ctrl Pts',(-2.162483104034,1.42720403096667,7.75308297536978));
#94070=CARTESIAN_POINT('Ctrl Pts',(-2.36994596827865,0.318725528032169,
7.82735314488528));
#94071=CARTESIAN_POINT('Ctrl Pts',(-2.3684552380494,0.00123397076206695,
7.84858989190502));
#94072=CARTESIAN_POINT('Origin',(0.,0.,-1.84858989190512));
#94073=CARTESIAN_POINT('',(-2.36788211521185,-0.000378178454202572,5.65141010809494));
#94074=CARTESIAN_POINT('',(-2.37324908705979,-0.00197702543379558,5.84858989190501));
#94075=CARTESIAN_POINT('',(-2.37175,1.74448693060498E-12,-1.84858989190512));
#94076=CARTESIAN_POINT('Ctrl Pts',(-2.36788211521185,-0.000378178454202779,
5.65141010809495));
#94077=CARTESIAN_POINT('Ctrl Pts',(-2.36841223428828,-0.373990025746932,
5.67638558488381));
#94078=CARTESIAN_POINT('Ctrl Pts',(-2.10879213104349,-1.54006374105855,
5.75438269628806));
#94079=CARTESIAN_POINT('Ctrl Pts',(-0.281671949479292,-2.79087559782923,
5.8854014423077));
#94080=CARTESIAN_POINT('Ctrl Pts',(2.19526531462978,-1.74617750760439,6.04446634615385));
#94081=CARTESIAN_POINT('Ctrl Pts',(2.65597549661169,0.902285903180645,6.20353125));
#94082=CARTESIAN_POINT('Ctrl Pts',(0.677322340573879,2.7220507226428,6.36259615384616));
#94083=CARTESIAN_POINT('Ctrl Pts',(-1.76364020147583,2.08355828545319,6.51188910654447));
#94084=CARTESIAN_POINT('Ctrl Pts',(-2.36704384272867,0.641453873263,6.6081604246274));
#94085=CARTESIAN_POINT('Ctrl Pts',(-2.37291859965002,-0.00205150633385984,
6.65141010809495));
#94086=CARTESIAN_POINT('Ctrl Pts',(-2.37324908705979,-0.00197702543379559,
5.84858989190501));
#94087=CARTESIAN_POINT('Ctrl Pts',(-2.37445062243721,-0.136267538027153,
5.85761874160283));
#94088=CARTESIAN_POINT('Ctrl Pts',(-2.302879494702,-1.05806940655756,5.91968101379641));
#94089=CARTESIAN_POINT('Ctrl Pts',(-1.09487577505419,-2.58278078105689,
6.03477670848575));
#94090=CARTESIAN_POINT('Ctrl Pts',(1.58097518564988,-2.31733186836853,6.19387697597303));
#94091=CARTESIAN_POINT('Ctrl Pts',(2.80419879604699,0.0773216531487339,
6.3529772434603));
#94092=CARTESIAN_POINT('Ctrl Pts',(1.45087604201706,2.40093070214407,6.51207751094759));
#94093=CARTESIAN_POINT('Ctrl Pts',(-1.23553671852851,2.51852308763786,6.67117777843485));
#94094=CARTESIAN_POINT('Ctrl Pts',(-2.32916856749468,0.969941120947585,
6.78334857208735));
#94095=CARTESIAN_POINT('Ctrl Pts',(-2.37510581896078,0.0921919765870843,
6.84248594324406));
#94096=CARTESIAN_POINT('Ctrl Pts',(-2.3744297718001,0.00152245248726472,
6.84858989190502));
#94097=CARTESIAN_POINT('Origin',(0.,0.,-1.84858989190512));
#94098=CARTESIAN_POINT('',(-2.37152629080235,0.002190319628347,4.65141010809494));
#94099=CARTESIAN_POINT('',(-2.36795166666981,-0.000576822865031718,4.84858989190501));
#94100=CARTESIAN_POINT('',(-2.37175,1.74448693060498E-12,-1.84858989190512));
#94101=CARTESIAN_POINT('Ctrl Pts',(-2.37152629080235,0.00219031962834669,
4.65141010809494));
#94102=CARTESIAN_POINT('Ctrl Pts',(-2.36603445450948,-0.596527709585613,
4.69158911052483));
#94103=CARTESIAN_POINT('Ctrl Pts',(-1.83185547982759,-1.99405983737433,
4.78478974757012));
#94104=CARTESIAN_POINT('Ctrl Pts',(0.518721084171678,-2.75667446873791,
4.93101201923077));
#94105=CARTESIAN_POINT('Ctrl Pts',(2.59933167366719,-1.05441952748531,5.09007692307692));
#94106=CARTESIAN_POINT('Ctrl Pts',(2.29260307415327,1.61626013811133,5.24914182692309));
#94107=CARTESIAN_POINT('Ctrl Pts',(-0.119751836615735,2.80249624215965,
5.40820673076923));
#94108=CARTESIAN_POINT('Ctrl Pts',(-2.06061632414504,1.63268656403164,5.54229615782653));
#94109=CARTESIAN_POINT('Ctrl Pts',(-2.36728681913762,0.419168440159318,
5.62336395026843));
#94110=CARTESIAN_POINT('Ctrl Pts',(-2.36788211521185,-0.000378178454202779,
5.65141010809495));
#94111=CARTESIAN_POINT('Ctrl Pts',(-2.36795166666981,-0.000576822865031856,
4.84858989190501));
#94112=CARTESIAN_POINT('Ctrl Pts',(-2.36873490379575,-0.361987846498752,
4.87275153996161));
#94113=CARTESIAN_POINT('Ctrl Pts',(-2.12091250633926,-1.5156564236008,4.94994661051396));
#94114=CARTESIAN_POINT('Ctrl Pts',(-0.323855289127461,-2.78650807957066,
5.08017510356208));
#94115=CARTESIAN_POINT('Ctrl Pts',(2.16917497708905,-1.77881686650588,5.23927537104935));
#94116=CARTESIAN_POINT('Ctrl Pts',(2.66912974919035,0.863282055751294,5.39837563853664));
#94117=CARTESIAN_POINT('Ctrl Pts',(0.716641933714364,2.71218249102838,5.55747590602391));
#94118=CARTESIAN_POINT('Ctrl Pts',(-1.74613891360093,2.10557828017548,5.70754732381337));
#94119=CARTESIAN_POINT('Ctrl Pts',(-2.36739307519176,0.652524581666242,
5.80458531910707));
#94120=CARTESIAN_POINT('Ctrl Pts',(-2.37324908705979,-0.00197702543379559,
5.84858989190501));
#94121=CARTESIAN_POINT('Origin',(0.,0.,-1.84858989190512));
#94122=CARTESIAN_POINT('',(-2.37545952780932,-0.000647831802807195,3.65141010809494));
#94123=CARTESIAN_POINT('',(-2.37112606337681,0.0021794697323349,3.84858989190501));
#94124=CARTESIAN_POINT('',(-2.37175,1.74448693060498E-12,-1.84858989190512));
#94125=CARTESIAN_POINT('Ctrl Pts',(-2.37545952780932,-0.000647831802807618,
3.65141010809494));
#94126=CARTESIAN_POINT('Ctrl Pts',(-2.37558652664713,-0.0356769482557227,
3.65377100155047));
#94127=CARTESIAN_POINT('Ctrl Pts',(-2.35898981085398,-0.857277173788602,
3.70915352962139));
#94128=CARTESIAN_POINT('Ctrl Pts',(-1.41044229536976,-2.42466043275193,
3.8175576923077));
#94129=CARTESIAN_POINT('Ctrl Pts',(1.27680339699028,-2.49761862144671,3.97662259615385));
#94130=CARTESIAN_POINT('Ctrl Pts',(2.79137735375039,-0.276655306861728,
4.1356875));
#94131=CARTESIAN_POINT('Ctrl Pts',(1.74222902142711,2.19840026511027,4.29475240384616));
#94132=CARTESIAN_POINT('Ctrl Pts',(-0.907058170011317,2.65434948083033,
4.45381730769232));
#94133=CARTESIAN_POINT('Ctrl Pts',(-2.26449923905453,1.17305206370316,4.57270320910857));
#94134=CARTESIAN_POINT('Ctrl Pts',(-2.37328167618444,0.193561806400188,
4.63856747590945));
#94135=CARTESIAN_POINT('Ctrl Pts',(-2.37152629080235,0.00219031962834669,
4.65141010809494));
#94136=CARTESIAN_POINT('Ctrl Pts',(-2.37112606337681,0.0021794697323349,
3.84858989190501));
#94137=CARTESIAN_POINT('Ctrl Pts',(-2.36586016382344,-0.583609254788488,
3.88788433832038));
#94138=CARTESIAN_POINT('Ctrl Pts',(-1.85065310628272,-1.96827731595091,
3.98021220723151));
#94139=CARTESIAN_POINT('Ctrl Pts',(0.473337684987186,-2.76504266915617,
4.12557349863841));
#94140=CARTESIAN_POINT('Ctrl Pts',(2.58207206872294,-1.09654610377387,4.28467376612568));
#94141=CARTESIAN_POINT('Ctrl Pts',(2.31835396766711,1.57947599104097,4.44377403361296));
#94142=CARTESIAN_POINT('Ctrl Pts',(-0.075507864702191,2.804248221581,4.60287430110024));
#94143=CARTESIAN_POINT('Ctrl Pts',(-2.04698568380069,1.65772178093785,4.73781292053093));
#94144=CARTESIAN_POINT('Ctrl Pts',(-2.36701574352502,0.431288484076751,
4.81971811746585));
#94145=CARTESIAN_POINT('Ctrl Pts',(-2.36795166666981,-0.000576822865031856,
4.84858989190501));
#94146=CARTESIAN_POINT('Origin',(0.,0.,-1.84858989190512));
#94147=CARTESIAN_POINT('',(-2.36956417455327,-0.00186242956101223,2.65141010809494));
#94148=CARTESIAN_POINT('',(-2.37560005937361,-0.000387335438401248,2.84858989190501));
#94149=CARTESIAN_POINT('',(-2.37175,1.74448693060498E-12,-1.84858989190512));
#94150=CARTESIAN_POINT('Ctrl Pts',(-2.36956417455326,-0.00186242956101212,
2.65141010809494));
#94151=CARTESIAN_POINT('Ctrl Pts',(-2.37148092984202,-0.264144138683627,
2.6689745271915));
#94152=CARTESIAN_POINT('Ctrl Pts',(-2.21019729025586,-1.31588391544579,
2.73956058090345));
#94153=CARTESIAN_POINT('Ctrl Pts',(-0.667532999398916,-2.7244678431737,
2.86316826923077));
#94154=CARTESIAN_POINT('Ctrl Pts',(1.93074019393295,-2.03483859399145,3.02223317307692));
#94155=CARTESIAN_POINT('Ctrl Pts',(2.75573769451142,0.523674979307748,3.18129807692308));
#94156=CARTESIAN_POINT('Ctrl Pts',(1.04974590737629,2.60122262971082,3.34036298076923));
#94157=CARTESIAN_POINT('Ctrl Pts',(-1.5807472859228,2.2943181908652,3.49706699115986));
#94158=CARTESIAN_POINT('Ctrl Pts',(-2.37273434966335,0.751017177696373,
3.60074936693509));
#94159=CARTESIAN_POINT('Ctrl Pts',(-2.37545952780932,-0.000647831802807618,
3.65141010809494));
#94160=CARTESIAN_POINT('Ctrl Pts',(-2.37560005937361,-0.000387335438401326,
2.84858989190501));
#94161=CARTESIAN_POINT('Ctrl Pts',(-2.37564677277175,-0.0210645241833399,
2.8499837141834));
#94162=CARTESIAN_POINT('Ctrl Pts',(-2.3660208670964,-0.828441659307457,
2.90441095895754));
#94163=CARTESIAN_POINT('Ctrl Pts',(-1.45398069647754,-2.39905181471807,
3.01187162622745));
#94164=CARTESIAN_POINT('Ctrl Pts',(1.23227769270891,-2.52011928935842,3.17097189371473));
#94165=CARTESIAN_POINT('Ctrl Pts',(2.78629802603849,-0.325657548824043,
3.330072161202));
#94166=CARTESIAN_POINT('Ctrl Pts',(1.78021952909652,2.16802397289482,3.48917242868929));
#94167=CARTESIAN_POINT('Ctrl Pts',(-0.861555466122802,2.66968756742434,
3.64827269617656));
#94168=CARTESIAN_POINT('Ctrl Pts',(-2.25476675598426,1.20032433252879,3.76807851724848));
#94169=CARTESIAN_POINT('Ctrl Pts',(-2.37296724131938,0.206995620831109,
3.83485091582462));
#94170=CARTESIAN_POINT('Ctrl Pts',(-2.37112606337681,0.0021794697323349,
3.84858989190501));
#94171=CARTESIAN_POINT('Origin',(0.,0.,-1.84858989190512));
#94172=CARTESIAN_POINT('',(-2.36870542925002,0.0014289424853233,1.65141010809494));
#94173=CARTESIAN_POINT('',(-2.36995499373098,-0.00198919729222008,1.84858989190501));
#94174=CARTESIAN_POINT('',(-2.37175,1.74448693060498E-12,-1.84858989190512));
#94175=CARTESIAN_POINT('Ctrl Pts',(-2.36870542925002,0.00142894248532303,
1.65141010809494));
#94176=CARTESIAN_POINT('Ctrl Pts',(-2.36602971570103,-0.488326778583579,
1.68417805283253));
#94177=CARTESIAN_POINT('Ctrl Pts',(-1.97907368647692,-1.77443351813344,
1.7699676321855));
#94178=CARTESIAN_POINT('Ctrl Pts',(0.12982574190393,-2.80204465094187,1.90877884615384));
#94179=CARTESIAN_POINT('Ctrl Pts',(2.42719129243389,-1.40608362715869,2.06784375));
#94180=CARTESIAN_POINT('Ctrl Pts',(2.49531987128246,1.28129126381962,2.22690865384615));
#94181=CARTESIAN_POINT('Ctrl Pts',(0.271637692292844,2.79186965803179,2.38597355769231));
#94182=CARTESIAN_POINT('Ctrl Pts',(-1.92843376376444,1.85461617100725,2.5274740424419));
#94183=CARTESIAN_POINT('Ctrl Pts',(-2.36569482908863,0.527604502187907,
2.61595289257612));
#94184=CARTESIAN_POINT('Ctrl Pts',(-2.36956417455326,-0.00186242956101212,
2.65141010809494));
#94185=CARTESIAN_POINT('Ctrl Pts',(-2.36995499373098,-0.00198919729222004,
1.84858989190501));
#94186=CARTESIAN_POINT('Ctrl Pts',(-2.37190237644613,-0.248671344879013,
1.86511651254217));
#94187=CARTESIAN_POINT('Ctrl Pts',(-2.22278002190394,-1.28465291067756,
1.93467655567509));
#94188=CARTESIAN_POINT('Ctrl Pts',(-0.720149694819682,-2.71125275032746,
2.05727002130378));
#94189=CARTESIAN_POINT('Ctrl Pts',(1.89163063518288,-2.07153172086814,2.21637028879105));
#94190=CARTESIAN_POINT('Ctrl Pts',(2.76534828940725,0.471549254232345,2.37547055627834));
#94191=CARTESIAN_POINT('Ctrl Pts',(1.09821595227919,2.58136221632247,2.53457082376561));
#94192=CARTESIAN_POINT('Ctrl Pts',(-1.55453093352958,2.3216703064687,2.69227726897451));
#94193=CARTESIAN_POINT('Ctrl Pts',(-2.37386937875385,0.765680029795463,
2.79695029168764));
#94194=CARTESIAN_POINT('Ctrl Pts',(-2.37560005937361,-0.000387335438401326,
2.84858989190501));
#94195=CARTESIAN_POINT('Origin',(0.,0.,-1.84858989190512));
#94196=CARTESIAN_POINT('',(-2.37475566780996,0.00146584572226412,0.651410108094944));
#94197=CARTESIAN_POINT('',(-2.36841685556579,0.00122403911035851,0.848589891905012));
#94198=CARTESIAN_POINT('',(-2.37175,1.74448693060498E-12,-1.84858989190512));
#94199=CARTESIAN_POINT('Ctrl Pts',(-2.37475566780996,0.00146584572226396,
0.651410108094944));
#94200=CARTESIAN_POINT('Ctrl Pts',(-2.37004404586893,-0.710785278156698,
0.699381578473552));
#94201=CARTESIAN_POINT('Ctrl Pts',(-1.65019917004401,-2.21908588862768,
0.800374683467544));
#94202=CARTESIAN_POINT('Ctrl Pts',(0.916620294059412,-2.65092658244327,
0.954389423076924));
#94203=CARTESIAN_POINT('Ctrl Pts',(2.72564945922899,-0.662711191614906,
1.11345432692308));
#94204=CARTESIAN_POINT('Ctrl Pts',(2.03137230801958,1.93443429127041,1.27251923076923));
#94205=CARTESIAN_POINT('Ctrl Pts',(-0.528630951316314,2.75477110121152,
1.43158413461539));
#94206=CARTESIAN_POINT('Ctrl Pts',(-2.17575442924696,1.39728243218704,1.55788109372396));
#94207=CARTESIAN_POINT('Ctrl Pts',(-2.37035927336069,0.304144311723338,
1.63115641821714));
#94208=CARTESIAN_POINT('Ctrl Pts',(-2.36870542925002,0.00142894248532303,
1.65141010809494));
#94209=CARTESIAN_POINT('Ctrl Pts',(-2.36841685556579,0.00122403911035841,
0.848589891905012));
#94210=CARTESIAN_POINT('Ctrl Pts',(-2.36625022962319,-0.472111298629738,
0.880249310900949));
#94211=CARTESIAN_POINT('Ctrl Pts',(-1.99902079532434,-1.74146140232311,
0.964942152392647));
#94212=CARTESIAN_POINT('Ctrl Pts',(0.0718874078444588,-2.8043235471302,
1.1026684163801));
#94213=CARTESIAN_POINT('Ctrl Pts',(2.39810709656883,-1.45554260356973,1.26176868386738));
#94214=CARTESIAN_POINT('Ctrl Pts',(2.52091778453322,1.23065290615308,1.42086895135466));
#94215=CARTESIAN_POINT('Ctrl Pts',(0.327458637825707,2.78608392325822,1.57996921884194));
#94216=CARTESIAN_POINT('Ctrl Pts',(-1.90777171460039,1.8859618485243,1.72254286569206));
#94217=CARTESIAN_POINT('Ctrl Pts',(-2.36565328459846,0.542924156848317,
1.81208309004641));
#94218=CARTESIAN_POINT('Ctrl Pts',(-2.36995499373098,-0.00198919729222004,
1.84858989190501));
#94219=CARTESIAN_POINT('Origin',(0.,0.,49.5));
#94220=CARTESIAN_POINT('',(-2.86956349206012,0.00162216627751805,49.1339652973708));
#94221=CARTESIAN_POINT('Ctrl Pts',(-0.439445221993838,2.33068358199194,
49.62825));
#94222=CARTESIAN_POINT('Ctrl Pts',(-0.359505261208484,2.34930630909117,
49.6247612467635));
#94223=CARTESIAN_POINT('Ctrl Pts',(-0.278760108098212,2.36340128745442,
49.6212867191599));
#94224=CARTESIAN_POINT('Ctrl Pts',(-0.197534229629186,2.37315541881725,
49.6178216918657));
#94225=CARTESIAN_POINT('Ctrl Pts',(-0.114150649388022,2.3831686610315,49.6142646188385));
#94226=CARTESIAN_POINT('Ctrl Pts',(-0.0302597106601846,2.38860739990529,
49.6107175575613));
#94227=CARTESIAN_POINT('Ctrl Pts',(0.0538029108463651,2.38962152881013,
49.6071753960455));
#94228=CARTESIAN_POINT('Ctrl Pts',(0.0939026325081102,2.3901052906306,49.605485706998));
#94229=CARTESIAN_POINT('Ctrl Pts',(0.134041570065805,2.38958147509166,49.6037971328912));
#94230=CARTESIAN_POINT('Ctrl Pts',(0.174183675497746,2.38806230251539,49.6021091188373));
#94231=CARTESIAN_POINT('Ctrl Pts',(0.198287612532619,2.3871500922631,49.6010955251549));
#94232=CARTESIAN_POINT('Ctrl Pts',(0.222392693138791,2.3858789481315,49.6000821334042));
#94233=CARTESIAN_POINT('Ctrl Pts',(0.24649108949659,2.38425107690571,49.5990688234506));
#94234=CARTESIAN_POINT('Ctrl Pts',(0.262231163126216,2.38318781889581,49.5984069713903));
#94235=CARTESIAN_POINT('Ctrl Pts',(0.277969056250135,2.38197221991301,49.5977451258474));
#94236=CARTESIAN_POINT('Ctrl Pts',(0.293686527897986,2.3806064861569,49.5970839288824));
#94237=CARTESIAN_POINT('Ctrl Pts',(0.379432205080258,2.37315581162149,49.5934768104613));
#94238=CARTESIAN_POINT('Ctrl Pts',(0.464683129359647,2.36123436880514,49.5898842179419));
#94239=CARTESIAN_POINT('Ctrl Pts',(0.549087259753569,2.34500689677144,49.5863009155998));
#94240=CARTESIAN_POINT('Ctrl Pts',(0.634238389507191,2.32863580722564,49.5826859000639));
#94241=CARTESIAN_POINT('Ctrl Pts',(0.71852862073425,2.30788198144388,49.5790803398741));
#94242=CARTESIAN_POINT('Ctrl Pts',(0.801595693877686,2.28286147762408,49.5754788590594));
#94243=CARTESIAN_POINT('Ctrl Pts',(0.854183456323832,2.26702159954283,49.5731988483359));
#94244=CARTESIAN_POINT('Ctrl Pts',(0.906280934573225,2.249470645855,49.5709204725652));
#94245=CARTESIAN_POINT('Ctrl Pts',(0.957793381125661,2.23022763047868,49.5686423677162));
#94246=CARTESIAN_POINT('Ctrl Pts',(0.971987759697525,2.22492517129849,49.5680146304446));
#94247=CARTESIAN_POINT('Ctrl Pts',(0.986130767173139,2.21949673426825,49.567387219577));
#94248=CARTESIAN_POINT('Ctrl Pts',(1.00021413720228,2.21394563250679,49.566760392062));
#94249=CARTESIAN_POINT('Ctrl Pts',(1.08183853281852,2.18177255707487,49.5631274251686));
#94250=CARTESIAN_POINT('Ctrl Pts',(1.16152778287534,2.1454580421936,49.5595110591734));
#94251=CARTESIAN_POINT('Ctrl Pts',(1.23892280784953,2.10514980872508,49.5559059771857));
#94252=CARTESIAN_POINT('Ctrl Pts',(1.31588775121095,2.06506556678656,49.5523209285203));
#94253=CARTESIAN_POINT('Ctrl Pts',(1.39058484076766,2.02103157966364,49.5487470388013));
#94254=CARTESIAN_POINT('Ctrl Pts',(1.46264758633523,1.97314377781481,49.5451790792837));
#94255=CARTESIAN_POINT('Ctrl Pts',(1.52263782893736,1.93327850723751,49.5422088516665));
#94256=CARTESIAN_POINT('Ctrl Pts',(1.58080248046675,1.89074157080871,49.5392427337394));
#94257=CARTESIAN_POINT('Ctrl Pts',(1.63691585662181,1.8455640580499,49.5362777089777));
#94258=CARTESIAN_POINT('Ctrl Pts',(1.66497254469934,1.82297530167049,49.5347951965969));
#94259=CARTESIAN_POINT('Ctrl Pts',(1.69251617012281,1.79972606657414,49.5333129575074));
#94260=CARTESIAN_POINT('Ctrl Pts',(1.71951680922542,1.77581828500007,49.5318306146436));
#94261=CARTESIAN_POINT('Ctrl Pts',(1.73353427516679,1.76340648568396,49.531061051726));
#94262=CARTESIAN_POINT('Ctrl Pts',(1.74740537466393,1.75081717401828,49.5302914608391));
#94263=CARTESIAN_POINT('Ctrl Pts',(1.76112577636582,1.7380504867577,49.5295217892232));
#94264=CARTESIAN_POINT('Ctrl Pts',(1.76984010737801,1.72994189481303,49.5290329425132));
#94265=CARTESIAN_POINT('Ctrl Pts',(1.77849214411516,1.72176307914284,49.5285441456439));
#94266=CARTESIAN_POINT('Ctrl Pts',(1.78707439365716,1.71352049619226,49.5280557560924));
#94267=CARTESIAN_POINT('Ctrl Pts',(1.79100755903657,1.70974299686188,49.5278319316899));
#94268=CARTESIAN_POINT('Ctrl Pts',(1.79492646082255,1.70595173973429,49.5276081707935));
#94269=CARTESIAN_POINT('Ctrl Pts',(1.79883101418844,1.70214675534458,49.5273844721621));
#94270=CARTESIAN_POINT('Ctrl Pts',(1.85864861208173,1.64385455009475,49.5239574182779));
#94271=CARTESIAN_POINT('Ctrl Pts',(1.91510096641586,1.58234433908994,49.5205449780736));
#94272=CARTESIAN_POINT('Ctrl Pts',(1.96816958093575,1.51800814503369,49.5171426893277));
#94273=CARTESIAN_POINT('Ctrl Pts',(2.02278845482118,1.45179253904477,49.5136410117049));
#94274=CARTESIAN_POINT('Ctrl Pts',(2.07382343813989,1.38258284038499,49.5101500872995));
#94275=CARTESIAN_POINT('Ctrl Pts',(2.12122068206654,1.31076313229951,49.5066650512987));
#94276=CARTESIAN_POINT('Ctrl Pts',(2.16728133943421,1.24096871616235,49.5032782921573));
#94277=CARTESIAN_POINT('Ctrl Pts',(2.20990663387466,1.16870853483454,49.4998970940011));
#94278=CARTESIAN_POINT('Ctrl Pts',(2.24901234132568,1.0943063482077,49.4965169920791));
#94279=CARTESIAN_POINT('Ctrl Pts',(2.2661210883355,1.06175539155845,49.4950381974882));
#94280=CARTESIAN_POINT('Ctrl Pts',(2.28255569813228,1.02879414143743,49.4935596127234));
#94281=CARTESIAN_POINT('Ctrl Pts',(2.29830685053076,0.995448545649893,49.4920808639053));
#94282=CARTESIAN_POINT('Ctrl Pts',(2.30471320039571,0.981886137791351,49.4914794233217));
#94283=CARTESIAN_POINT('Ctrl Pts',(2.31100647394448,0.96826014379224,49.4908779555999));
#94284=CARTESIAN_POINT('Ctrl Pts',(2.31718597494133,0.954572285797792,49.4902764355847));
#94285=CARTESIAN_POINT('Ctrl Pts',(2.32211929848942,0.943644763947515,49.4897962199723));
#94286=CARTESIAN_POINT('Ctrl Pts',(2.32697938553938,0.932679312829285,49.4893160377747));
#94287=CARTESIAN_POINT('Ctrl Pts',(2.33176231477172,0.921685451781552,49.4888362497009));
#94288=CARTESIAN_POINT('Ctrl Pts',(2.36731939269898,0.839955291244647,49.4852694267143));
#94289=CARTESIAN_POINT('Ctrl Pts',(2.3986749483017,0.756527190235498,49.4817186327847));
#94290=CARTESIAN_POINT('Ctrl Pts',(2.42577696253307,0.671808303375818,49.4781788484286));
#94291=CARTESIAN_POINT('Ctrl Pts',(2.45320047087974,0.586084449750662,49.4745970738414));
#94292=CARTESIAN_POINT('Ctrl Pts',(2.47626933263316,0.499038107217648,49.4710265715762));
#94293=CARTESIAN_POINT('Ctrl Pts',(2.49488476821487,0.411062505937825,49.4674621413933));
#94294=CARTESIAN_POINT('Ctrl Pts',(2.51281826366768,0.326309719005444,49.4640282871492));
#94295=CARTESIAN_POINT('Ctrl Pts',(2.52661866832979,0.240693578216629,49.4606000682581));
#94296=CARTESIAN_POINT('Ctrl Pts',(2.53615367370349,0.154552993143809,49.4571728353021));
#94297=CARTESIAN_POINT('Ctrl Pts',(2.53972930071863,0.122250273741502,49.4558876229436));
#94298=CARTESIAN_POINT('Ctrl Pts',(2.54270464826766,0.0898737425312771,
49.4546025492322));
#94299=CARTESIAN_POINT('Ctrl Pts',(2.54507104088501,0.0574411829209008,
49.4533173689837));
#94300=CARTESIAN_POINT('Ctrl Pts',(2.54659675859018,0.0365304810961177,
49.4524887565865));
#94301=CARTESIAN_POINT('Ctrl Pts',(2.54786931761251,0.0155964887192117,
49.4516600999024));
#94302=CARTESIAN_POINT('Ctrl Pts',(2.54888617789747,-0.00535601068066993,
49.4508313332178));
#94303=CARTESIAN_POINT('Ctrl Pts',(2.54959366579885,-0.0199338637528056,
49.4502547128));
#94304=CARTESIAN_POINT('Ctrl Pts',(2.55017695702511,-0.0345129004678059,
49.4496783466839));
#94305=CARTESIAN_POINT('Ctrl Pts',(2.5506354515805,-0.0490849422160798,
49.4491024711239));
#94306=CARTESIAN_POINT('Ctrl Pts',(2.55349263168339,-0.139892885849451,
49.4455138130422));
#94307=CARTESIAN_POINT('Ctrl Pts',(2.55151149704795,-0.230507570687691,
49.4419410548054));
#94308=CARTESIAN_POINT('Ctrl Pts',(2.54459631698184,-0.320534826816672,
49.4383790803832));
#94309=CARTESIAN_POINT('Ctrl Pts',(2.53778415703423,-0.409220885969587,
49.4348701711051));
#94310=CARTESIAN_POINT('Ctrl Pts',(2.52618405231378,-0.497337839177241,
49.4313717267274));
#94311=CARTESIAN_POINT('Ctrl Pts',(2.50965462981406,-0.584515376296054,
49.4278788564812));
#94312=CARTESIAN_POINT('Ctrl Pts',(2.50750901683598,-0.595831516048816,
49.4274254620731));
#94313=CARTESIAN_POINT('Ctrl Pts',(2.50528027513273,-0.607131824718634,
49.4269721615863));
#94314=CARTESIAN_POINT('Ctrl Pts',(2.50296803009266,-0.618415487757582,
49.4265189443241));
#94315=CARTESIAN_POINT('Ctrl Pts',(2.48519637484993,-0.705140452425336,
49.4230355674352));
#94316=CARTESIAN_POINT('Ctrl Pts',(2.46249614940113,-0.790883208828462,
49.4195571068563));
#94317=CARTESIAN_POINT('Ctrl Pts',(2.43513714111733,-0.8753863679234,49.416078705898));
#94318=CARTESIAN_POINT('Ctrl Pts',(2.42592803142475,-0.903830339773648,
49.414907867553));
#94319=CARTESIAN_POINT('Ctrl Pts',(2.4161906539963,-0.932133740819968,49.4137370359631));
#94320=CARTESIAN_POINT('Ctrl Pts',(2.40593406766555,-0.96028630774472,49.4125660259065));
#94321=CARTESIAN_POINT('Ctrl Pts',(2.39924822373631,-0.978637800395067,
49.4118026929392));
#94322=CARTESIAN_POINT('Ctrl Pts',(2.39233957405065,-0.996930415172384,
49.4110390638345));
#94323=CARTESIAN_POINT('Ctrl Pts',(2.38522272103957,-1.01513098367692,49.4102763599805));
#94324=CARTESIAN_POINT('Ctrl Pts',(2.35171164784641,-1.10083186612637,49.4066850219782));
#94325=CARTESIAN_POINT('Ctrl Pts',(2.31355264766449,-1.18460163813465,49.4031096924922));
#94326=CARTESIAN_POINT('Ctrl Pts',(2.27110938627169,-1.26617525182304,49.3995452516877));
#94327=CARTESIAN_POINT('Ctrl Pts',(2.2290466817146,-1.34701745620675,49.3960127705458));
#94328=CARTESIAN_POINT('Ctrl Pts',(2.18277549541836,-1.4257034416751,49.3924909836995));
#94329=CARTESIAN_POINT('Ctrl Pts',(2.13259475634065,-1.50196208234925,49.3889749078001));
#94330=CARTESIAN_POINT('Ctrl Pts',(2.08216402897786,-1.57860062509649,49.3854413156623));
#94331=CARTESIAN_POINT('Ctrl Pts',(2.02778413096789,-1.65278836814677,49.3819134915142));
#94332=CARTESIAN_POINT('Ctrl Pts',(1.96971197405773,-1.72422532172408,49.3783863771579));
#94333=CARTESIAN_POINT('Ctrl Pts',(1.94766500938463,-1.75134620160306,49.3770473160699));
#94334=CARTESIAN_POINT('Ctrl Pts',(1.92508543871163,-1.7780702874266,49.3757083572859));
#94335=CARTESIAN_POINT('Ctrl Pts',(1.90198583988356,-1.80437986478666,49.3743692240236));
#94336=CARTESIAN_POINT('Ctrl Pts',(1.88944491551879,-1.81866350764111,49.3736421997544));
#94337=CARTESIAN_POINT('Ctrl Pts',(1.87675070104281,-1.83282496139081,49.3729151240582));
#94338=CARTESIAN_POINT('Ctrl Pts',(1.86390512055704,-1.84686128720403,49.372187952644));
#94339=CARTESIAN_POINT('Ctrl Pts',(1.85444773605752,-1.85719534180929,49.3716525825478));
#94340=CARTESIAN_POINT('Ctrl Pts',(1.84491471803415,-1.86745454471056,49.3711175241102));
#94341=CARTESIAN_POINT('Ctrl Pts',(1.83530860507554,-1.87763647573028,49.3705828398716));
#94342=CARTESIAN_POINT('Ctrl Pts',(1.77156448674401,-1.94520159999665,49.3670347892161));
#94343=CARTESIAN_POINT('Ctrl Pts',(1.70458530858084,-2.00938821260543,49.363502069587));
#94344=CARTESIAN_POINT('Ctrl Pts',(1.63467500708789,-2.06992478749503,49.3599797407958));
#94345=CARTESIAN_POINT('Ctrl Pts',(1.5647324226398,-2.13048931677031,49.3564557854748));
#94346=CARTESIAN_POINT('Ctrl Pts',(1.49185537900294,-2.18740119976334,49.3529422305904));
#94347=CARTESIAN_POINT('Ctrl Pts',(1.4163068404822,-2.24035820837223,49.3494341291071));
#94348=CARTESIAN_POINT('Ctrl Pts',(1.34192288164103,-2.29249888542362,49.3459801049597));
#94349=CARTESIAN_POINT('Ctrl Pts',(1.26494848743881,-2.34080631444827,49.3425313673809));
#94350=CARTESIAN_POINT('Ctrl Pts',(1.18560428430781,-2.3849524025052,49.3390831946023));
#94351=CARTESIAN_POINT('Ctrl Pts',(1.1560523297861,-2.40139472765421,49.3377989136957));
#94352=CARTESIAN_POINT('Ctrl Pts',(1.12617137745806,-2.41725934019025,49.3365147111386));
#94353=CARTESIAN_POINT('Ctrl Pts',(1.095972007602,-2.43252757553188,49.3352303429717));
#94354=CARTESIAN_POINT('Ctrl Pts',(1.07971681644229,-2.4407458954946,49.3345390156303));
#94355=CARTESIAN_POINT('Ctrl Pts',(1.06336936453226,-2.44879141198345,49.3338476403074));
#94356=CARTESIAN_POINT('Ctrl Pts',(1.04693125869691,-2.45666108941232,49.3331561789576));
#94357=CARTESIAN_POINT('Ctrl Pts',(1.03431734823736,-2.46269994859887,49.3326255806247));
#94358=CARTESIAN_POINT('Ctrl Pts',(1.02165372665814,-2.46863344887536,49.3320950869736));
#94359=CARTESIAN_POINT('Ctrl Pts',(1.00894994693436,-2.47445653363982,49.3315650429079));
#94360=CARTESIAN_POINT('Ctrl Pts',(0.961614070867921,-2.49615407757779,
49.3295900322613));
#94361=CARTESIAN_POINT('Ctrl Pts',(0.91368552170473,-2.51633592893095,49.3276197738702));
#94362=CARTESIAN_POINT('Ctrl Pts',(0.865212251108304,-2.53495176364714,
49.3256534164861));
#94363=CARTESIAN_POINT('Ctrl Pts',(0.781689405409389,-2.56702815278748,
49.3222652447708));
#94364=CARTESIAN_POINT('Ctrl Pts',(0.69655068261115,-2.59445802060023,49.3188886550312));
#94365=CARTESIAN_POINT('Ctrl Pts',(0.610163038527935,-2.61737933997433,
49.3155192924974));
#94366=CARTESIAN_POINT('Ctrl Pts',(0.521562429201812,-2.64088782761347,
49.3120636180579));
#94367=CARTESIAN_POINT('Ctrl Pts',(0.431647336561218,-2.65965394393264,
49.308615545841));
#94368=CARTESIAN_POINT('Ctrl Pts',(0.340792399615863,-2.67377635564093,
49.305170377766));
#94369=CARTESIAN_POINT('Ctrl Pts',(0.251252423365253,-2.6876943710122,49.3017750722606));
#94370=CARTESIAN_POINT('Ctrl Pts',(0.16079875261803,-2.69710194612434,49.298382587441));
#94371=CARTESIAN_POINT('Ctrl Pts',(0.0697819260538942,-2.70204634331308,
49.2949884262775));
#94372=CARTESIAN_POINT('Ctrl Pts',(0.056678488182449,-2.7027581743428,49.2944997783911));
#94373=CARTESIAN_POINT('Ctrl Pts',(0.0435624055918989,-2.70337745931282,
49.2940110595948));
#94374=CARTESIAN_POINT('Ctrl Pts',(0.0304377310135361,-2.70390414115064,
49.2935223683404));
#94375=CARTESIAN_POINT('Ctrl Pts',(-0.0632353432642269,-2.70766316059304,
49.290034494268));
#94376=CARTESIAN_POINT('Ctrl Pts',(-0.156972776620133,-2.70669504074848,
49.2865618620568));
#94377=CARTESIAN_POINT('Ctrl Pts',(-0.250383234795894,-2.70113638510294,
49.2830997990332));
#94378=CARTESIAN_POINT('Ctrl Pts',(-0.345161089864368,-2.69549635860658,
49.2795870563073));
#94379=CARTESIAN_POINT('Ctrl Pts',(-0.43960325480989,-2.68513042806245,
49.2760851944697));
#94380=CARTESIAN_POINT('Ctrl Pts',(-0.533311979758323,-2.67012840852803,
49.2725893326246));
#94381=CARTESIAN_POINT('Ctrl Pts',(-0.626952633413095,-2.65513728666486,
49.2690960102211));
#94382=CARTESIAN_POINT('Ctrl Pts',(-0.719861888547964,-2.6355167074097,
49.2656086790962));
#94383=CARTESIAN_POINT('Ctrl Pts',(-0.811639396756275,-2.61130474078774,
49.262122468983));
#94384=CARTESIAN_POINT('Ctrl Pts',(-0.852869462444847,-2.6004277732849,
49.2605563263105));
#94385=CARTESIAN_POINT('Ctrl Pts',(-0.893870988019684,-2.58862350739258,
49.2589904098762));
#94386=CARTESIAN_POINT('Ctrl Pts',(-0.934606640503465,-2.57589208119221,
49.2574242781235));
#94387=CARTESIAN_POINT('Ctrl Pts',(-0.955365781692795,-2.56940406742735,
49.2566261676677));
#94388=CARTESIAN_POINT('Ctrl Pts',(-0.976055862454838,-2.562675238885,49.255828001294));
#94389=CARTESIAN_POINT('Ctrl Pts',(-0.996671844395906,-2.55570541111516,
49.2550297205652));
#94390=CARTESIAN_POINT('Ctrl Pts',(-1.01068707739322,-2.55096715705456,
49.2544870304113));
#94391=CARTESIAN_POINT('Ctrl Pts',(-1.02466976493489,-2.54611684946725,
49.2539442204075));
#94392=CARTESIAN_POINT('Ctrl Pts',(-1.03860223115708,-2.54116030770371,
49.2534019001196));
#94393=CARTESIAN_POINT('Ctrl Pts',(-1.12917963816755,-2.50893696019858,
49.2498761807911));
#94394=CARTESIAN_POINT('Ctrl Pts',(-1.21777942064694,-2.47218038079066,
49.2463655720126));
#94395=CARTESIAN_POINT('Ctrl Pts',(-1.30400292535831,-2.43098062826895,
49.242865238774));
#94396=CARTESIAN_POINT('Ctrl Pts',(-1.38886736099538,-2.39043027302829,
49.2394200783642));
#94397=CARTESIAN_POINT('Ctrl Pts',(-1.47143074991837,-2.34557546596676,
49.2359848721178));
#94398=CARTESIAN_POINT('Ctrl Pts',(-1.55130162346499,-2.29645380037892,
49.2325550100709));
#94399=CARTESIAN_POINT('Ctrl Pts',(-1.6116479732812,-2.25933998049077,49.2299635816101));
#94400=CARTESIAN_POINT('Ctrl Pts',(-1.6704571549813,-2.21978942207171,49.2273752039075));
#94401=CARTESIAN_POINT('Ctrl Pts',(-1.72755116942149,-2.17780075375096,
49.224787888648));
#94402=CARTESIAN_POINT('Ctrl Pts',(-1.76872966611956,-2.14751683946056,
49.2229218129497));
#94403=CARTESIAN_POINT('Ctrl Pts',(-1.80901576369452,-2.11596429670162,
49.2210562899208));
#94404=CARTESIAN_POINT('Ctrl Pts',(-1.84838795223496,-2.08320010102078,
49.2191905735852));
#94405=CARTESIAN_POINT('Ctrl Pts',(-1.87206203371001,-2.06349933591812,
49.2180687380415));
#94406=CARTESIAN_POINT('Ctrl Pts',(-1.89540563437032,-2.04336042988252,
49.2169468326079));
#94407=CARTESIAN_POINT('Ctrl Pts',(-1.91841351965119,-2.02279520631578,
49.2158246951126));
#94408=CARTESIAN_POINT('Ctrl Pts',(-1.93117286120055,-2.01139047666229,
49.2152023982177));
#94409=CARTESIAN_POINT('Ctrl Pts',(-1.94383029046328,-1.99985323695415,
49.2145799600185));
#94410=CARTESIAN_POINT('Ctrl Pts',(-1.95636866376425,-1.98820093939874,
49.2139581660398));
#94411=CARTESIAN_POINT('Ctrl Pts',(-2.02501357614443,-1.92440710223034,
49.2105539769829));
#94412=CARTESIAN_POINT('Ctrl Pts',(-2.09020338271483,-1.8570710837208,49.2071637169369));
#94413=CARTESIAN_POINT('Ctrl Pts',(-2.15185690424115,-1.78660322661286,
49.2037830333995));
#94414=CARTESIAN_POINT('Ctrl Pts',(-2.21484733000207,-1.71460733389174,
49.2003290426117));
#94415=CARTESIAN_POINT('Ctrl Pts',(-2.27414695035793,-1.63934166565729,
49.1968850481522));
#94416=CARTESIAN_POINT('Ctrl Pts',(-2.3296369179527,-1.5611981913315,49.1934464081936));
#94417=CARTESIAN_POINT('Ctrl Pts',(-2.38568234800599,-1.48227248972664,
49.1899733469605));
#94418=CARTESIAN_POINT('Ctrl Pts',(-2.43784197477932,-1.40041028970125,
49.1865057479634));
#94419=CARTESIAN_POINT('Ctrl Pts',(-2.48595320048127,-1.31598041155428,
49.1830388285787));
#94420=CARTESIAN_POINT('Ctrl Pts',(-2.51305842340654,-1.26841374420506,
49.1810856124339));
#94421=CARTESIAN_POINT('Ctrl Pts',(-2.53887790137548,-1.22003151950339,
49.1791326120012));
#94422=CARTESIAN_POINT('Ctrl Pts',(-2.56337609854124,-1.17089633028993,
49.1771789720447));
#94423=CARTESIAN_POINT('Ctrl Pts',(-2.56995917422177,-1.15769288242065,
49.1766539962843));
#94424=CARTESIAN_POINT('Ctrl Pts',(-2.57644782254101,-1.14443294732825,
49.1761288913047));
#94425=CARTESIAN_POINT('Ctrl Pts',(-2.58283802576922,-1.13112453966317,
49.1756039094184));
#94426=CARTESIAN_POINT('Ctrl Pts',(-2.62538221167359,-1.04252088347651,
49.1721087268444));
#94427=CARTESIAN_POINT('Ctrl Pts',(-2.66345146630088,-0.952014028769855,
49.168628527235));
#94428=CARTESIAN_POINT('Ctrl Pts',(-2.69692936295805,-0.860010437873625,
49.1651586115314));
#94429=CARTESIAN_POINT('Ctrl Pts',(-2.73050479700952,-0.767738795772912,
49.1616785862758));
#94430=CARTESIAN_POINT('Ctrl Pts',(-2.75946252850468,-0.673960808919952,
49.1582089049373));
#94431=CARTESIAN_POINT('Ctrl Pts',(-2.78364169059793,-0.579056964346966,
49.1547448272653));
#94432=CARTESIAN_POINT('Ctrl Pts',(-2.80735578926856,-0.48597850588979,
49.1513473778666));
#94433=CARTESIAN_POINT('Ctrl Pts',(-2.82647364105441,-0.391816203459708,
49.1479553186449));
#94434=CARTESIAN_POINT('Ctrl Pts',(-2.84079674623874,-0.296913748806167,
49.1445641776455));
#94435=CARTESIAN_POINT('Ctrl Pts',(-2.85209612830125,-0.222045968391273,
49.1418889338846));
#94436=CARTESIAN_POINT('Ctrl Pts',(-2.86041066761624,-0.146717119309908,
49.1392142615796));
#94437=CARTESIAN_POINT('Ctrl Pts',(-2.86561997416828,-0.0710943294859263,
49.1365379651472));
#94438=CARTESIAN_POINT('Ctrl Pts',(-2.86729088743676,-0.0468379103917938,
49.1356795285828));
#94439=CARTESIAN_POINT('Ctrl Pts',(-2.86864006663653,-0.0225815264959612,
49.1348219958472));
#94440=CARTESIAN_POINT('Ctrl Pts',(-2.86966548199755,0.0016690505250476,
49.1339652973708));
#94441=CARTESIAN_POINT('',(0.260874132846714,2.92567963864295,49.058));
#94442=CARTESIAN_POINT('Ctrl Pts',(0.260739855805342,2.92492329228914,49.058));
#94443=CARTESIAN_POINT('Ctrl Pts',(0.162865051941415,2.92111867579054,49.0703774519651));
#94444=CARTESIAN_POINT('Ctrl Pts',(0.0654587677403667,2.91267041664908,
49.0827990502223));
#94445=CARTESIAN_POINT('Ctrl Pts',(-0.0311012750313888,2.89958669379796,
49.0952843365015));
#94446=CARTESIAN_POINT('Ctrl Pts',(-0.129420938708193,2.88626454528355,
49.1079971430894));
#94447=CARTESIAN_POINT('Ctrl Pts',(-0.226864310025817,2.86813635666484,
49.1207759800322));
#94448=CARTESIAN_POINT('Ctrl Pts',(-0.323009383677986,2.84515947512996,
49.1336414769778));
#94449=CARTESIAN_POINT('Ctrl Pts',(-0.413314826332502,2.82357815661815,
49.1457255531816));
#94450=CARTESIAN_POINT('Ctrl Pts',(-0.502475357477472,2.79771863584763,
49.1578860820237));
#94451=CARTESIAN_POINT('Ctrl Pts',(-0.59011056116163,2.76750695016159,49.1701401578498));
#94452=CARTESIAN_POINT('Ctrl Pts',(-0.618328969582016,2.75777883121033,
49.1740859524842));
#94453=CARTESIAN_POINT('Ctrl Pts',(-0.646388950214392,2.74759918873813,
49.1780414463566));
#94454=CARTESIAN_POINT('Ctrl Pts',(-0.674276952688285,2.73696477818488,
49.1820072101754));
#94455=CARTESIAN_POINT('Ctrl Pts',(-0.694945139639471,2.72908346844834,
49.1849462929616));
#94456=CARTESIAN_POINT('Ctrl Pts',(-0.715518858776697,2.72095236969504,
49.1878910165143));
#94457=CARTESIAN_POINT('Ctrl Pts',(-0.735992427615463,2.71257003283589,
49.1908416131441));
#94458=CARTESIAN_POINT('Ctrl Pts',(-0.750134370446515,2.7067800052356,49.1928797125681));
#94459=CARTESIAN_POINT('Ctrl Pts',(-0.764229517079808,2.70086959326046,
49.1949207644322));
#94460=CARTESIAN_POINT('Ctrl Pts',(-0.778260340253251,2.69484524810002,
49.1969625551167));
#94461=CARTESIAN_POINT('Ctrl Pts',(-0.861823008089798,2.65896635864705,
49.2091227451959));
#94462=CARTESIAN_POINT('Ctrl Pts',(-0.943237200345705,2.6189972815904,49.2213278864296));
#94463=CARTESIAN_POINT('Ctrl Pts',(-1.02217019948904,2.57491088258204,49.2335969425659));
#94464=CARTESIAN_POINT('Ctrl Pts',(-1.06131160945252,2.5530492551749,49.2396809398966));
#94465=CARTESIAN_POINT('Ctrl Pts',(-1.09984243477703,2.53017455154342,49.2457806538004));
#94466=CARTESIAN_POINT('Ctrl Pts',(-1.13771892917144,2.50627986935387,49.2518983966494));
#94467=CARTESIAN_POINT('Ctrl Pts',(-1.21599994719749,2.45689567799419,49.2645422050562));
#94468=CARTESIAN_POINT('Ctrl Pts',(-1.29148891934137,2.40315618786065,49.2772630228555));
#94469=CARTESIAN_POINT('Ctrl Pts',(-1.36397315623523,2.34538874880156,49.2900812635639));
#94470=CARTESIAN_POINT('Ctrl Pts',(-1.43889280980964,2.28568036657046,49.3033301876675));
#94471=CARTESIAN_POINT('Ctrl Pts',(-1.5106031566708,2.22166779667127,49.3166831913371));
#94472=CARTESIAN_POINT('Ctrl Pts',(-1.57881491577384,2.15369213867893,49.3301628156358));
#94473=CARTESIAN_POINT('Ctrl Pts',(-1.59215311282773,2.1404001090774,49.3327986351408));
#94474=CARTESIAN_POINT('Ctrl Pts',(-1.6053573553333,2.12695651327283,49.3354392961489));
#94475=CARTESIAN_POINT('Ctrl Pts',(-1.61842521038769,2.11336386827515,49.3380849671945));
#94476=CARTESIAN_POINT('Ctrl Pts',(-1.62805298867044,2.1033494495531,49.3400341726402));
#94477=CARTESIAN_POINT('Ctrl Pts',(-1.63760069310815,2.09326038599484,49.3419848774496));
#94478=CARTESIAN_POINT('Ctrl Pts',(-1.64706556304477,2.08310024119305,49.3439367104448));
#94479=CARTESIAN_POINT('Ctrl Pts',(-1.70828813901715,2.01738034845456,49.3565619493159));
#94480=CARTESIAN_POINT('Ctrl Pts',(-1.76607890037575,1.94865710831166,49.3692405129108));
#94481=CARTESIAN_POINT('Ctrl Pts',(-1.82026814410794,1.87725108113391,49.3819940806871));
#94482=CARTESIAN_POINT('Ctrl Pts',(-1.87420815042845,1.80617347805226,49.3946889898441));
#94483=CARTESIAN_POINT('Ctrl Pts',(-1.92457998069414,1.73243671357817,49.4074582148224));
#94484=CARTESIAN_POINT('Ctrl Pts',(-1.97116800133376,1.65633974881965,49.4203231373166));
#94485=CARTESIAN_POINT('Ctrl Pts',(-2.01693944620795,1.5815765805262,49.4329625687126));
#94486=CARTESIAN_POINT('Ctrl Pts',(-2.05905869204356,1.50453433051914,49.4456943723306));
#94487=CARTESIAN_POINT('Ctrl Pts',(-2.09727163215101,1.42549384358289,49.4585388251477));
#94488=CARTESIAN_POINT('Ctrl Pts',(-2.1192404942794,1.38005296530499,49.4659231827046));
#94489=CARTESIAN_POINT('Ctrl Pts',(-2.13991732470015,1.33395165722691,49.4733447727726));
#94490=CARTESIAN_POINT('Ctrl Pts',(-2.15924596868274,1.28724457024862,49.4808074483121));
#94491=CARTESIAN_POINT('Ctrl Pts',(-2.16488416199063,1.27362004565863,49.4829843215228));
#94492=CARTESIAN_POINT('Ctrl Pts',(-2.17040807886406,1.25994255303091,49.4851649158573));
#94493=CARTESIAN_POINT('Ctrl Pts',(-2.17580969047169,1.24623072785564,49.4873465904162));
#94494=CARTESIAN_POINT('Ctrl Pts',(-2.20698364607134,1.16709659895971,49.4999375411865));
#94495=CARTESIAN_POINT('Ctrl Pts',(-2.23414211094401,1.08669178286697,49.5125848962906));
#94496=CARTESIAN_POINT('Ctrl Pts',(-2.25710446510236,1.00528373148052,49.5253107322942));
#94497=CARTESIAN_POINT('Ctrl Pts',(-2.27971678650434,0.925116645389746,
49.5378425786301));
#94498=CARTESIAN_POINT('Ctrl Pts',(-2.29826001442132,0.843975867542557,
49.5504505314132));
#94499=CARTESIAN_POINT('Ctrl Pts',(-2.31251203424867,0.762119412589603,
49.563155672931));
#94500=CARTESIAN_POINT('Ctrl Pts',(-2.32635004093017,0.682640841532014,
49.5754917372462));
#94501=CARTESIAN_POINT('Ctrl Pts',(-2.33614243912025,0.602486942314531,
49.5879194257547));
#94502=CARTESIAN_POINT('Ctrl Pts',(-2.34163918216539,0.521906755120729,
49.6004580363135));
#94503=CARTESIAN_POINT('Ctrl Pts',(-2.34567307551512,0.462771394677,49.6096597430938));
#94504=CARTESIAN_POINT('Ctrl Pts',(-2.34739252847471,0.403406675792388,
49.6189211885841));
#94505=CARTESIAN_POINT('Ctrl Pts',(-2.34668236863849,0.343918483395766,
49.62825));
#94506=CARTESIAN_POINT('',(-2.14330812717712,2.01108871876559,49.058));
#94507=CARTESIAN_POINT('Origin',(0.,0.,49.058));
#94508=CARTESIAN_POINT('Ctrl Pts',(-2.86966548199755,0.0016690505250476,
49.1339652973708));
#94509=CARTESIAN_POINT('Ctrl Pts',(-2.87368608546791,0.0967543767551498,
49.1306062245523));
#94510=CARTESIAN_POINT('Ctrl Pts',(-2.87273263089904,0.191749483183767,
49.1272599768048));
#94511=CARTESIAN_POINT('Ctrl Pts',(-2.86665574610838,0.286315728950319,
49.12392236081));
#94512=CARTESIAN_POINT('Ctrl Pts',(-2.86052341350175,0.381744833232796,
49.1205542911331));
#94513=CARTESIAN_POINT('Ctrl Pts',(-2.84917446165842,0.476738011679848,
49.1171950114464));
#94514=CARTESIAN_POINT('Ctrl Pts',(-2.83288404805877,0.57100164318236,49.1138402125967));
#94515=CARTESIAN_POINT('Ctrl Pts',(-2.81628545073246,0.667048563799475,
49.110421947316));
#94516=CARTESIAN_POINT('Ctrl Pts',(-2.79455638587865,0.762338849772889,
49.1070083340138));
#94517=CARTESIAN_POINT('Ctrl Pts',(-2.76793357574644,0.85655626228785,49.1035948143183));
#94518=CARTESIAN_POINT('Ctrl Pts',(-2.75923473119273,0.887341240344261,
49.1024794671004));
#94519=CARTESIAN_POINT('Ctrl Pts',(-2.75001301471277,0.918011581896025,
49.1013641298762));
#94520=CARTESIAN_POINT('Ctrl Pts',(-2.74027553745566,0.948555907391574,
49.1002486436324));
#94521=CARTESIAN_POINT('Ctrl Pts',(-2.73372252544349,0.969111265477753,
49.0994979569236));
#94522=CARTESIAN_POINT('Ctrl Pts',(-2.72693592120902,0.989609548497314,
49.0987472027259));
#94523=CARTESIAN_POINT('Ctrl Pts',(-2.71991775760214,1.01004722720839,49.0979963325757));
#94524=CARTESIAN_POINT('Ctrl Pts',(-2.71424481770592,1.0265674637604,49.0973893873019));
#94525=CARTESIAN_POINT('Ctrl Pts',(-2.70841986421024,1.0430497756366,49.0967823033947));
#94526=CARTESIAN_POINT('Ctrl Pts',(-2.70245178824862,1.05947149606707,49.0961758256804));
#94527=CARTESIAN_POINT('Ctrl Pts',(-2.66875576630627,1.15218925896325,49.0927516255701));
#94528=CARTESIAN_POINT('Ctrl Pts',(-2.6304519663529,1.24312504392082,49.0893412796056));
#94529=CARTESIAN_POINT('Ctrl Pts',(-2.58783597912855,1.33197382727985,49.085940362308));
#94530=CARTESIAN_POINT('Ctrl Pts',(-2.5446561368894,1.42199817491223,49.0824944472432));
#94531=CARTESIAN_POINT('Ctrl Pts',(-2.49704886581761,1.50988075199989,49.0790582119988));
#94532=CARTESIAN_POINT('Ctrl Pts',(-2.44526848354104,1.59529347018132,49.0756270531001));
#94533=CARTESIAN_POINT('Ctrl Pts',(-2.39355330634354,1.68059863135375,49.0722002149301));
#94534=CARTESIAN_POINT('Ctrl Pts',(-2.33767502868706,1.76344096821467,49.0687784403291));
#94535=CARTESIAN_POINT('Ctrl Pts',(-2.27784106807338,1.84347061755202,49.0653571431915));
#94536=CARTESIAN_POINT('Ctrl Pts',(-2.23495772093708,1.90082833210961,49.0629050796593));
#94537=CARTESIAN_POINT('Ctrl Pts',(-2.19004149603404,1.95674081908624,49.0604532613844));
#94538=CARTESIAN_POINT('Ctrl Pts',(-2.14315631774277,2.01106840053253,49.058));
#94539=CARTESIAN_POINT('',(-2.,-2.44929359829471E-16,50.));
#94540=CARTESIAN_POINT('',(-2.5,-3.06161699786838E-16,49.5));
#94541=CARTESIAN_POINT('Origin',(0.,0.,50.));
#94542=CARTESIAN_POINT('Ctrl Pts',(1.70810875200399,-2.39535560853235,-0.329233991005384));
#94543=CARTESIAN_POINT('Ctrl Pts',(2.50610891073096,-1.82630813584529,-0.276212356389999));
#94544=CARTESIAN_POINT('Ctrl Pts',(3.47463875979381,0.16229507325623,-0.17016908715923));
#94545=CARTESIAN_POINT('Ctrl Pts',(1.73917099852795,3.01633623709207,-0.0111041833130765));
#94546=CARTESIAN_POINT('Ctrl Pts',(-1.59514451425713,3.09116303725476,0.147960720533078));
#94547=CARTESIAN_POINT('Ctrl Pts',(-3.46361225058625,0.331379558630963,
0.307025624379232));
#94548=CARTESIAN_POINT('Ctrl Pts',(-2.15136645360759,-2.7350655110993,0.466090528225386));
#94549=CARTESIAN_POINT('Ctrl Pts',(1.137007233108,-3.28830020261314,0.62515543207154));
#94550=CARTESIAN_POINT('Ctrl Pts',(3.38098902036554,-0.822049678815183,
0.784220335917693));
#94551=CARTESIAN_POINT('Ctrl Pts',(2.51978384323507,2.39953860437162,0.943285239763849));
#94552=CARTESIAN_POINT('Ctrl Pts',(-0.655731952682091,3.41711250332626,
1.10235014361));
#94553=CARTESIAN_POINT('Ctrl Pts',(-3.22897844832054,1.2963528837586,1.26141504745616));
#94554=CARTESIAN_POINT('Ctrl Pts',(-2.83659947794847,-2.01508134321981,
1.42047995130231));
#94555=CARTESIAN_POINT('Ctrl Pts',(0.16104030048805,-3.47575223487759,1.57954485514846));
#94556=CARTESIAN_POINT('Ctrl Pts',(3.01077127957883,-1.74415432954563,1.73860975899462));
#94557=CARTESIAN_POINT('Ctrl Pts',(3.09528030412668,1.5893576043674,1.89767466284077));
#94558=CARTESIAN_POINT('Ctrl Pts',(0.336948704848476,3.46313082488865,2.05673956668693));
#94559=CARTESIAN_POINT('Ctrl Pts',(-2.73085088642586,2.15621606241621,2.21580447053308));
#94560=CARTESIAN_POINT('Ctrl Pts',(-3.29051850755748,-1.13106224326845,
2.37486937437924));
#94561=CARTESIAN_POINT('Ctrl Pts',(-0.828030814474741,-3.37952330330655,
2.53393427822538));
#94562=CARTESIAN_POINT('Ctrl Pts',(2.39495631940617,-2.52408354317363,2.69299918207155));
#94563=CARTESIAN_POINT('Ctrl Pts',(3.41831149878882,0.649584395119446,2.85206408591769));
#94564=CARTESIAN_POINT('Ctrl Pts',(1.30214080720984,3.22664571586789,3.01112898976385));
#94565=CARTESIAN_POINT('Ctrl Pts',(-2.00997259209927,2.84021540432072,3.17019389361));
#94566=CARTESIAN_POINT('Ctrl Pts',(-3.4760398031417,-0.154792205052638,
3.32925879745616));
#94567=CARTESIAN_POINT('Ctrl Pts',(-1.74956097100319,-3.00763191447529,
3.48832370130231));
#94568=CARTESIAN_POINT('Ctrl Pts',(1.583790700515,-3.09813175262809,3.64738860514846));
#94569=CARTESIAN_POINT('Ctrl Pts',(3.46252015378254,-0.343172725955958,
3.80645350899462));
#94570=CARTESIAN_POINT('Ctrl Pts',(2.16112059915153,2.72697104667658,3.96551841284077));
#94571=CARTESIAN_POINT('Ctrl Pts',(-1.12514604666361,3.29254608310422,4.12458331668693));
#94572=CARTESIAN_POINT('Ctrl Pts',(-3.37802965884603,0.83410368592,4.28364822053308));
#94573=CARTESIAN_POINT('Ctrl Pts',(-2.52838400629955,-2.39041579049229,
4.44271312437924));
#94574=CARTESIAN_POINT('Ctrl Pts',(0.643439413780638,-3.41947350565055,
4.60177802822539));
#94575=CARTESIAN_POINT('Ctrl Pts',(3.22430010917227,-1.3079381257977,4.76084293207155));
#94576=CARTESIAN_POINT('Ctrl Pts',(2.84382344014261,2.00486447826478,4.9199078359177));
#94577=CARTESIAN_POINT('Ctrl Pts',(-0.148544283050351,3.47631240410399,
5.07897273976384));
#94578=CARTESIAN_POINT('Ctrl Pts',(-3.00448248021664,1.75496392014332,5.23803764361001));
#94579=CARTESIAN_POINT('Ctrl Pts',(-3.10097337776917,-1.57821970755046,
5.39710254745616));
#94580=CARTESIAN_POINT('Ctrl Pts',(-0.349395541421692,-3.46189775853851,
5.55616745130231));
#94581=CARTESIAN_POINT('Ctrl Pts',(2.7230823466392,-2.16601843675395,5.71523235514847));
#94582=CARTESIAN_POINT('Ctrl Pts',(3.29456304881679,1.11922636330076,5.87429725899461));
#94583=CARTESIAN_POINT('Ctrl Pts',(0.840173848831963,3.3765250241448,6.03336216284078));
#94584=CARTESIAN_POINT('Ctrl Pts',(-2.38586753206279,2.53267634220902,6.19242706668693));
#94585=CARTESIAN_POINT('Ctrl Pts',(-3.42062446981773,-0.6372923751473,6.35149197053308));
#94586=CARTESIAN_POINT('Ctrl Pts',(-1.31373121710534,-3.2219440752657,6.51055687437924));
#94587=CARTESIAN_POINT('Ctrl Pts',(1.99974988670252,-2.84742229491342,6.66962177822538));
#94588=CARTESIAN_POINT('Ctrl Pts',(3.47657377546659,0.142295884250894,6.82868668207155));
#94589=CARTESIAN_POINT('Ctrl Pts',(1.76036119961975,3.00132333843091,6.98775158591769));
#94590=CARTESIAN_POINT('Ctrl Pts',(-1.57264361602868,3.10380498612606,7.14681648976386));
#94591=CARTESIAN_POINT('Ctrl Pts',(-3.46126417978726,0.35561722772998,7.30588139361));
#94592=CARTESIAN_POINT('Ctrl Pts',(-2.17090927703816,-2.71918484951032,
7.46494629745616));
#94593=CARTESIAN_POINT('Ctrl Pts',(1.11330306427908,-3.29656937163524,7.62401120130232));
#94594=CARTESIAN_POINT('Ctrl Pts',(3.37500948166289,-0.846241297516434,
7.78307610514846));
#94595=CARTESIAN_POINT('Ctrl Pts',(2.53696049635548,2.38131156610565,7.94214100899463));
#94596=CARTESIAN_POINT('Ctrl Pts',(-0.63114327775138,3.42176438374795,8.10120591284077));
#94597=CARTESIAN_POINT('Ctrl Pts',(-3.2195776329391,1.31952006442305,8.26027081668694));
#94598=CARTESIAN_POINT('Ctrl Pts',(-2.8510119511463,-1.99462883498604,8.41933572053308));
#94599=CARTESIAN_POINT('Ctrl Pts',(0.13604702576719,-3.47682391583421,8.57840062437923));
#94600=CARTESIAN_POINT('Ctrl Pts',(2.99815450093433,-1.76575279228548,8.73746552822539));
#94601=CARTESIAN_POINT('Ctrl Pts',(3.10662656770694,1.5670624441145,8.89653043207155));
#94602=CARTESIAN_POINT('Ctrl Pts',(0.361837765224454,3.46061941949619,9.0555953359177));
#94603=CARTESIAN_POINT('Ctrl Pts',(-2.71527856811274,2.17579310424599,9.21466023976385));
#94604=CARTESIAN_POINT('Ctrl Pts',(-3.29856504495654,-1.10737616875548,
9.37372514361001));
#94605=CARTESIAN_POINT('Ctrl Pts',(-0.852306012436442,-3.37348303628481,
9.53279004745616));
#94606=CARTESIAN_POINT('Ctrl Pts',(2.37674790737222,-2.54123645490509,9.69185495130231));
#94607=CARTESIAN_POINT('Ctrl Pts',(3.42289324374123,0.624992141460518,9.85091985514848));
#94608=CARTESIAN_POINT('Ctrl Pts',(1.32530464905932,3.21720078983556,10.0099847589946));
#94609=CARTESIAN_POINT('Ctrl Pts',(-1.98950133966361,2.85459239724579,10.1690496628408));
#94610=CARTESIAN_POINT('Ctrl Pts',(-3.47706282439622,-0.129797727786466,
10.3281145666869));
#94611=CARTESIAN_POINT('Ctrl Pts',(-1.77113868072445,-2.99497597796349,
10.4871794705331));
#94612=CARTESIAN_POINT('Ctrl Pts',(1.56147620983851,-3.10943811339688,10.6462443743792));
#94613=CARTESIAN_POINT('Ctrl Pts',(3.45996347974781,-0.368057133809716,
10.8053092782254));
#94614=CARTESIAN_POINT('Ctrl Pts',(2.18066990260054,2.71136351506559,10.9643741820716));
#94615=CARTESIAN_POINT('Ctrl Pts',(-1.10144569587676,3.30055006233375,11.1234390859177));
#94616=CARTESIAN_POINT('Ctrl Pts',(-3.37194569294167,0.858367974000013,
11.2825039897639));
#94617=CARTESIAN_POINT('Ctrl Pts',(-2.54550420404445,-2.37217657060532,
11.44156889361));
#94618=CARTESIAN_POINT('Ctrl Pts',(0.618838986145877,-3.42401104615079,
11.6006337974562));
#94619=CARTESIAN_POINT('Ctrl Pts',(3.21481355363338,-1.33108495232717,11.7596987013023));
#94620=CARTESIAN_POINT('Ctrl Pts',(2.85816362164538,1.98436741729946,11.9187636051485));
#94621=CARTESIAN_POINT('Ctrl Pts',(-0.123548010496914,3.47729050038087,
12.0778285089946));
#94622=CARTESIAN_POINT('Ctrl Pts',(-2.99178777978657,1.77651884753764,12.2368934128408));
#94623=CARTESIAN_POINT('Ctrl Pts',(-3.11223961411324,-1.55588493124686,
12.3959583166869));
#94624=CARTESIAN_POINT('Ctrl Pts',(-0.37427531339427,-3.45929636266111,
12.5550232205331));
#94625=CARTESIAN_POINT('Ctrl Pts',(2.70743970301638,-2.18553965634745,12.7140881243793));
#94626=CARTESIAN_POINT('Ctrl Pts',(3.30252441735429,1.09551166480118,12.8731530282254));
#94627=CARTESIAN_POINT('Ctrl Pts',(0.864427162624142,3.37039745659979,13.0322179320716));
#94628=CARTESIAN_POINT('Ctrl Pts',(-2.36759757057254,2.54976372998672,13.1912828359177));
#94629=CARTESIAN_POINT('Ctrl Pts',(-3.42511778736563,-0.612683831685064,
13.3503477397639));
#94630=CARTESIAN_POINT('Ctrl Pts',(-1.33686095555343,-3.21241593204452,
13.50941264361));
#94631=CARTESIAN_POINT('Ctrl Pts',(1.97922708447866,-2.86172561280827,13.6684775474562));
#94632=CARTESIAN_POINT('Ctrl Pts',(3.47750694305263,0.117297894088165,13.8275424513023));
#94633=CARTESIAN_POINT('Ctrl Pts',(1.78189327534454,2.98858991670296,13.9866073551485));
#94634=CARTESIAN_POINT('Ctrl Pts',(-1.55028862640208,3.11503106080583,14.1456722589946));
#94635=CARTESIAN_POINT('Ctrl Pts',(-3.45861807039121,0.380492283890413,
14.3047371628408));
#94636=CARTESIAN_POINT('Ctrl Pts',(-2.19040234975507,-2.70350714464087,
14.4638020666869));
#94637=CARTESIAN_POINT('Ctrl Pts',(1.0895740946985,-3.30448810364006,14.6228669705331));
#94638=CARTESIAN_POINT('Ctrl Pts',(3.36883833226074,-0.870483558734738,
14.7819318743792));
#94639=CARTESIAN_POINT('Ctrl Pts',(2.55401501897158,2.36301092206625,14.9409967782254));
#94640=CARTESIAN_POINT('Ctrl Pts',(-0.606526697962181,3.42621346381042,
15.1000616820716));
#94641=CARTESIAN_POINT('Ctrl Pts',(-3.21000793281444,1.34263264007885,15.2591265859177));
#94642=CARTESIAN_POINT('Ctrl Pts',(-2.86527835922753,-1.97408035780693,
15.4181914897639));
#94643=CARTESIAN_POINT('Ctrl Pts',(0.11104739875106,-3.4777121517123,15.57725639361));
#94644=CARTESIAN_POINT('Ctrl Pts',(2.9853823990433,-1.78726194678318,15.7363212974562));
#94645=CARTESIAN_POINT('Ctrl Pts',(3.11781244445693,1.54468731338294,15.8953862013023));
#94646=CARTESIAN_POINT('Ctrl Pts',(0.386708025214324,3.45792860512932,16.0544511051485));
#94647=CARTESIAN_POINT('Ctrl Pts',(-2.69956585264314,2.19525796711455,16.2135160089946));
#94648=CARTESIAN_POINT('Ctrl Pts',(-3.30644111484741,-1.08363300474993,
16.3725809128408));
#94649=CARTESIAN_POINT('Ctrl Pts',(-0.876537142766755,-3.3672683249612,
16.5316458166869));
#94650=CARTESIAN_POINT('Ctrl Pts',(2.35841663990349,-2.55825805726535,16.6907107205331));
#94651=CARTESIAN_POINT('Ctrl Pts',(3.42729807194563,0.600367604867713,16.8497756243792));
#94652=CARTESIAN_POINT('Ctrl Pts',(1.34839998725813,3.20758956372211,17.0088405282254));
#94653=CARTESIAN_POINT('Ctrl Pts',(-1.96892725391064,2.8688218494261,17.1679054320716));
#94654=CARTESIAN_POINT('Ctrl Pts',(-3.47790612569696,-0.104796544677688,
17.3269703359177));
#94655=CARTESIAN_POINT('Ctrl Pts',(-1.79262484451019,-2.98216523716939,
17.4860352397639));
#94656=CARTESIAN_POINT('Ctrl Pts',(1.53908101028433,-3.12058375608137,17.64510014361));
#94657=CARTESIAN_POINT('Ctrl Pts',(3.45722796910274,-0.392922517286194,
17.8041650474562));
#94658=CARTESIAN_POINT('Ctrl Pts',(2.20010649273994,2.69561583975543,17.9632299513023));
#94659=CARTESIAN_POINT('Ctrl Pts',(-1.077688414148,3.30838344466717,18.1222948551485));
#94660=CARTESIAN_POINT('Ctrl Pts',(-3.36568743977307,0.882587895164228,
18.2813597589946));
#94661=CARTESIAN_POINT('Ctrl Pts',(-2.56249283116099,-2.35381473892603,
18.4404246628408));
#94662=CARTESIAN_POINT('Ctrl Pts',(0.594206572298488,-3.42837160826742,
18.599489566687));
#94663=CARTESIAN_POINT('Ctrl Pts',(3.20516083258003,-1.35416297845998,18.7585544705331));
#94664=CARTESIAN_POINT('Ctrl Pts',(2.8723560719568,1.96376778943683,18.9176193743793));
#94665=CARTESIAN_POINT('Ctrl Pts',(-0.0985453520613107,3.47808886437995,
19.0766842782254));
#94666=CARTESIAN_POINT('Ctrl Pts',(-2.97893844147421,1.79798195120084,19.2357491820716));
#94667=CARTESIAN_POINT('Ctrl Pts',(-3.12334498672647,-1.53346973521728,
19.3948140859177));
#94668=CARTESIAN_POINT('Ctrl Pts',(-0.399135740030314,-3.45651616457484,
19.5538789897639));
#94669=CARTESIAN_POINT('Ctrl Pts',(2.69165711873815,-2.20494791096822,19.71294389361));
#94670=CARTESIAN_POINT('Ctrl Pts',(3.31031508682473,1.07174034209662,19.8720087974562));
#94671=CARTESIAN_POINT('Ctrl Pts',(0.888635796380244,3.36409568180341,20.0310737013023));
#94672=CARTESIAN_POINT('Ctrl Pts',(-2.34920523400022,2.56671932697806,20.1901386051485));
#94673=CARTESIAN_POINT('Ctrl Pts',(-3.42943406930774,-0.588043620157575,
20.3492035089946));
#94674=CARTESIAN_POINT('Ctrl Pts',(-1.3599215950672,-3.20272174723417,20.5082684128408));
#94675=CARTESIAN_POINT('Ctrl Pts',(1.95860198105303,-2.87588101540241,20.6673333166869));
#94676=CARTESIAN_POINT('Ctrl Pts',(3.47826036717098,0.0922938410963431,
20.8263982205331));
#94677=CARTESIAN_POINT('Ctrl Pts',(1.80333324954904,2.97570202238189,20.9854631243793));
#94678=CARTESIAN_POINT('Ctrl Pts',(-1.52785350630899,3.1260961274721,21.1445280282254));
#94679=CARTESIAN_POINT('Ctrl Pts',(-3.45579319384513,0.405347673374805,
21.3035929320716));
#94680=CARTESIAN_POINT('Ctrl Pts',(-2.20978220615917,-2.68768970237991,
21.4626578359177));
#94681=CARTESIAN_POINT('Ctrl Pts',(1.06578880781087,-3.3122360350799,21.6217227397639));
#94682=CARTESIAN_POINT('Ctrl Pts',(3.36249305619432,-0.894680826877306,
21.78078764361));
#94683=CARTESIAN_POINT('Ctrl Pts',(2.57093753106305,2.34458814001697,21.9398525474562));
#94684=CARTESIAN_POINT('Ctrl Pts',(-0.581878768354349,3.43048545163438,
22.0989174513023));
#94685=CARTESIAN_POINT('Ctrl Pts',(-3.20027231556393,1.36567581847664,22.2579823551485));
#94686=CARTESIAN_POINT('Ctrl Pts',(-2.87939666837566,-1.95342984544721,
22.4170472589946));
#94687=CARTESIAN_POINT('Ctrl Pts',(0.0860420319779839,-3.47842063351599,
22.5761121628408));
#94688=CARTESIAN_POINT('Ctrl Pts',(2.97245599034753,-1.80867872226767,22.735177066687));
#94689=CARTESIAN_POINT('Ctrl Pts',(3.12883716943083,1.52223234170245,22.8942419705331));
#94690=CARTESIAN_POINT('Ctrl Pts',(0.411558297252309,3.45505905924915,23.0533068743793));
#94691=CARTESIAN_POINT('Ctrl Pts',(-2.68371360349739,2.21460936269578,23.2123717782254));
#94692=CARTESIAN_POINT('Ctrl Pts',(-3.3141462832271,-1.05983383051717,23.3714366820716));
#94693=CARTESIAN_POINT('Ctrl Pts',(-0.90072296712697,-3.36087956812301,
23.5305015859177));
#94694=CARTESIAN_POINT('Ctrl Pts',(2.33996347189163,-2.57514742978914,23.6895664897639));
#94695=CARTESIAN_POINT('Ctrl Pts',(3.43152575185086,0.575712036804067,23.84863139361));
#94696=CARTESIAN_POINT('Ctrl Pts',(1.3714256300995,3.19781254548213,24.0076962974562));
#94697=CARTESIAN_POINT('Ctrl Pts',(-1.9482513993279,2.88290301951934,24.1667612013023));
#94698=CARTESIAN_POINT('Ctrl Pts',(-3.47856966289727,-0.0797899449027475,
24.3258261051485));
#94699=CARTESIAN_POINT('Ctrl Pts',(-1.81401835208813,-2.96920035585748,
24.4848910089946));
#94700=CARTESIAN_POINT('Ctrl Pts',(1.51660625955678,-3.13156810374769,24.6439559128408));
#94701=CARTESIAN_POINT('Ctrl Pts',(3.45431376315845,-0.417767591599538,
24.8030208166869));
#94702=CARTESIAN_POINT('Ctrl Pts',(2.21942936498409,2.67972883493518,24.9620857205332));
#94703=CARTESIAN_POINT('Ctrl Pts',(-1.05387542945276,3.31604582509538,25.1211506243792));
#94704=CARTESIAN_POINT('Ctrl Pts',(-3.35925522280188,0.906762197610325,
25.2802155282254));
#94705=CARTESIAN_POINT('Ctrl Pts',(-2.5793490095563,-2.3353312445642,25.4392804320715));
#94706=CARTESIAN_POINT('Ctrl Pts',(0.569543445428409,-3.43255496659649,
25.5983453359177));
#94707=CARTESIAN_POINT('Ctrl Pts',(3.19534244493507,-1.37717101136099,25.7574102397639));
#94708=CARTESIAN_POINT('Ctrl Pts',(2.88640005750619,1.94306665942397,25.91647514361));
#94709=CARTESIAN_POINT('Ctrl Pts',(-0.073537600067748,3.47870745483333,
26.0755400474562));
#94710=CARTESIAN_POINT('Ctrl Pts',(-2.96593512942888,1.81935212176105,26.2346049513023));
#94711=CARTESIAN_POINT('Ctrl Pts',(-3.13428892160056,-1.51097527804684,
26.3936698551485));
#94712=CARTESIAN_POINT('Ctrl Pts',(-0.42397553635747,-3.45355730798075,
26.5527347589946));
#94713=CARTESIAN_POINT('Ctrl Pts',(2.67573540956612,-2.22424219745308,26.7117996628408));
#94714=CARTESIAN_POINT('Ctrl Pts',(3.31793465454823,1.04791362386632,26.870864566687));
#94715=CARTESIAN_POINT('Ctrl Pts',(0.912798498817672,3.3576200254783,27.0299294705331));
#94716=CARTESIAN_POINT('Ctrl Pts',(-2.33069147299888,2.58354225679144,27.1889943743792));
#94717=CARTESIAN_POINT('Ctrl Pts',(-3.43357309254645,-0.563373014154682,
27.3480592782254));
#94718=CARTESIAN_POINT('Ctrl Pts',(-1.38291194370096,-3.19286202190228,
27.5071241820715));
#94719=CARTESIAN_POINT('Ctrl Pts',(1.93787564248457,-2.88988777103919,27.6661890859177));
#94720=CARTESIAN_POINT('Ctrl Pts',(3.4788340088791,0.0672850176711449,27.8252539897639));
#94721=CARTESIAN_POINT('Ctrl Pts',(1.82468001405561,2.96266032161008,27.98431889361));
#94722=CARTESIAN_POINT('Ctrl Pts',(-1.50533941536355,3.13699961419979,28.1433837974562));
#94723=CARTESIAN_POINT('Ctrl Pts',(-3.45278969615972,0.430182111471415,
28.3024487013023));
#94724=CARTESIAN_POINT('Ctrl Pts',(-2.22904784455505,-2.67173334029076,
28.4615136051485));
#94725=CARTESIAN_POINT('Ctrl Pts',(1.04194843301715,-3.3198127654839,28.6205785089947));
#94726=CARTESIAN_POINT('Ctrl Pts',(3.35597398143476,-0.918831851248986,
28.7796434128408));
#94727=CARTESIAN_POINT('Ctrl Pts',(2.58772715794839,2.32604417218444,28.9387083166869));
#94728=CARTESIAN_POINT('Ctrl Pts',(-0.557200762916511,3.43458012641168,
29.0977732205331));
#94729=CARTESIAN_POINT('Ctrl Pts',(-3.19037128439679,1.38864840857327,29.2568381243793));
#94730=CARTESIAN_POINT('Ctrl Pts',(-2.89336614885126,-1.93267836527921,
29.4159030282254));
#94731=CARTESIAN_POINT('Ctrl Pts',(0.061032217911679,-3.47894932462569,
29.5749679320716));
#94732=CARTESIAN_POINT('Ctrl Pts',(2.95937594298018,-1.83000201176034,29.7340328359177));
#94733=CARTESIAN_POINT('Ctrl Pts',(3.13970017278865,1.49969868971325,29.8930977397638));
#94734=CARTESIAN_POINT('Ctrl Pts',(0.436387296891261,3.45201093017516,30.0521626436101));
#94735=CARTESIAN_POINT('Ctrl Pts',(-2.66772264003783,2.23384629076543,30.2112275474561));
#94736=CARTESIAN_POINT('Ctrl Pts',(-3.32168015183512,-1.03597987617585,
30.3702924513024));
#94737=CARTESIAN_POINT('Ctrl Pts',(-0.924862235413484,-3.35431709598879,
30.5293573551484));
#94738=CARTESIAN_POINT('Ctrl Pts',(2.32138935713386,-2.59190369950783,30.6884222589947));
#94739=CARTESIAN_POINT('Ctrl Pts',(3.43557606493896,0.551026711653098,30.8474871628408));
#94740=CARTESIAN_POINT('Ctrl Pts',(1.39438038744657,3.1878702404648,31.0065520666869));
#94741=CARTESIAN_POINT('Ctrl Pts',(-1.92747484459752,2.89683517970569,31.1656169705331));
#94742=CARTESIAN_POINT('Ctrl Pts',(-3.47905340170063,-0.0547792209889362,
31.3246818743793));
#94743=CARTESIAN_POINT('Ctrl Pts',(-1.83531809768251,-2.95608200414939,
31.4837467782254));
#94744=CARTESIAN_POINT('Ctrl Pts',(1.49405311931838,-3.14239058864294,31.6428116820716));
#94745=CARTESIAN_POINT('Ctrl Pts',(3.45122101254281,-0.442591072571193,
31.8018765859177));
#94746=CARTESIAN_POINT('Ctrl Pts',(2.23863752058297,2.66370332176368,31.9609414897639));
#94747=CARTESIAN_POINT('Ctrl Pts',(-1.03000797262355,3.32353680756941,32.12000639361));
#94748=CARTESIAN_POINT('Ctrl Pts',(-3.35264937449288,0.930889631830323,
32.2790712974562));
#94749=CARTESIAN_POINT('Ctrl Pts',(-2.59607186797765,-2.31672704288437,
32.4381362013023));
#94750=CARTESIAN_POINT('Ctrl Pts',(0.544850880309637,-3.436560904911,32.5972011051485));
#94751=CARTESIAN_POINT('Ctrl Pts',(3.18535889818595,-1.40010786180367,32.7562660089947));
#94752=CARTESIAN_POINT('Ctrl Pts',(2.90029485239572,1.9222650972495,32.9153309128408));
#94753=CARTESIAN_POINT('Ctrl Pts',(-0.0485260471031247,3.47914623976763,
33.074395816687));
#94754=CARTESIAN_POINT('Ctrl Pts',(-2.95277851575862,1.84062825464868,33.2334607205331));
#94755=CARTESIAN_POINT('Ctrl Pts',(-3.14507085307143,-1.48840272241665,
33.3925256243793));
#94756=CARTESIAN_POINT('Ctrl Pts',(-0.44879341847017,-3.45041994581451,
33.5515905282254));
#94757=CARTESIAN_POINT('Ctrl Pts',(2.65967539845273,-2.24342151852971,33.7106554320715));
#94758=CARTESIAN_POINT('Ctrl Pts',(3.32538272668884,1.0240327416525,33.8697203359177));
#94759=CARTESIAN_POINT('Ctrl Pts',(0.936914021027954,3.35097082233462,34.0287852397639));
#94760=CARTESIAN_POINT('Ctrl Pts',(-2.31205724449761,2.60023164989254,34.18785014361));
#94761=CARTESIAN_POINT('Ctrl Pts',(-3.43753464314619,-0.538673288837053,
34.3469150474562));
#94762=CARTESIAN_POINT('Ctrl Pts',(-1.40583081314219,-3.18283726567299,
34.5059799513024));
#94763=CARTESIAN_POINT('Ctrl Pts',(1.91704914006494,-2.90374515574508,34.6650448551485));
#94764=CARTESIAN_POINT('Ctrl Pts',(3.47922783852685,0.0422727164548873,
34.8241097589947));
#94765=CARTESIAN_POINT('Ctrl Pts',(1.84593246550451,2.94946548847979,34.9831746628408));
#94766=CARTESIAN_POINT('Ctrl Pts',(-1.4827475172617,3.14774095741551,35.142239566687));
#94767=CARTESIAN_POINT('Ctrl Pts',(-3.44960773257809,0.454994314551468,
35.3013044705331));
#94768=CARTESIAN_POINT('Ctrl Pts',(-2.24819826915098,-2.65563888311707,
35.4603693743793));
#94769=CARTESIAN_POINT('Ctrl Pts',(1.01805420256545,-3.3272179032302,35.6194342782254));
#94770=CARTESIAN_POINT('Ctrl Pts',(3.34928144493648,-0.942935383544889,
35.7784991820716));
#94771=CARTESIAN_POINT('Ctrl Pts',(2.60438303181454,2.30737997705909,35.9375640859177));
#94772=CARTESIAN_POINT('Ctrl Pts',(-0.532493957191848,3.438497276499,36.0966289897639));
#94773=CARTESIAN_POINT('Ctrl Pts',(-3.1803053510721,1.41154922297418,36.25569389361));
#94774=CARTESIAN_POINT('Ctrl Pts',(-2.90718607860752,-1.91182698989406,
36.4147587974562));
#94775=CARTESIAN_POINT('Ctrl Pts',(0.0360192492456371,-3.47929819771466,
36.5738237013024));
#94776=CARTESIAN_POINT('Ctrl Pts',(2.94614293301552,-1.85123071311478,36.7328886051485));
#94777=CARTESIAN_POINT('Ctrl Pts',(3.15040089304948,1.47708752212243,36.8919535089947));
#94778=CARTESIAN_POINT('Ctrl Pts',(0.461193740783423,3.44878437545738,37.0510184128408));
#94779=CARTESIAN_POINT('Ctrl Pts',(-2.65159378879653,2.2529677570157,37.210083316687));
#94780=CARTESIAN_POINT('Ctrl Pts',(-3.32904233126504,-1.01207237467599,
37.3691482205331));
#94781=CARTESIAN_POINT('Ctrl Pts',(-0.948953699929094,-3.34758124775602,
37.5282131243792));
#94782=CARTESIAN_POINT('Ctrl Pts',(2.3026952556788,-2.60852600033258,37.6872780282255));
#94783=CARTESIAN_POINT('Ctrl Pts',(3.43944880185957,0.526312905336293,37.8463429320715));
#94784=CARTESIAN_POINT('Ctrl Pts',(1.4172630728265,3.17776316256248,38.0054078359178));
#94785=CARTESIAN_POINT('Ctrl Pts',(-1.90659866360674,2.91061760986732,38.1644727397638));
#94786=CARTESIAN_POINT('Ctrl Pts',(-3.47935731710377,-0.029765665676874,
38.32353764361));
#94787=CARTESIAN_POINT('Ctrl Pts',(-1.85652298036374,-2.94281086009925,
38.4826025474562));
#94788=CARTESIAN_POINT('Ctrl Pts',(1.47142275528341,-3.15305065138051,38.6416674513023));
#94789=CARTESIAN_POINT('Ctrl Pts',(3.44794987711221,-0.467391677138788,
38.8007323551485));
#94790=CARTESIAN_POINT('Ctrl Pts',(2.25772996671604,2.6475401285588,38.9597972589946));
#94791=CARTESIAN_POINT('Ctrl Pts',(-1.00608727730826,3.33085600489952,39.1188621628408));
#94792=CARTESIAN_POINT('Ctrl Pts',(-3.3458702362856,0.954968950738659,39.277927066687));
#94793=CARTESIAN_POINT('Ctrl Pts',(-2.61266054206305,-2.29800309549042,
39.4369919705331));
#94794=CARTESIAN_POINT('Ctrl Pts',(0.520130153238007,-3.44038921615408,
39.5960568743793));
#94795=CARTESIAN_POINT('Ctrl Pts',(3.1752107083567,-1.42297234424072,39.7551217782254));
#94796=CARTESIAN_POINT('Ctrl Pts',(2.91403973843892,1.90136417809308,39.9141866820716));
#94797=CARTESIAN_POINT('Ctrl Pts',(-0.023511985950815,3.47940519650318,
40.0732515859177));
#94798=CARTESIAN_POINT('Ctrl Pts',(-2.93946928049521,1.86180925015472,40.2323164897639));
#94799=CARTESIAN_POINT('Ctrl Pts',(-3.15569022384854,-1.46575323504451,
40.39138139361));
#94800=CARTESIAN_POINT('Ctrl Pts',(-0.473588103595339,-3.44710424023842,
40.5504462974562));
#94801=CARTESIAN_POINT('Ctrl Pts',(2.64347791549904,-2.26248488286786,40.7095112013023));
#94802=CARTESIAN_POINT('Ctrl Pts',(3.33265891827465,1.00009892979701,40.8685761051485));
#94803=CARTESIAN_POINT('Ctrl Pts',(0.960981116541363,3.34414841605268,41.0276410089946));
#94804=CARTESIAN_POINT('Ctrl Pts',(-2.29330351165203,2.61678664364926,41.1867059128408));
#94805=CARTESIAN_POINT('Ctrl Pts',(-3.44131851634454,-0.513945720870379,
41.3457708166869));
#94806=CARTESIAN_POINT('Ctrl Pts',(-1.42867701877307,-3.17264799670034,
41.5048357205332));
#94807=CARTESIAN_POINT('Ctrl Pts',(1.89612355026292,-2.91745245326724,41.6639006243792));
#94808=CARTESIAN_POINT('Ctrl Pts',(3.47944183575824,0.0172582302697266,
41.8229655282254));
#94809=CARTESIAN_POINT('Ctrl Pts',(1.86708950541063,2.93611820499827,41.9820304320716));
#94810=CARTESIAN_POINT('Ctrl Pts',(-1.46007897972099,3.15831960192657,42.1410953359177));
#94811=CARTESIAN_POINT('Ctrl Pts',(-3.44624746756781,0.479783000135612,
42.3001602397639));
#94812=CARTESIAN_POINT('Ctrl Pts',(-2.26723249011047,-2.6394071627402,42.45922514361));
#94813=CARTESIAN_POINT('Ctrl Pts',(0.994107351487493,-3.33445106556614,
42.6182900474562));
#94814=CARTESIAN_POINT('Ctrl Pts',(3.34241579261952,-0.966990177915068,
42.7773549513024));
#94815=CARTESIAN_POINT('Ctrl Pts',(2.620904291762,2.28859651934561,42.9364198551484));
#94816=CARTESIAN_POINT('Ctrl Pts',(-0.507759628212212,3.44223669942876,
43.0954847589948));
#94817=CARTESIAN_POINT('Ctrl Pts',(-3.17007503587205,1.43437707799479,43.2545496628407));
#94818=CARTESIAN_POINT('Ctrl Pts',(-2.92085574332787,-1.89087679704625,
43.4136145666871));
#94819=CARTESIAN_POINT('Ctrl Pts',(0.0110044188368612,-3.47946723475014,
43.572679470533));
#94820=CARTESIAN_POINT('Ctrl Pts',(2.93275764443294,-1.87236372907448,43.7317443743794));
#94821=CARTESIAN_POINT('Ctrl Pts',(3.16093877712245,1.45440000764499,43.8908092782254));
#94822=CARTESIAN_POINT('Ctrl Pts',(0.485976346743174,3.44537956186525,44.0498741820716));
#94823=CARTESIAN_POINT('Ctrl Pts',(-2.63532788342538,2.27197277311243,44.2089390859177));
#94824=CARTESIAN_POINT('Ctrl Pts',(-3.33623244099863,-0.988112561746271,
44.3680039897639));
#94825=CARTESIAN_POINT('Ctrl Pts',(-0.972996115420525,-3.34067237156277,
44.52706889361));
#94826=CARTESIAN_POINT('Ctrl Pts',(2.28388213372536,-2.62501347313853,44.6861337974562));
#94827=CARTESIAN_POINT('Ctrl Pts',(3.44314376253889,0.501571895322309,44.8451987013024));
#94828=CARTESIAN_POINT('Ctrl Pts',(1.44007250330464,3.16749183404082,45.0042636051485));
#94829=CARTESIAN_POINT('Ctrl Pts',(-1.88562393503503,2.92424959789918,45.1633285089947));
#94830=CARTESIAN_POINT('Ctrl Pts',(-3.47948139407905,-0.00475057237518032,
45.3223934128408));
#94831=CARTESIAN_POINT('Ctrl Pts',(-1.87763190280657,-2.92938760866342,
45.481458316687));
#94832=CARTESIAN_POINT('Ctrl Pts',(1.44871633468005,-3.16354774286744,45.6405232205331));
#94833=CARTESIAN_POINT('Ctrl Pts',(3.44450053066955,-0.492168119800616,
45.7995881243793));
#94834=CARTESIAN_POINT('Ctrl Pts',(2.27670570752794,2.63124008384628,45.9586530282254));
#94835=CARTESIAN_POINT('Ctrl Pts',(-0.982114562709173,3.33800305195324,
46.1177179320716));
#94836=CARTESIAN_POINT('Ctrl Pts',(-3.33891819138147,0.978998884598715,
46.2767828359177));
#94837=CARTESIAN_POINT('Ctrl Pts',(-2.62911411180905,-2.27916032222356,
46.4358477397639));
#94838=CARTESIAN_POINT('Ctrl Pts',(0.495382422596211,-3.44403979392057,
46.5949126436101));
#94839=CARTESIAN_POINT('Ctrl Pts',(3.16489862768261,-1.44576310238133,46.7539775474562));
#94840=CARTESIAN_POINT('Ctrl Pts',(2.92763357084724,1.88036464943404,46.9130424513024));
#94841=CARTESIAN_POINT('Ctrl Pts',(0.00150411901917797,3.47948494655473,
47.0721073551485));
#94842=CARTESIAN_POINT('Ctrl Pts',(-2.92600969204226,1.88289280238792,47.2311722589946));
#94843=CARTESIAN_POINT('Ctrl Pts',(-3.1661434702008,-1.44302567639757,47.3902371628409));
#94844=CARTESIAN_POINT('Ctrl Pts',(-0.498364061107948,-3.44361476949528,
47.5493020666869));
#94845=CARTESIAN_POINT('Ctrl Pts',(2.62715476810754,-2.28142289884137,47.7083669705332));
#94846=CARTESIAN_POINT('Ctrl Pts',(3.33974192706535,0.976097389996902,47.8674318743792));
#94847=CARTESIAN_POINT('Ctrl Pts',(0.98503845904953,3.33718374751698,48.0264967782254));
#94848=CARTESIAN_POINT('Ctrl Pts',(-2.27450738921853,2.63314803356416,48.1855616820716));
#94849=CARTESIAN_POINT('Ctrl Pts',(-3.44477925969703,-0.489080282373686,
48.3446265859177));
#94850=CARTESIAN_POINT('Ctrl Pts',(-1.45172651666228,-3.16250708908811,
48.5036914897639));
#94851=CARTESIAN_POINT('Ctrl Pts',(1.87562906970625,-2.930603662586,48.66275639361));
#94852=CARTESIAN_POINT('Ctrl Pts',(3.47846261219738,-0.00853227987589602,
48.8218212974562));
#94853=CARTESIAN_POINT('Ctrl Pts',(1.89011874233621,2.92411545551553,48.9808862013023));
#94854=CARTESIAN_POINT('Ctrl Pts',(-1.44140102367388,3.16572539725362,49.1399511051485));
#94855=CARTESIAN_POINT('Ctrl Pts',(-2.76878294100723,1.39636109408963,49.2459943743793));
#94856=CARTESIAN_POINT('Ctrl Pts',(-2.91090525077888,0.426608275808069,
49.2990160089947));
#94857=CARTESIAN_POINT('Ctrl Pts',(1.59774743137957,-2.24059110187418,-0.219489327336923));
#94858=CARTESIAN_POINT('Ctrl Pts',(2.34418860636375,-1.70830992437181,-0.166467692721538));
#94859=CARTESIAN_POINT('Ctrl Pts',(3.25014150704371,0.151809149222066,-0.0604244234907686));
#94860=CARTESIAN_POINT('Ctrl Pts',(1.6268027386243,2.82145002145618,0.0986404803553848));
#94861=CARTESIAN_POINT('Ctrl Pts',(-1.49208184042344,2.89144224391758,0.25770538420154));
#94862=CARTESIAN_POINT('Ctrl Pts',(-3.23982742326958,0.309969044999859,
0.416770288047693));
#94863=CARTESIAN_POINT('Ctrl Pts',(-2.01236614540808,-2.55835226526823,
0.575835191893847));
#94864=CARTESIAN_POINT('Ctrl Pts',(1.06354492009181,-3.07584232922318,0.73490009574));
#94865=CARTESIAN_POINT('Ctrl Pts',(3.16254249998669,-0.768936849748424,
0.893964999586155));
#94866=CARTESIAN_POINT('Ctrl Pts',(2.35697999816324,2.24450383333788,1.05302990343231));
#94867=CARTESIAN_POINT('Ctrl Pts',(-0.613364952226834,3.19633203595468,
1.21209480727846));
#94868=CARTESIAN_POINT('Ctrl Pts',(-3.02035336785881,1.21259520961831,1.37115971112462));
#94869=CARTESIAN_POINT('Ctrl Pts',(-2.65332609790095,-1.88488644904668,
1.53022461497077));
#94870=CARTESIAN_POINT('Ctrl Pts',(0.150635447626677,-3.25118304023235,
1.68928951881692));
#94871=CARTESIAN_POINT('Ctrl Pts',(2.81624461719718,-1.63146409541665,1.84835442266308));
#94872=CARTESIAN_POINT('Ctrl Pts',(2.89529349317861,1.48666882418481,2.00741932650923));
#94873=CARTESIAN_POINT('Ctrl Pts',(0.315178367329934,3.23937710260303,2.16648423035539));
#94874=CARTESIAN_POINT('Ctrl Pts',(-2.55440994851684,2.01690241981572,2.32554913420154));
#94875=CARTESIAN_POINT('Ctrl Pts',(-3.07791730894721,-1.05798403748725,
2.4846140380477));
#94876=CARTESIAN_POINT('Ctrl Pts',(-0.7745315427828,-3.16117148326227,2.64367894189385));
#94877=CARTESIAN_POINT('Ctrl Pts',(2.2402176109151,-2.36100189344623,2.80274384574));
#94878=CARTESIAN_POINT('Ctrl Pts',(3.19745356402969,0.607614589848881,2.96180874958616));
#94879=CARTESIAN_POINT('Ctrl Pts',(1.21800917393199,3.01817135381553,3.12087365343231));
#94880=CARTESIAN_POINT('Ctrl Pts',(-1.88010777557473,2.65670839839355,3.27993855727847));
#94881=CARTESIAN_POINT('Ctrl Pts',(-3.25145202864119,-0.144791043152296,
3.43900346112461));
#94882=CARTESIAN_POINT('Ctrl Pts',(-1.63652141245871,-2.81330808723417,
3.59806836497077));
#94883=CARTESIAN_POINT('Ctrl Pts',(1.48146159934009,-2.89796070890096,3.75713326881692));
#94884=CARTESIAN_POINT('Ctrl Pts',(3.23880588710515,-0.321000252924548,
3.91619817266308));
#94885=CARTESIAN_POINT('Ctrl Pts',(2.02149007324339,2.55078078615448,4.07526307650923));
#94886=CARTESIAN_POINT('Ctrl Pts',(-1.05245008777951,3.07981388234626,4.23432798035539));
#94887=CARTESIAN_POINT('Ctrl Pts',(-3.15977434353249,0.780212044531519,
4.39339288420154));
#94888=CARTESIAN_POINT('Ctrl Pts',(-2.36502450260688,-2.23597044667527,
4.5524577880477));
#94889=CARTESIAN_POINT('Ctrl Pts',(0.601866637244319,-3.19854049334634,
4.71152269189385));
#94890=CARTESIAN_POINT('Ctrl Pts',(3.01597729733724,-1.22343192636024,4.87058759574001));
#94891=CARTESIAN_POINT('Ctrl Pts',(2.66008331814616,1.87532969821363,5.02965249958615));
#94892=CARTESIAN_POINT('Ctrl Pts',(-0.138946800905478,3.25170701678921,
5.18871740343232));
#94893=CARTESIAN_POINT('Ctrl Pts',(-2.8103621386866,1.64157527574487,5.34778230727846));
#94894=CARTESIAN_POINT('Ctrl Pts',(-2.90061873595268,-1.47625054958176,
5.50684721112463));
#94895=CARTESIAN_POINT('Ctrl Pts',(-0.326821010774226,-3.23822370496875,
5.66591211497077));
#94896=CARTESIAN_POINT('Ctrl Pts',(2.5471433359694,-2.02607146037076,5.82497701881693));
#94897=CARTESIAN_POINT('Ctrl Pts',(3.08170053141509,1.04691287659405,5.98404192266308));
#94898=CARTESIAN_POINT('Ctrl Pts',(0.785890012745933,3.15836692364413,6.14310682650924));
#94899=CARTESIAN_POINT('Ctrl Pts',(-2.23171605232569,2.36903950965249,6.30217173035538));
#94900=CARTESIAN_POINT('Ctrl Pts',(-3.19961709343961,-0.596116760267523,
6.46123663420156));
#94901=CARTESIAN_POINT('Ctrl Pts',(-1.22885072463386,-3.01377348735263,
6.62030153804768));
#94902=CARTESIAN_POINT('Ctrl Pts',(1.87054556165231,-2.66344965003764,6.77936644189386));
#94903=CARTESIAN_POINT('Ctrl Pts',(3.2519515008847,0.133102112667476,6.93843134574));
#94904=CARTESIAN_POINT('Ctrl Pts',(1.64662383568568,2.80740710981763,7.09749624958616));
#94905=CARTESIAN_POINT('Ctrl Pts',(-1.47103473068521,2.90326739340707,7.25656115343231));
#94906=CARTESIAN_POINT('Ctrl Pts',(-3.23763106189424,0.33264071242159,7.41562605727848));
#94907=CARTESIAN_POINT('Ctrl Pts',(-2.03064630227834,-2.54349765707501,
7.57469096112461));
#94908=CARTESIAN_POINT('Ctrl Pts',(1.04137228335836,-3.08357722522978,7.73375586497078));
#94909=CARTESIAN_POINT('Ctrl Pts',(3.15694930072946,-0.791565442099757,
7.89282076881693));
#94910=CARTESIAN_POINT('Ctrl Pts',(2.37304686356079,2.2274544484337,8.05188567266308));
#94911=CARTESIAN_POINT('Ctrl Pts',(-0.590364957545297,3.2006833572544,8.21095057650924));
#94912=CARTESIAN_POINT('Ctrl Pts',(-3.01155994143853,1.23426555312279,8.37001548035538));
#94913=CARTESIAN_POINT('Ctrl Pts',(-2.66680737771094,-1.86575538232892,
8.52908038420155));
#94914=CARTESIAN_POINT('Ctrl Pts',(0.127256994445537,-3.25218547962251,
8.6881452880477));
#94915=CARTESIAN_POINT('Ctrl Pts',(2.80444301168003,-1.651667076242,8.84721019189386));
#94916=CARTESIAN_POINT('Ctrl Pts',(2.90590667191787,1.46581415964166,9.00627509574));
#94917=CARTESIAN_POINT('Ctrl Pts',(0.33845933948028,3.23702795972191,9.16533999958617));
#94918=CARTESIAN_POINT('Ctrl Pts',(-2.53984376146567,2.03521458422612,9.3244049034323));
#94919=CARTESIAN_POINT('Ctrl Pts',(-3.08544395761391,-1.03582832599161,
9.48346980727847));
#94920=CARTESIAN_POINT('Ctrl Pts',(-0.797238314318297,-3.15552147935736,
9.64253471112462));
#94921=CARTESIAN_POINT('Ctrl Pts',(2.22318564879756,-2.37704655139174,9.80159961497078));
#94922=CARTESIAN_POINT('Ctrl Pts',(3.20173928132981,0.584611247661624,9.96066451881693));
#94923=CARTESIAN_POINT('Ctrl Pts',(1.23967639434314,3.00933666674422,10.1197294226631));
#94924=CARTESIAN_POINT('Ctrl Pts',(-1.86095917572251,2.6701564903198,10.2787943265092));
#94925=CARTESIAN_POINT('Ctrl Pts',(-3.25240895224441,-0.121411465122582,
10.4378592303554));
#94926=CARTESIAN_POINT('Ctrl Pts',(-1.65670498112303,-2.80146985384903,
10.5969241342015));
#94927=CARTESIAN_POINT('Ctrl Pts',(1.4605888533167,-2.90853656295908,10.7559890380477));
#94928=CARTESIAN_POINT('Ctrl Pts',(3.23641440039971,-0.344276873153268,
10.9150539418939));
#94929=CARTESIAN_POINT('Ctrl Pts',(2.03977629145653,2.53618166094517,11.07411884574));
#94930=CARTESIAN_POINT('Ctrl Pts',(-1.03028102240352,3.08730072253707,11.2331837495862));
#94931=CARTESIAN_POINT('Ctrl Pts',(-3.15408346414037,0.80290861107543,11.3922486534323));
#94932=CARTESIAN_POINT('Ctrl Pts',(-2.38103856022442,-2.21890966720757,
11.5513135572785));
#94933=CARTESIAN_POINT('Ctrl Pts',(0.578855649203793,-3.20278486225466,
11.7103784611246));
#94934=CARTESIAN_POINT('Ctrl Pts',(3.00710367045189,-1.24508323081533,11.8694433649708));
#94935=CARTESIAN_POINT('Ctrl Pts',(2.67349697704504,1.85615695732711,12.0285082688169));
#94936=CARTESIAN_POINT('Ctrl Pts',(-0.115565543582453,3.25262191802848,
12.1875731726631));
#94937=CARTESIAN_POINT('Ctrl Pts',(-2.79848764592934,1.66173753405392,12.3466380765092));
#94938=CARTESIAN_POINT('Ctrl Pts',(-2.91115705803489,-1.45535882859056,
12.5057029803554));
#94939=CARTESIAN_POINT('Ctrl Pts',(-0.350093294647169,-3.23579038590974,
12.6647678842015));
#94940=CARTESIAN_POINT('Ctrl Pts',(2.53251136734384,-2.0443314092331,12.8238327880477));
#94941=CARTESIAN_POINT('Ctrl Pts',(3.08914751400102,1.02473039051453,12.9828976918939));
#94942=CARTESIAN_POINT('Ctrl Pts',(0.808576314053412,3.15263525972394,13.14196259574));
#94943=CARTESIAN_POINT('Ctrl Pts',(-2.21462651747716,2.38502287716278,13.3010274995862));
#94944=CARTESIAN_POINT('Ctrl Pts',(-3.20382009665126,-0.573098180765103,
13.4600924034323));
#94945=CARTESIAN_POINT('Ctrl Pts',(-1.25048604507266,-3.00486095977523,
13.6191573072785));
#94946=CARTESIAN_POINT('Ctrl Pts',(1.85134874265622,-2.67682882709524,13.7782222111246));
#94947=CARTESIAN_POINT('Ctrl Pts',(3.25282437628674,0.109719248710308,13.9372871149708));
#94948=CARTESIAN_POINT('Ctrl Pts',(1.6667647187771,2.79549639755494,14.0963520188169));
#94949=CARTESIAN_POINT('Ctrl Pts',(-1.45012410235871,2.91376814867984,14.2554169226631));
#94950=CARTESIAN_POINT('Ctrl Pts',(-3.23515591826786,0.355908585172157,
14.4144818265092));
#94951=CARTESIAN_POINT('Ctrl Pts',(-2.04887992284062,-2.52883289251848,
14.5735467303554));
#94952=CARTESIAN_POINT('Ctrl Pts',(1.01917644825584,-3.09098432603974,14.7326116342016));
#94953=CARTESIAN_POINT('Ctrl Pts',(3.15117687078646,-0.814241404942834,
14.8916765380477));
#94954=CARTESIAN_POINT('Ctrl Pts',(2.38899948933553,2.21033621344296,15.0507414418939));
#94955=CARTESIAN_POINT('Ctrl Pts',(-0.567338860944949,3.20484498117529,
15.20980634574));
#94956=CARTESIAN_POINT('Ctrl Pts',(-3.00260854195925,1.25588481966146,15.3688712495862));
#94957=CARTESIAN_POINT('Ctrl Pts',(-2.68015202970693,-1.84653454724265,
15.5279361534323));
#94958=CARTESIAN_POINT('Ctrl Pts',(0.103872599392466,-3.25301632636516,
15.6870010572785));
#94959=CARTESIAN_POINT('Ctrl Pts',(2.79249611838898,-1.67178651905237,15.8460659611246));
#94960=CARTESIAN_POINT('Ctrl Pts',(2.91636982645886,1.44488469153185,16.0051308649708));
#94961=CARTESIAN_POINT('Ctrl Pts',(0.361722725942028,3.23451099952371,16.1641957688169));
#94962=CARTESIAN_POINT('Ctrl Pts',(-2.52514624835235,2.05342181758519,16.3232606726631));
#94963=CARTESIAN_POINT('Ctrl Pts',(-3.09281115271945,-1.01361921356935,
16.4823255765092));
#94964=CARTESIAN_POINT('Ctrl Pts',(-0.81990386544276,-3.14970830203922,
16.6413904803554));
#94965=CARTESIAN_POINT('Ctrl Pts',(2.2060387689647,-2.39296838389635,16.8004553842016));
#94966=CARTESIAN_POINT('Ctrl Pts',(3.20585951251589,0.56157770834868,16.9595202880477));
#94967=CARTESIAN_POINT('Ctrl Pts',(1.26127953714111,3.00034642428035,17.1185851918939));
#94968=CARTESIAN_POINT('Ctrl Pts',(-1.84171438663855,2.6834665741446,17.27765009574));
#94969=CARTESIAN_POINT('Ctrl Pts',(-3.25319776764363,-0.0980256145163866,
17.4367149995862));
#94970=CARTESIAN_POINT('Ctrl Pts',(-1.67680291865692,-2.7894868181238,17.5957799034323));
#94971=CARTESIAN_POINT('Ctrl Pts',(1.43964061303579,-2.91896208296729,17.7548448072785));
#94972=CARTESIAN_POINT('Ctrl Pts',(3.23385563176069,-0.367535698174335,
17.9139097111246));
#94973=CARTESIAN_POINT('Ctrl Pts',(2.05795707879432,2.52145144675506,18.0729746149708));
#94974=CARTESIAN_POINT('Ctrl Pts',(-1.00805870440757,3.09462798813861,18.2320395188169));
#94975=CARTESIAN_POINT('Ctrl Pts',(-3.14822955822641,0.825563677260734,
18.3911044226631));
#94976=CARTESIAN_POINT('Ctrl Pts',(-2.3969295480238,-2.20173419792519,18.5501693265093));
#94977=CARTESIAN_POINT('Ctrl Pts',(0.55581474158759,-3.20686368739564,18.7092342303554));
#94978=CARTESIAN_POINT('Ctrl Pts',(2.99807461404624,-1.26667018008408,18.8682991342016));
#94979=CARTESIAN_POINT('Ctrl Pts',(2.68677244970067,1.83688827641538,19.0273640380477));
#94980=CARTESIAN_POINT('Ctrl Pts',(-0.0921783129706565,3.25336869953601,
19.1864289418939));
#94981=CARTESIAN_POINT('Ctrl Pts',(-2.78646850648086,1.68181390138538,19.34549384574));
#94982=CARTESIAN_POINT('Ctrl Pts',(-2.92154490983091,-1.43439188381135,
19.5045587495862));
#94983=CARTESIAN_POINT('Ctrl Pts',(-0.37334748309046,-3.23318981709592,
19.6636236534323));
#94984=CARTESIAN_POINT('Ctrl Pts',(2.51774849966255,-2.06248569181699,19.8226885572785));
#94985=CARTESIAN_POINT('Ctrl Pts',(3.09643482642802,1.00249493873363,19.9817534611246));
#94986=CARTESIAN_POINT('Ctrl Pts',(0.831220822112772,3.14674064412511,20.1408183649708));
#94987=CARTESIAN_POINT('Ctrl Pts',(-2.19742251423028,2.40088296892136,20.2998832688169));
#94988=CARTESIAN_POINT('Ctrl Pts',(-3.20785750257054,-0.550049979278808,
20.4589481726631));
#94989=CARTESIAN_POINT('Ctrl Pts',(-1.27205673107604,-2.99579311859597,
20.6180130765092));
#94990=CARTESIAN_POINT('Ctrl Pts',(1.83205623216379,-2.69006964569557,20.7770779803554));
#94991=CARTESIAN_POINT('Ctrl Pts',(3.25352912149012,0.0863307136449077,
20.9361428842016));
#94992=CARTESIAN_POINT('Ctrl Pts',(1.68681945104979,2.78344119321081,21.0952077880477));
#94993=CARTESIAN_POINT('Ctrl Pts',(-1.42913852081457,2.9241182987059,21.2542726918939));
#94994=CARTESIAN_POINT('Ctrl Pts',(-3.23251355768036,0.379158061915388,
21.41333759574));
#94995=CARTESIAN_POINT('Ctrl Pts',(-2.06700764202351,-2.51403741903719,
21.5724024995862));
#94996=CARTESIAN_POINT('Ctrl Pts',(0.996927934521134,-3.09823166175065,
21.7314674034323));
#94997=CARTESIAN_POINT('Ctrl Pts',(3.1452415645452,-0.836875281723708,21.8905323072785));
#94998=CARTESIAN_POINT('Ctrl Pts',(2.40482863381765,2.19310373180877,22.0495972111246));
#94999=CARTESIAN_POINT('Ctrl Pts',(-0.544283440045353,3.20884095483013,
22.2086621149708));
#95000=CARTESIAN_POINT('Ctrl Pts',(-2.99350194529984,1.27743917271579,22.367727018817));
#95001=CARTESIAN_POINT('Ctrl Pts',(-2.69335815147779,-1.82721826949352,
22.5267919226631));
#95002=CARTESIAN_POINT('Ctrl Pts',(0.0804828354295357,-3.25367903298773,
22.6858568265093));
#95003=CARTESIAN_POINT('Ctrl Pts',(2.78040488809325,-1.69181955147998,22.8449217303554));
#95004=CARTESIAN_POINT('Ctrl Pts',(2.92668224127907,1.42388054101619,23.0039866342016));
#95005=CARTESIAN_POINT('Ctrl Pts',(0.384967415878305,3.23182685569862,23.1630515380477));
#95006=CARTESIAN_POINT('Ctrl Pts',(-2.51031821686753,2.07152291480586,23.3221164418939));
#95007=CARTESIAN_POINT('Ctrl Pts',(-3.1000184883019,-0.991357709754248,
23.48118134574));
#95008=CARTESIAN_POINT('Ctrl Pts',(-0.84252703782683,-3.1437323243294,23.6402462495862));
#95009=CARTESIAN_POINT('Ctrl Pts',(2.18877786461233,-2.40876652996629,23.7993111534323));
#95010=CARTESIAN_POINT('Ctrl Pts',(3.20981404099739,0.538515142515751,23.9583760572785));
#95011=CARTESIAN_POINT('Ctrl Pts',(1.28281748761557,2.99120110155944,24.1174409611246));
#95012=CARTESIAN_POINT('Ctrl Pts',(-1.82237440403357,2.69663795642391,24.2765058649708));
#95013=CARTESIAN_POINT('Ctrl Pts',(-3.25381843354455,-0.074634697216143,
24.4355707688169));
#95014=CARTESIAN_POINT('Ctrl Pts',(-1.69681418652307,-2.77735960093697,
24.5946356726631));
#95015=CARTESIAN_POINT('Ctrl Pts',(1.41861796140208,-2.92923672926757,24.7537005765093));
#95016=CARTESIAN_POINT('Ctrl Pts',(3.23112971336905,-0.390775526212221,
24.9127654803554));
#95017=CARTESIAN_POINT('Ctrl Pts',(2.07603149557764,2.50659090516829,25.0718303842016));
#95018=CARTESIAN_POINT('Ctrl Pts',(-0.985784282427312,3.10179530030949,
25.2308952880477));
#95019=CARTESIAN_POINT('Ctrl Pts',(-3.14221292835331,0.848176072164354,
25.3899601918939));
#95020=CARTESIAN_POINT('Ctrl Pts',(-2.41269664464596,-2.18444492661569,
25.54902509574));
#95021=CARTESIAN_POINT('Ctrl Pts',(0.532745105324541,-3.21077675792875,
25.7080899995862));
#95022=CARTESIAN_POINT('Ctrl Pts',(2.98889059480765,-1.2881916584007,25.8671549034324));
#95023=CARTESIAN_POINT('Ctrl Pts',(2.69990904993852,1.81752465143196,26.0262198072784));
#95024=CARTESIAN_POINT('Ctrl Pts',(-0.0687863178969091,3.25394732271021,
26.1852847111247));
#95025=CARTESIAN_POINT('Ctrl Pts',(-2.77430534157964,1.70180334004416,26.3443496149708));
#95026=CARTESIAN_POINT('Ctrl Pts',(-2.93178175441925,-1.41335079897282,
26.503414518817));
#95027=CARTESIAN_POINT('Ctrl Pts',(-0.39658237415413,-3.23042213294379,
26.6624794226631));
#95028=CARTESIAN_POINT('Ctrl Pts',(2.50285549598059,-2.08053336977387,26.8215443265093));
#95029=CARTESIAN_POINT('Ctrl Pts',(3.10356209203342,0.980207670545344,26.9806092303554));
#95030=CARTESIAN_POINT('Ctrl Pts',(0.853822366487097,3.14068338152529,27.1396741342016));
#95031=CARTESIAN_POINT('Ctrl Pts',(-2.18010493181619,2.41661896516052,27.2987390380477));
#95032=CARTESIAN_POINT('Ctrl Pts',(-3.21172910251423,-0.526973347111528,
27.4578039418939));
#95033=CARTESIAN_POINT('Ctrl Pts',(-1.29356166771021,-2.98657043250842,
27.61686884574));
#95034=CARTESIAN_POINT('Ctrl Pts',(1.81266902735566,-2.7031714214545,27.7759337495863));
#95035=CARTESIAN_POINT('Ctrl Pts',(3.2540657000684,0.0629377163649865,27.9349986534323));
#95036=CARTESIAN_POINT('Ctrl Pts',(1.70678699592574,2.77124211988804,28.0940635572785));
#95037=CARTESIAN_POINT('Ctrl Pts',(-1.408079070744,2.9343173085124,28.2531284611246));
#95038=CARTESIAN_POINT('Ctrl Pts',(-3.22970411670864,0.402387940945082,
28.4121933649708));
#95039=CARTESIAN_POINT('Ctrl Pts',(-2.08502852285137,-2.49911200137148,
28.571258268817));
#95040=CARTESIAN_POINT('Ctrl Pts',(0.974627892123291,-3.10531885776615,
28.7303231726631));
#95041=CARTESIAN_POINT('Ctrl Pts',(3.13914368878651,-0.859465902554945,
28.8893880765092));
#95042=CARTESIAN_POINT('Ctrl Pts',(2.42053347883902,2.17575789423417,29.0484529803554));
#95043=CARTESIAN_POINT('Ctrl Pts',(-0.521199886522412,3.21267107167726,
29.2075178842015));
#95044=CARTESIAN_POINT('Ctrl Pts',(-2.98424062215708,1.29892749819622,29.3665827880478));
#95045=CARTESIAN_POINT('Ctrl Pts',(-2.70642506043275,-1.8078075474907,29.5256476918938));
#95046=CARTESIAN_POINT('Ctrl Pts',(0.0570889115140672,-3.25417356523664,
29.68471259574));
#95047=CARTESIAN_POINT('Ctrl Pts',(2.76816994575776,-1.71176513806837,29.8437774995862));
#95048=CARTESIAN_POINT('Ctrl Pts',(2.93684338335604,1.40280279374565,30.0028424034323));
#95049=CARTESIAN_POINT('Ctrl Pts',(0.40819220783041,3.22897566698317,30.1619073072785));
#95050=CARTESIAN_POINT('Ctrl Pts',(-2.49536043343434,2.08951694028864,30.3209722111246));
#95051=CARTESIAN_POINT('Ctrl Pts',(-3.10706559183244,-0.969044965186682,
30.4800371149708));
#95052=CARTESIAN_POINT('Ctrl Pts',(-0.865106662136416,-3.13759385511094,
30.6391020188169));
#95053=CARTESIAN_POINT('Ctrl Pts',(2.17140382791264,-2.42444017303564,30.7981669226631));
#95054=CARTESIAN_POINT('Ctrl Pts',(3.21360266237481,0.515424742208121,30.9572318265092));
#95055=CARTESIAN_POINT('Ctrl Pts',(1.30428913252471,2.98190117127995,31.1162967303554));
#95056=CARTESIAN_POINT('Ctrl Pts',(-1.80294022754192,2.70966995636255,31.2753616342015));
#95057=CARTESIAN_POINT('Ctrl Pts',(-3.25427091786653,-0.0512399222386381,
31.4344265380477));
#95058=CARTESIAN_POINT('Ctrl Pts',(-1.71673775039014,-2.7650888291135,31.5934914418938));
#95059=CARTESIAN_POINT('Ctrl Pts',(1.39752198502285,-2.93935997078965,31.7525563457401));
#95060=CARTESIAN_POINT('Ctrl Pts',(3.22823678612057,-0.41399515605946,31.9116212495861));
#95061=CARTESIAN_POINT('Ctrl Pts',(2.09399860758597,2.49160080428844,32.0706861534323));
#95062=CARTESIAN_POINT('Ctrl Pts',(-0.96345890777087,3.10880228858957,32.2297510572785));
#95063=CARTESIAN_POINT('Ctrl Pts',(-3.13603388550525,0.870744627009331,
32.3888159611247));
#95064=CARTESIAN_POINT('Ctrl Pts',(-2.42833903512999,-2.16704274691726,
32.5478808649708));
#95065=CARTESIAN_POINT('Ctrl Pts',(0.509647932825191,-3.21452387159745,
32.706945768817));
#95066=CARTESIAN_POINT('Ctrl Pts',(2.97955208743464,-1.30964655337489,32.8660106726631));
#95067=CARTESIAN_POINT('Ctrl Pts',(2.71290609876123,1.79806708323324,33.0250755765093));
#95068=CARTESIAN_POINT('Ctrl Pts',(-0.0453907674337705,3.25435775764352,
33.1841404803554));
#95069=CARTESIAN_POINT('Ctrl Pts',(-2.76199877990863,1.7217048168272,33.3432053842015));
#95070=CARTESIAN_POINT('Ctrl Pts',(-2.94186706268354,-1.39223666163496,
33.5022702880478));
#95071=CARTESIAN_POINT('Ctrl Pts',(-0.419796766886049,-3.22748747650781,
33.6613351918938));
#95072=CARTESIAN_POINT('Ctrl Pts',(2.48783312607924,-2.09847351026542,33.8204000957401));
#95073=CARTESIAN_POINT('Ctrl Pts',(3.11052894242712,0.957869737921647,33.9794649995861));
#95074=CARTESIAN_POINT('Ctrl Pts',(0.87637977896019,3.13446378500892,34.1385299034323));
#95075=CARTESIAN_POINT('Ctrl Pts',(-2.16267466533653,2.43223005252675,34.2975948072785));
#95076=CARTESIAN_POINT('Ctrl Pts',(-3.21543469636917,-0.5038694770355,34.4566597111246));
#95077=CARTESIAN_POINT('Ctrl Pts',(-1.3149997434398,-2.97719337820976,34.6157246149708));
#95078=CARTESIAN_POINT('Ctrl Pts',(1.79318813030706,-2.7161334771746,34.774789518817));
#95079=CARTESIAN_POINT('Ctrl Pts',(3.25443408428712,0.0395414659949287,
34.933854422663));
#95080=CARTESIAN_POINT('Ctrl Pts',(1.72666632133354,2.75889980812558,35.0929193265093));
#95081=CARTESIAN_POINT('Ctrl Pts',(-1.38694684065627,2.94436465093854,35.2519842303554));
#95082=CARTESIAN_POINT('Ctrl Pts',(-3.22672774056554,0.425597021568032,
35.4110491342015));
#95083=CARTESIAN_POINT('Ctrl Pts',(-2.10294163387085,-2.48405741097813,
35.5701140380478));
#95084=CARTESIAN_POINT('Ctrl Pts',(0.9522774736946,-3.11224554776717,35.7291789418938));
#95085=CARTESIAN_POINT('Ctrl Pts',(3.13288355869409,-0.882012099784934,
35.8882438457401));
#95086=CARTESIAN_POINT('Ctrl Pts',(2.43611321265621,2.15829959728129,36.0473087495861));
#95087=CARTESIAN_POINT('Ctrl Pts',(-0.498089393506169,3.21633513374765,
36.2063736534324));
#95088=CARTESIAN_POINT('Ctrl Pts',(-2.97482505122513,1.32034868542603,36.3654385572784));
#95089=CARTESIAN_POINT('Ctrl Pts',(-2.7193520811766,-1.78830338452491,36.5245034611247));
#95090=CARTESIAN_POINT('Ctrl Pts',(0.0336920368183218,-3.25449989755074,
36.6835683649708));
#95091=CARTESIAN_POINT('Ctrl Pts',(2.75579192377546,-1.73162224788107,36.842633268817));
#95092=CARTESIAN_POINT('Ctrl Pts',(2.94685272748626,1.3816525391753,37.0016981726631));
#95093=CARTESIAN_POINT('Ctrl Pts',(0.431395901367992,3.22595758074802,37.1607630765093));
#95094=CARTESIAN_POINT('Ctrl Pts',(-2.48027367118244,2.1074029639682,37.3198279803554));
#95095=CARTESIAN_POINT('Ctrl Pts',(-3.11395209906432,-0.946682133155469,
37.4788928842016));
#95096=CARTESIAN_POINT('Ctrl Pts',(-0.887641571288324,-3.1312932116657,
37.6379577880477));
#95097=CARTESIAN_POINT('Ctrl Pts',(2.15391755688526,-2.43998850297376,37.7970226918939));
#95098=CARTESIAN_POINT('Ctrl Pts',(3.21722518082396,0.49230770090969,37.95608759574));
#95099=CARTESIAN_POINT('Ctrl Pts',(1.32569336205399,2.97244711413151,38.1151524995862));
#95100=CARTESIAN_POINT('Ctrl Pts',(-1.7834128616667,2.72256190036968,38.2742174034323));
#95101=CARTESIAN_POINT('Ctrl Pts',(-3.25455519722178,-0.0278424988002109,
38.4332823072785));
#95102=CARTESIAN_POINT('Ctrl Pts',(-1.73657258045988,-2.75267513689822,
38.5923472111246));
#95103=CARTESIAN_POINT('Ctrl Pts',(1.37635377429526,-2.94933128428904,38.7514121149708));
#95104=CARTESIAN_POINT('Ctrl Pts',(3.22517699954328,-0.437193387552653,
38.910477018817));
#95105=CARTESIAN_POINT('Ctrl Pts',(2.11185748614512,2.47648191891553,39.0695419226631));
#95106=CARTESIAN_POINT('Ctrl Pts',(-0.941083734379852,3.11564859080552,
39.2286068265092));
#95107=CARTESIAN_POINT('Ctrl Pts',(-3.12969274906124,0.893268175284591,
39.3876717303555));
#95108=CARTESIAN_POINT('Ctrl Pts',(-2.44385591096055,-2.14952855830434,
39.5467366342015));
#95109=CARTESIAN_POINT('Ctrl Pts',(0.486524417923579,-3.21810483472289,
39.7058015380477));
#95110=CARTESIAN_POINT('Ctrl Pts',(2.97005957461085,-1.33103375605782,39.8648664418939));
#95111=CARTESIAN_POINT('Ctrl Pts',(2.72576292438452,1.77851657753127,40.02393134574));
#95112=CARTESIAN_POINT('Ctrl Pts',(-0.0219928708375552,3.25459998312159,
40.1829962495862));
#95113=CARTESIAN_POINT('Ctrl Pts',(-2.74954945756262,1.74151730307793,40.3420611534324));
#95114=CARTESIAN_POINT('Ctrl Pts',(-2.95180031333992,-1.37105056313366,
40.5011260572785));
#95115=CARTESIAN_POINT('Ctrl Pts',(-0.442989461393428,-3.22438599947294,
40.6601909611247));
#95116=CARTESIAN_POINT('Ctrl Pts',(2.47268216642652,-2.11630518601147,40.8192558649708));
#95117=CARTESIAN_POINT('Ctrl Pts',(3.11733501751034,0.935482295453273,40.978320768817));
#95118=CARTESIAN_POINT('Ctrl Pts',(0.898891893597044,3.12808217605105,41.1373856726631));
#95119=CARTESIAN_POINT('Ctrl Pts',(-2.14513261571724,2.44771542412284,41.2964505765093));
#95120=CARTESIAN_POINT('Ctrl Pts',(-3.21897409260272,-0.480739563230735,
41.4555154803553));
#95121=CARTESIAN_POINT('Ctrl Pts',(-1.33636985018545,-2.96766244037597,
41.6145803842017));
#95122=CARTESIAN_POINT('Ctrl Pts',(1.77361454793589,-2.72895514288032,41.7736452880476));
#95123=CARTESIAN_POINT('Ctrl Pts',(3.2546342551055,0.0161431718273427,41.9327101918939));
#95124=CARTESIAN_POINT('Ctrl Pts',(1.74645639976147,2.74641489586606,42.0917750957401));
#95125=CARTESIAN_POINT('Ctrl Pts',(-1.3657429228224,2.95425980666279,42.2508399995862));
#95126=CARTESIAN_POINT('Ctrl Pts',(-3.22358458309233,0.448784104166184,
42.4099049034324));
#95127=CARTESIAN_POINT('Ctrl Pts',(-2.120746049199,-2.46887442599044,42.5689698072784));
#95128=CARTESIAN_POINT('Ctrl Pts',(0.929877834471077,-3.1190113737308,42.7280347111247));
#95129=CARTESIAN_POINT('Ctrl Pts',(3.12646149783801,-0.904512708058399,
42.8870996149708));
#95130=CARTESIAN_POINT('Ctrl Pts',(2.45156702999263,2.14072974332502,43.0461645188169));
#95131=CARTESIAN_POINT('Ctrl Pts',(-0.474953155519126,3.21983295165524,
43.2052294226632));
#95132=CARTESIAN_POINT('Ctrl Pts',(-2.96525571917066,1.3417016271988,43.3642943265092));
#95133=CARTESIAN_POINT('Ctrl Pts',(-2.73213854554495,-1.7687067887167,43.5233592303554));
#95134=CARTESIAN_POINT('Ctrl Pts',(0.0102934206674854,-3.25465801306237,
43.6824241342016));
#95135=CARTESIAN_POINT('Ctrl Pts',(2.74327146193368,-1.75138985455559,43.8414890380477));
#95136=CARTESIAN_POINT('Ctrl Pts',(2.95670975631421,1.36043087050919,44.0005539418939));
#95137=CARTESIAN_POINT('Ctrl Pts',(0.45457729714776,3.22277275298764,44.1596188457401));
#95138=CARTESIAN_POINT('Ctrl Pts',(-2.46505870990123,2.12518006136686,44.3186837495862));
#95139=CARTESIAN_POINT('Ctrl Pts',(-3.12067765406467,-0.924270369548566,
44.4777486534324));
#95140=CARTESIAN_POINT('Ctrl Pts',(-0.910130600485398,-3.12483071963845,
44.6368135572785));
#95141=CARTESIAN_POINT('Ctrl Pts',(2.13631995530277,-2.45541071616408,44.7958784611246));
#95142=CARTESIAN_POINT('Ctrl Pts',(3.22068140919789,0.469165213551552,44.9549433649708));
#95143=CARTESIAN_POINT('Ctrl Pts',(1.34702906969843,2.96283941863608,45.114008268817));
#95144=CARTESIAN_POINT('Ctrl Pts',(-1.76379331539366,2.73531312234951,45.2730731726631));
#95145=CARTESIAN_POINT('Ctrl Pts',(-3.2546712575536,-0.00444363674203639,
45.4321380765093));
#95146=CARTESIAN_POINT('Ctrl Pts',(-1.7563176503055,-2.74011916499234,45.5912029803554));
#95147=CARTESIAN_POINT('Ctrl Pts',(1.3551144210326,-2.95915015614983,45.7502678842016));
#95148=CARTESIAN_POINT('Ctrl Pts',(3.22195051621063,-0.460369018246669,
45.9093327880477));
#95149=CARTESIAN_POINT('Ctrl Pts',(2.1296071997422,2.46123502404409,46.0683976918939));
#95150=CARTESIAN_POINT('Ctrl Pts',(-0.918659902683561,3.12233386541619,
46.22746259574));
#95151=CARTESIAN_POINT('Ctrl Pts',(-3.123189877464,0.915745529291522,46.3865274995862));
#95152=CARTESIAN_POINT('Ctrl Pts',(-2.45924641157584,-2.13190322118698,
46.5455924034324));
#95153=CARTESIAN_POINT('Ctrl Pts',(0.463375644159019,-3.22151954777474,
46.7046573072785));
#95154=CARTESIAN_POINT('Ctrl Pts',(2.96041375996944,-1.352351997789,46.8637222111247));
#95155=CARTESIAN_POINT('Ctrl Pts',(2.7384784559849,1.75887383351055,47.0227871149707));
#95156=CARTESIAN_POINT('Ctrl Pts',(0.00140693752478723,3.25467458050298,
47.1818520188171));
#95157=CARTESIAN_POINT('Ctrl Pts',(-2.7369594963831,1.76123864188931,47.340916922663));
#95158=CARTESIAN_POINT('Ctrl Pts',(-2.9615781729108,-1.34979143756155,47.4999818265093));
#95159=CARTESIAN_POINT('Ctrl Pts',(-0.466164638283834,-3.22112198428059,
47.6590467303553));
#95160=CARTESIAN_POINT('Ctrl Pts',(2.45741366154578,-2.13401961218112,47.8181116342016));
#95161=CARTESIAN_POINT('Ctrl Pts',(3.12396039138569,0.913031500959189,47.9771765380477));
#95162=CARTESIAN_POINT('Ctrl Pts',(0.921394885372682,3.12156749643814,48.1362414418939));
#95163=CARTESIAN_POINT('Ctrl Pts',(-2.12755091531158,2.46301970066826,48.2953063457401));
#95164=CARTESIAN_POINT('Ctrl Pts',(-3.22221123648809,-0.457480686744324,
48.4543712495861));
#95165=CARTESIAN_POINT('Ctrl Pts',(-1.35793011442734,-2.95817673926339,
48.6134361534324));
#95166=CARTESIAN_POINT('Ctrl Pts',(1.75444422073719,-2.74125664937627,48.7725010572784));
#95167=CARTESIAN_POINT('Ctrl Pts',(3.25371829941633,-0.00798100720446507,
48.9315659611247));
#95168=CARTESIAN_POINT('Ctrl Pts',(1.7679977121055,2.73518764693765,49.0906308649707));
#95169=CARTESIAN_POINT('Ctrl Pts',(-1.34827175404425,2.96118711175811,49.249695768817));
#95170=CARTESIAN_POINT('Ctrl Pts',(-2.58989120385452,1.30614186523129,49.3557390380477));
#95171=CARTESIAN_POINT('Ctrl Pts',(-2.72283095673211,0.399045011670457,
49.4087606726631));
#95172=CARTESIAN_POINT('Ctrl Pts',(1.48738611075516,-2.08582659521601,-0.109744663668461));
#95173=CARTESIAN_POINT('Ctrl Pts',(2.18226830199655,-1.59031171289833,-0.0567230290530766));
#95174=CARTESIAN_POINT('Ctrl Pts',(3.02564425429361,0.141323225187899,0.0493202401776927));
#95175=CARTESIAN_POINT('Ctrl Pts',(1.51443447872066,2.6265638058203,0.208385144023846));
#95176=CARTESIAN_POINT('Ctrl Pts',(-1.38901916658974,2.69172145058039,0.367450047870002));
#95177=CARTESIAN_POINT('Ctrl Pts',(-3.01604259595292,0.288558531368754,
0.526514951716154));
#95178=CARTESIAN_POINT('Ctrl Pts',(-1.87336583720858,-2.38163901943715,
0.685579855562309));
#95179=CARTESIAN_POINT('Ctrl Pts',(0.990082607075607,-2.86338445583323,
0.844644759408461));
#95180=CARTESIAN_POINT('Ctrl Pts',(2.94409597960784,-0.715824020681664,
1.00370966325462));
#95181=CARTESIAN_POINT('Ctrl Pts',(2.19417615309141,2.08946906230414,1.16277456710077));
#95182=CARTESIAN_POINT('Ctrl Pts',(-0.570997951771571,2.9755515685831,1.32183947094693));
#95183=CARTESIAN_POINT('Ctrl Pts',(-2.81172828739708,1.12883753547801,1.48090437479308));
#95184=CARTESIAN_POINT('Ctrl Pts',(-2.47005271785342,-1.75469155487355,
1.63996927863923));
#95185=CARTESIAN_POINT('Ctrl Pts',(0.140230594765303,-3.02661384558711,
1.79903418248539));
#95186=CARTESIAN_POINT('Ctrl Pts',(2.62171795481554,-1.51877386128767,1.95809908633154));
#95187=CARTESIAN_POINT('Ctrl Pts',(2.69530668223053,1.38398004400222,2.11716399017769));
#95188=CARTESIAN_POINT('Ctrl Pts',(0.293408029811388,3.01562338031741,2.27622889402385));
#95189=CARTESIAN_POINT('Ctrl Pts',(-2.37796901060781,1.87758877721523,2.43529379787));
#95190=CARTESIAN_POINT('Ctrl Pts',(-2.86531611033693,-0.984905831706037,
2.59435870171616));
#95191=CARTESIAN_POINT('Ctrl Pts',(-0.721032271090857,-2.94281966321798,
2.7534236055623));
#95192=CARTESIAN_POINT('Ctrl Pts',(2.08547890242402,-2.19792024371884,2.91248850940847));
#95193=CARTESIAN_POINT('Ctrl Pts',(2.97659562927056,0.565644784578315,3.07155341325461));
#95194=CARTESIAN_POINT('Ctrl Pts',(1.13387754065414,2.80969699176317,3.23061831710078));
#95195=CARTESIAN_POINT('Ctrl Pts',(-1.75024295905019,2.47320139246638,3.38968322094693));
#95196=CARTESIAN_POINT('Ctrl Pts',(-3.02686425414068,-0.134789881251951,
3.54874812479308));
#95197=CARTESIAN_POINT('Ctrl Pts',(-1.52348185391423,-2.61898425999305,
3.70781302863924));
#95198=CARTESIAN_POINT('Ctrl Pts',(1.37913249816518,-2.69778966517383,3.86687793248538));
#95199=CARTESIAN_POINT('Ctrl Pts',(3.01509162042777,-0.298827779893139,
4.02594283633155));
#95200=CARTESIAN_POINT('Ctrl Pts',(1.88185954733525,2.37459052563238,4.1850077401777));
#95201=CARTESIAN_POINT('Ctrl Pts',(-0.979754128895413,2.86708168158829,
4.34407264402385));
#95202=CARTESIAN_POINT('Ctrl Pts',(-2.94151902821897,0.726320403143036,
4.50313754787));
#95203=CARTESIAN_POINT('Ctrl Pts',(-2.20166499891421,-2.08152510285824,
4.66220245171616));
#95204=CARTESIAN_POINT('Ctrl Pts',(0.560293860707996,-2.97760748104212,
4.82126735556231));
#95205=CARTESIAN_POINT('Ctrl Pts',(2.80765448550222,-1.13892572692277,4.98033225940847));
#95206=CARTESIAN_POINT('Ctrl Pts',(2.47634319614971,1.74579491816248,5.13939716325462));
#95207=CARTESIAN_POINT('Ctrl Pts',(-0.129349318760607,3.02710162947443,
5.29846206710077));
#95208=CARTESIAN_POINT('Ctrl Pts',(-2.61624179715656,1.52818663134642,5.45752697094693));
#95209=CARTESIAN_POINT('Ctrl Pts',(-2.70026409413619,-1.37428139161307,
5.61659187479307));
#95210=CARTESIAN_POINT('Ctrl Pts',(-0.304246480126756,-3.01454965139899,
5.77565677863924));
#95211=CARTESIAN_POINT('Ctrl Pts',(2.37120432529958,-1.88612448398758,5.93472168248538));
#95212=CARTESIAN_POINT('Ctrl Pts',(2.86883801401339,0.974599389887348,6.09378658633155));
#95213=CARTESIAN_POINT('Ctrl Pts',(0.731606176659906,2.94020882314347,6.25285149017769));
#95214=CARTESIAN_POINT('Ctrl Pts',(-2.07756457258859,2.20540267709597,6.41191639402386));
#95215=CARTESIAN_POINT('Ctrl Pts',(-2.97860971706148,-0.554941145387749,
6.57098129787));
#95216=CARTESIAN_POINT('Ctrl Pts',(-1.14397023216239,-2.80560289943957,
6.73004620171617));
#95217=CARTESIAN_POINT('Ctrl Pts',(1.74134123660211,-2.47947700516185,6.88911110556231));
#95218=CARTESIAN_POINT('Ctrl Pts',(3.0273292263028,0.123908341084059,7.04817600940847));
#95219=CARTESIAN_POINT('Ctrl Pts',(1.5328864717516,2.61349088120435,7.20724091325462));
#95220=CARTESIAN_POINT('Ctrl Pts',(-1.36942584534175,2.70272980068808,7.36630581710077));
#95221=CARTESIAN_POINT('Ctrl Pts',(-3.01399794400122,0.309664197113199,
7.52537072094693));
#95222=CARTESIAN_POINT('Ctrl Pts',(-1.89038332751853,-2.36781046463971,
7.68443562479308));
#95223=CARTESIAN_POINT('Ctrl Pts',(0.969441502437645,-2.87058507882431,
7.84350052863925));
#95224=CARTESIAN_POINT('Ctrl Pts',(2.93888911979601,-0.736889586683079,
8.00256543248538));
#95225=CARTESIAN_POINT('Ctrl Pts',(2.2091332307661,2.07359733076176,8.16163033633156));
#95226=CARTESIAN_POINT('Ctrl Pts',(-0.549586637339215,2.97960233076085,
8.32069524017768));
#95227=CARTESIAN_POINT('Ctrl Pts',(-2.80354224993797,1.14901104182252,8.47976014402387));
#95228=CARTESIAN_POINT('Ctrl Pts',(-2.48260280427558,-1.7368819296718,8.63882504787));
#95229=CARTESIAN_POINT('Ctrl Pts',(0.118466963123882,-3.02754704341081,
8.79788995171617));
#95230=CARTESIAN_POINT('Ctrl Pts',(2.61073152242574,-1.53758136019852,8.95695485556231));
#95231=CARTESIAN_POINT('Ctrl Pts',(2.7051867761288,1.36456587516881,9.11601975940847));
#95232=CARTESIAN_POINT('Ctrl Pts',(0.315080913736107,3.01343649994762,9.27508466325462));
#95233=CARTESIAN_POINT('Ctrl Pts',(-2.3644089548186,1.89463606420625,9.43414956710077));
#95234=CARTESIAN_POINT('Ctrl Pts',(-2.87232287027127,-0.964280483227741,
9.59321447094693));
#95235=CARTESIAN_POINT('Ctrl Pts',(-0.742170616200155,-2.93755992242991,
9.75227937479308));
#95236=CARTESIAN_POINT('Ctrl Pts',(2.06962339022292,-2.21285664787839,9.91134427863924));
#95237=CARTESIAN_POINT('Ctrl Pts',(2.98058531891839,0.544230353862732,10.0704091824854));
#95238=CARTESIAN_POINT('Ctrl Pts',(1.15404813962696,2.80147254365288,10.2294740863316));
#95239=CARTESIAN_POINT('Ctrl Pts',(-1.73241701178142,2.48572058339382,10.3885389901777));
#95240=CARTESIAN_POINT('Ctrl Pts',(-3.02775508009259,-0.113025202458703,
10.5476038940239));
#95241=CARTESIAN_POINT('Ctrl Pts',(-1.54227128152162,-2.60796372973456,
10.70666879787));
#95242=CARTESIAN_POINT('Ctrl Pts',(1.3597014967949,-2.70763501252128,10.8657337017162));
#95243=CARTESIAN_POINT('Ctrl Pts',(3.01286532105161,-0.320496612496818,
11.0247986055623));
#95244=CARTESIAN_POINT('Ctrl Pts',(1.89888268031252,2.36099980682474,11.1838635094085));
#95245=CARTESIAN_POINT('Ctrl Pts',(-0.959116348930274,2.8740513827404,11.3429284132546));
#95246=CARTESIAN_POINT('Ctrl Pts',(-2.93622123533907,0.747449248150846,
11.5019933171008));
#95247=CARTESIAN_POINT('Ctrl Pts',(-2.2165729164044,-2.06564276380982,11.6610582209469));
#95248=CARTESIAN_POINT('Ctrl Pts',(0.538872312261706,-2.98155867835853,
11.8201231247931));
#95249=CARTESIAN_POINT('Ctrl Pts',(2.79939378727039,-1.15908150930349,11.9791880286392));
#95250=CARTESIAN_POINT('Ctrl Pts',(2.4888303324447,1.72794649735476,12.1382529324854));
#95251=CARTESIAN_POINT('Ctrl Pts',(-0.107583076667991,3.0279533356761,12.2973178363316));
#95252=CARTESIAN_POINT('Ctrl Pts',(-2.60518751207211,1.54695622057019,12.4563827401777));
#95253=CARTESIAN_POINT('Ctrl Pts',(-2.71007450195653,-1.35483272593425,
12.6154476440239));
#95254=CARTESIAN_POINT('Ctrl Pts',(-0.325911275900068,-3.01228440915837,
12.77451254787));
#95255=CARTESIAN_POINT('Ctrl Pts',(2.3575830316713,-1.90312316211876,12.9335774517162));
#95256=CARTESIAN_POINT('Ctrl Pts',(2.87577061064776,0.953949116227871,13.0926423555623));
#95257=CARTESIAN_POINT('Ctrl Pts',(0.752725465482682,2.93487306284808,13.2517072594085));
#95258=CARTESIAN_POINT('Ctrl Pts',(-2.06165546438178,2.22028202433883,13.4107721632546));
#95259=CARTESIAN_POINT('Ctrl Pts',(-2.98252240593688,-0.533512529845143,
13.5698370671008));
#95260=CARTESIAN_POINT('Ctrl Pts',(-1.16411113459189,-2.79730598750593,
13.728901970947));
#95261=CARTESIAN_POINT('Ctrl Pts',(1.72347040083377,-2.4919320413822,13.8879668747931));
#95262=CARTESIAN_POINT('Ctrl Pts',(3.02814180952086,0.102140603332451,14.0470317786392));
#95263=CARTESIAN_POINT('Ctrl Pts',(1.55163616220966,2.60240287840691,14.2060966824854));
#95264=CARTESIAN_POINT('Ctrl Pts',(-1.34995957831533,2.71250523655384,14.3651615863315));
#95265=CARTESIAN_POINT('Ctrl Pts',(-3.01169376614451,0.331324886453901,
14.5242264901777));
#95266=CARTESIAN_POINT('Ctrl Pts',(-1.90735749592618,-2.3541586403961,14.6832913940239));
#95267=CARTESIAN_POINT('Ctrl Pts',(0.948778801813178,-2.87748054843943,
14.84235629787));
#95268=CARTESIAN_POINT('Ctrl Pts',(2.93351540931218,-0.757999251150931,
15.0014212017162));
#95269=CARTESIAN_POINT('Ctrl Pts',(2.22398395969949,2.05766150481967,15.1604861055623));
#95270=CARTESIAN_POINT('Ctrl Pts',(-0.528151023927718,2.98347649854016,
15.3195510094085));
#95271=CARTESIAN_POINT('Ctrl Pts',(-2.79520915110406,1.16913699924407,15.4786159132546));
#95272=CARTESIAN_POINT('Ctrl Pts',(-2.49502570018633,-1.71898873667837,
15.6376808171008));
#95273=CARTESIAN_POINT('Ctrl Pts',(0.0966978000338692,-3.02832050101801,
15.7967457209469));
#95274=CARTESIAN_POINT('Ctrl Pts',(2.59960983773466,-1.55631109132156,15.9558106247931));
#95275=CARTESIAN_POINT('Ctrl Pts',(2.71492720846078,1.34508206968077,16.1148755286393));
#95276=CARTESIAN_POINT('Ctrl Pts',(0.336737426669731,3.0110933939181,16.2739404324854));
#95277=CARTESIAN_POINT('Ctrl Pts',(-2.35072664406156,1.91158566805583,16.4330053363316));
#95278=CARTESIAN_POINT('Ctrl Pts',(-2.87918119059149,-0.943605422388776,
16.5920702401777));
#95279=CARTESIAN_POINT('Ctrl Pts',(-0.763270588118764,-2.93214827911724,
16.7511351440239));
#95280=CARTESIAN_POINT('Ctrl Pts',(2.0536608980259,-2.22767871052736,16.91020004787));
#95281=CARTESIAN_POINT('Ctrl Pts',(2.98442095308616,0.52278781182965,17.0692649517162));
#95282=CARTESIAN_POINT('Ctrl Pts',(1.17415908702408,2.79310328483859,17.2283298555623));
#95283=CARTESIAN_POINT('Ctrl Pts',(-1.71450151936645,2.49811129886309,17.3873947594085));
#95284=CARTESIAN_POINT('Ctrl Pts',(-3.02848940959031,-0.0912546843550893,
17.5464596632546));
#95285=CARTESIAN_POINT('Ctrl Pts',(-1.56098099280365,-2.5968083990782,17.7055245671008));
#95286=CARTESIAN_POINT('Ctrl Pts',(1.34020021578723,-2.7173404098532,17.864589470947));
#95287=CARTESIAN_POINT('Ctrl Pts',(3.01048329441863,-0.342148879062476,
18.0236543747931));
#95288=CARTESIAN_POINT('Ctrl Pts',(1.9158076648487,2.34728705375469,18.1827192786393));
#95289=CARTESIAN_POINT('Ctrl Pts',(-0.938428994667144,2.88087253161005,
18.3417841824854));
#95290=CARTESIAN_POINT('Ctrl Pts',(-2.93077167667974,0.768539459357237,
18.5008490863316));
#95291=CARTESIAN_POINT('Ctrl Pts',(-2.23136626488662,-2.04965365692435,
18.6599139901777));
#95292=CARTESIAN_POINT('Ctrl Pts',(0.517422910876692,-2.98535576652387,
18.8189788940239));
#95293=CARTESIAN_POINT('Ctrl Pts',(2.79098839551245,-1.17917738170817,18.97804379787));
#95294=CARTESIAN_POINT('Ctrl Pts',(2.50118882744452,1.71000876339393,19.1371087017162));
#95295=CARTESIAN_POINT('Ctrl Pts',(-0.0858112738799978,3.02864853469207,
19.2961736055623));
#95296=CARTESIAN_POINT('Ctrl Pts',(-2.59399857148751,1.56564585156992,19.4552385094085));
#95297=CARTESIAN_POINT('Ctrl Pts',(-2.71974483293534,-1.33531403240542,
19.6143034132547));
#95298=CARTESIAN_POINT('Ctrl Pts',(-0.347559226150612,-3.009863469617,19.7733683171007));
#95299=CARTESIAN_POINT('Ctrl Pts',(2.34383988058696,-1.92002347266577,19.932433220947));
#95300=CARTESIAN_POINT('Ctrl Pts',(2.8825545660313,0.933249535370647,20.0914981247931));
#95301=CARTESIAN_POINT('Ctrl Pts',(0.773805847845303,2.92938560644681,20.2505630286393));
#95302=CARTESIAN_POINT('Ctrl Pts',(-2.04563979446034,2.23504661086466,20.4096279324854));
#95303=CARTESIAN_POINT('Ctrl Pts',(-2.98628093583334,-0.512056338400038,
20.5686928363316));
#95304=CARTESIAN_POINT('Ctrl Pts',(-1.18419186708488,-2.78886448995777,
20.7277577401777));
#95305=CARTESIAN_POINT('Ctrl Pts',(1.70551048327454,-2.50425827598873,20.8868226440239));
#95306=CARTESIAN_POINT('Ctrl Pts',(3.02879787580927,0.0803675861934736,
21.04588754787));
#95307=CARTESIAN_POINT('Ctrl Pts',(1.57030565255054,2.59118036403974,21.2049524517162));
#95308=CARTESIAN_POINT('Ctrl Pts',(-1.33042353532015,2.72214046993971,21.3640173555623));
#95309=CARTESIAN_POINT('Ctrl Pts',(-3.00923392151558,0.352968450455971,
21.5230822594085));
#95310=CARTESIAN_POINT('Ctrl Pts',(-1.92423307788785,-2.34038513569446,
21.6821471632546));
#95311=CARTESIAN_POINT('Ctrl Pts',(0.928067061231389,-2.8842272884214,21.8412120671008));
#95312=CARTESIAN_POINT('Ctrl Pts',(2.92799007289608,-0.779069736570111,
22.0002769709469));
#95313=CARTESIAN_POINT('Ctrl Pts',(2.23871973657225,2.04161932360058,22.1593418747931));
#95314=CARTESIAN_POINT('Ctrl Pts',(-0.506688111736351,2.98719645802588,
22.3184067786392));
#95315=CARTESIAN_POINT('Ctrl Pts',(-2.78673157503577,1.18920252695495,22.4774716824855));
#95316=CARTESIAN_POINT('Ctrl Pts',(-2.50731963457993,-1.70100669353983,
22.6365365863315));
#95317=CARTESIAN_POINT('Ctrl Pts',(0.0749236388810824,-3.02893743245946,
22.7956014901777));
#95318=CARTESIAN_POINT('Ctrl Pts',(2.58835378583897,-1.57496038069229,22.9546663940239));
#95319=CARTESIAN_POINT('Ctrl Pts',(2.72452731312732,1.32552874032994,23.11373129787));
#95320=CARTESIAN_POINT('Ctrl Pts',(0.3583765345043,3.00859465214809,23.2727962017162));
#95321=CARTESIAN_POINT('Ctrl Pts',(-2.33692283023767,1.92843646691595,23.4318611055623));
#95322=CARTESIAN_POINT('Ctrl Pts',(-2.88589069337668,-0.922881588991328,
23.5909260094085));
#95323=CARTESIAN_POINT('Ctrl Pts',(-0.784331108526694,-2.92658508053578,
23.7499909132546));
#95324=CARTESIAN_POINT('Ctrl Pts',(2.03759225733304,-2.24238563014344,23.9090558171008));
#95325=CARTESIAN_POINT('Ctrl Pts',(2.98810233014392,0.501318248227434,24.068120720947));
#95326=CARTESIAN_POINT('Ctrl Pts',(1.19420934513164,2.78458965763675,24.2271856247931));
#95327=CARTESIAN_POINT('Ctrl Pts',(-1.69649740873925,2.51037289332849,24.3862505286392));
#95328=CARTESIAN_POINT('Ctrl Pts',(-3.02906720419183,-0.0694794495295385,
24.5453154324854));
#95329=CARTESIAN_POINT('Ctrl Pts',(-1.57961002095801,-2.58551884601647,
24.7043803363315));
#95330=CARTESIAN_POINT('Ctrl Pts',(1.32062966324739,-2.72690535478744,24.8634452401778));
#95331=CARTESIAN_POINT('Ctrl Pts',(3.00794566357964,-0.363783460824903,
25.0225101440238));
#95332=CARTESIAN_POINT('Ctrl Pts',(1.9326336261712,2.33345297540141,25.1815750478701));
#95333=CARTESIAN_POINT('Ctrl Pts',(-0.91769313540187,2.88754477552359,25.3406399517161));
#95334=CARTESIAN_POINT('Ctrl Pts',(-2.92517063390475,0.78958994671838,25.4997048555623));
#95335=CARTESIAN_POINT('Ctrl Pts',(-2.24604427973561,-2.03355860866717,
25.6587697594085));
#95336=CARTESIAN_POINT('Ctrl Pts',(0.495946765220677,-2.98899854926102,
25.8178346632546));
#95337=CARTESIAN_POINT('Ctrl Pts',(2.78243874468022,-1.19921230544041,25.9768995671008));
#95338=CARTESIAN_POINT('Ctrl Pts',(2.51341804237085,1.69198264343994,26.135964470947));
#95339=CARTESIAN_POINT('Ctrl Pts',(-0.0640350357260733,3.02918719058709,
26.2950293747931));
#95340=CARTESIAN_POINT('Ctrl Pts',(-2.58267555373039,1.58425455832728,26.4540942786393));
#95341=CARTESIAN_POINT('Ctrl Pts',(-2.72927458723795,-1.31572631989881,
26.6131591824854));
#95342=CARTESIAN_POINT('Ctrl Pts',(-0.369189211950789,-3.00728695790684,
26.7722240863316));
#95343=CARTESIAN_POINT('Ctrl Pts',(2.32997558239507,-1.93682454209465,26.9312889901777));
#95344=CARTESIAN_POINT('Ctrl Pts',(2.8891895295186,0.912501717224372,27.0903538940239));
#95345=CARTESIAN_POINT('Ctrl Pts',(0.794846234156523,2.92374673757228,27.24941879787));
#95346=CARTESIAN_POINT('Ctrl Pts',(-2.02951839063349,2.2496956735296,27.4084837017162));
#95347=CARTESIAN_POINT('Ctrl Pts',(-2.989885112482,-0.490573680068375,27.5675486055623));
#95348=CARTESIAN_POINT('Ctrl Pts',(-1.20421139171946,-2.78027884311456,
27.7266135094085));
#95349=CARTESIAN_POINT('Ctrl Pts',(1.68746241222674,-2.51645507186982,27.8856784132547));
#95350=CARTESIAN_POINT('Ctrl Pts',(3.02929739125769,0.0585904150588297,
28.0447433171008));
#95351=CARTESIAN_POINT('Ctrl Pts',(1.58889397779588,2.57982391816599,28.203808220947));
#95352=CARTESIAN_POINT('Ctrl Pts',(-1.31081872612446,2.73163500282501,28.3628731247931));
#95353=CARTESIAN_POINT('Ctrl Pts',(-3.00661853725756,0.374593770418749,
28.5219380286392));
#95354=CARTESIAN_POINT('Ctrl Pts',(-1.9410092011477,-2.3264906624522,28.6810029324854));
#95355=CARTESIAN_POINT('Ctrl Pts',(0.907307351229441,-2.8908249500484,28.8400678363315));
#95356=CARTESIAN_POINT('Ctrl Pts',(2.92231339613825,-0.800099953860905,
28.9991327401777));
#95357=CARTESIAN_POINT('Ctrl Pts',(2.25333979972966,2.02547161628391,29.1581976440239));
#95358=CARTESIAN_POINT('Ctrl Pts',(-0.485199010128317,2.99076201694283,
29.31726254787));
#95359=CARTESIAN_POINT('Ctrl Pts',(-2.77810995991736,1.20920658781917,29.4763274517161));
#95360=CARTESIAN_POINT('Ctrl Pts',(-2.51948397201424,-1.68293672970218,
29.6353923555624));
#95361=CARTESIAN_POINT('Ctrl Pts',(0.0531456051164595,-3.02939780584758,
29.7944572594085));
#95362=CARTESIAN_POINT('Ctrl Pts',(2.57696394853534,-1.5935282643764,29.9535221632547));
#95363=CARTESIAN_POINT('Ctrl Pts',(2.73398659392343,1.30590689777805,30.1125870671008));
#95364=CARTESIAN_POINT('Ctrl Pts',(0.379997118769557,3.00594040379118,30.2716519709469));
#95365=CARTESIAN_POINT('Ctrl Pts',(-2.32299822683086,1.94518758981186,30.4307168747931));
#95366=CARTESIAN_POINT('Ctrl Pts',(-2.89245103182977,-0.902110054197515,
30.5897817786392));
#95367=CARTESIAN_POINT('Ctrl Pts',(-0.805351088859346,-2.92087061423309,
30.7488466824855));
#95368=CARTESIAN_POINT('Ctrl Pts',(2.02141829869142,-2.25697664656345,30.9079115863315));
#95369=CARTESIAN_POINT('Ctrl Pts',(2.99162925981065,0.479822772763149,31.0669764901778));
#95370=CARTESIAN_POINT('Ctrl Pts',(1.21419787760285,2.77593210209509,31.2260413940238));
#95371=CARTESIAN_POINT('Ctrl Pts',(-1.67840561048632,2.52250473301941,31.3851062978701));
#95372=CARTESIAN_POINT('Ctrl Pts',(-3.02948843403243,-0.0477006234883444,
31.5441712017161));
#95373=CARTESIAN_POINT('Ctrl Pts',(-1.59815740309777,-2.5740956540776,31.7032361055624));
#95374=CARTESIAN_POINT('Ctrl Pts',(1.30099085072732,-2.73632935293637,31.8623010094085));
#95375=CARTESIAN_POINT('Ctrl Pts',(3.00525255969833,-0.385399239547727,
32.0213659132547));
#95376=CARTESIAN_POINT('Ctrl Pts',(1.94935969458897,2.31949828681319,32.1804308171008));
#95377=CARTESIAN_POINT('Ctrl Pts',(-0.896909842918197,2.89406776960972,
32.339495720947));
#95378=CARTESIAN_POINT('Ctrl Pts',(-2.91941839651761,0.810599622188333,
32.4985606247931));
#95379=CARTESIAN_POINT('Ctrl Pts',(-2.26060620228232,-2.01735845095016,
32.6576255286393));
#95380=CARTESIAN_POINT('Ctrl Pts',(0.474444985340741,-2.99248683828391,
32.8166904324854));
#95381=CARTESIAN_POINT('Ctrl Pts',(2.77374527668334,-1.2191852449461,32.9757553363316));
#95382=CARTESIAN_POINT('Ctrl Pts',(2.52551734512674,1.67386906921698,33.1348202401777));
#95383=CARTESIAN_POINT('Ctrl Pts',(-0.0422554877644123,3.02956927551939,
33.2938851440239));
#95384=CARTESIAN_POINT('Ctrl Pts',(-2.57121904405865,1.60278137900572,33.45295004787));
#95385=CARTESIAN_POINT('Ctrl Pts',(-2.73866327229565,-1.29607060085328,
33.6120149517162));
#95386=CARTESIAN_POINT('Ctrl Pts',(-0.390800115301929,-3.00455500720112,
33.7710798555623));
#95387=CARTESIAN_POINT('Ctrl Pts',(2.31599085370575,-1.95352550200112,33.9301447594085));
#95388=CARTESIAN_POINT('Ctrl Pts',(2.8956751581654,0.891706734190801,34.0892096632547));
#95389=CARTESIAN_POINT('Ctrl Pts',(0.815845536892429,2.91795674768322,34.2482745671008));
#95390=CARTESIAN_POINT('Ctrl Pts',(-2.01329208617546,2.26422845516096,34.407339470947));
#95391=CARTESIAN_POINT('Ctrl Pts',(-2.99333474959216,-0.469065665233948,
34.5664043747931));
#95392=CARTESIAN_POINT('Ctrl Pts',(-1.22416867373741,-2.77154949074653,
34.7254692786393));
#95393=CARTESIAN_POINT('Ctrl Pts',(1.66932712054919,-2.52852179860413,34.8845341824854));
#95394=CARTESIAN_POINT('Ctrl Pts',(3.02964033004738,0.0368102155349702,
35.0435990863315));
#95395=CARTESIAN_POINT('Ctrl Pts',(1.60740017716258,2.56833412777138,35.2026639901778));
#95396=CARTESIAN_POINT('Ctrl Pts',(-1.29114616405084,2.74098834446158,35.3617288940238));
#95397=CARTESIAN_POINT('Ctrl Pts',(-3.00384774855298,0.396199728584597,
35.5207937978701));
#95398=CARTESIAN_POINT('Ctrl Pts',(-1.95768499859072,-2.31247593883919,
35.6798587017162));
#95399=CARTESIAN_POINT('Ctrl Pts',(0.88650074482376,-2.89727319230415,35.8389236055623));
#95400=CARTESIAN_POINT('Ctrl Pts',(2.91648567245169,-0.821088816024983,
35.9979885094085));
#95401=CARTESIAN_POINT('Ctrl Pts',(2.26784339349788,2.0092192175035,36.1570534132546));
#95402=CARTESIAN_POINT('Ctrl Pts',(-0.463684829820489,2.99417299099631,
36.3161183171008));
#95403=CARTESIAN_POINT('Ctrl Pts',(-2.76934475137816,1.22914814787788,36.4751832209469));
#95404=CARTESIAN_POINT('Ctrl Pts',(-2.53151808374568,-1.66477977915577,
36.6342481247931));
#95405=CARTESIAN_POINT('Ctrl Pts',(0.0313648243910064,-3.02970159738682,
36.7933130286392));
#95406=CARTESIAN_POINT('Ctrl Pts',(2.5654409145354,-1.61201378264736,36.9523779324855));
#95407=CARTESIAN_POINT('Ctrl Pts',(2.74330456192304,1.28621755622817,37.1114428363315));
#95408=CARTESIAN_POINT('Ctrl Pts',(0.401598061952563,3.00313078603868,37.2705077401778));
#95409=CARTESIAN_POINT('Ctrl Pts',(-2.30895355356834,1.96183817092069,37.4295726440238));
#95410=CARTESIAN_POINT('Ctrl Pts',(-2.8988618668636,-0.881291891634948,
37.5886375478701));
#95411=CARTESIAN_POINT('Ctrl Pts',(-0.826329442647554,-2.91500517557537,
37.7477024517162));
#95412=CARTESIAN_POINT('Ctrl Pts',(2.00513985809173,-2.27145100561495,37.9067673555623));
#95413=CARTESIAN_POINT('Ctrl Pts',(2.99500155978836,0.458302496483089,38.0658322594085));
#95414=CARTESIAN_POINT('Ctrl Pts',(1.23412365128147,2.76713106570055,38.2248971632546));
#95415=CARTESIAN_POINT('Ctrl Pts',(-1.66022705972667,2.53450619087203,38.3839620671008));
#95416=CARTESIAN_POINT('Ctrl Pts',(-3.0297530773398,-0.0259193319235489,
38.5430269709469));
#95417=CARTESIAN_POINT('Ctrl Pts',(-1.61662218055602,-2.5625394136972,38.7020918747932));
#95418=CARTESIAN_POINT('Ctrl Pts',(1.2812847933071,-2.74561191719758,38.8611567786392));
#95419=CARTESIAN_POINT('Ctrl Pts',(3.00240412197435,-0.406995097966519,
39.0202216824854));
#95420=CARTESIAN_POINT('Ctrl Pts',(1.9659850055742,2.30542370927227,39.1792865863316));
#95421=CARTESIAN_POINT('Ctrl Pts',(-0.876080191451438,2.90044117671153,
39.3383514901777));
#95422=CARTESIAN_POINT('Ctrl Pts',(-2.91351526183688,0.831567399830523,
39.4974163940239));
#95423=CARTESIAN_POINT('Ctrl Pts',(-2.27505127985805,-2.00105402111826,
39.6564812978701));
#95424=CARTESIAN_POINT('Ctrl Pts',(0.452918682609153,-2.99582045329171,
39.8155462017162));
#95425=CARTESIAN_POINT('Ctrl Pts',(2.764908440865,-1.23909516787493,39.9746111055624));
#95426=CARTESIAN_POINT('Ctrl Pts',(2.53748611033011,1.65566897696946,40.1336760094085));
#95427=CARTESIAN_POINT('Ctrl Pts',(-0.0204737557242954,3.02979476974,40.2927409132547));
#95428=CARTESIAN_POINT('Ctrl Pts',(-2.55962963463003,1.62122535600115,40.4518058171008));
#95429=CARTESIAN_POINT('Ctrl Pts',(-2.74791040283129,-1.2763478912228,40.6108707209469));
#95430=CARTESIAN_POINT('Ctrl Pts',(-0.412390819191514,-3.00166775870746,
40.7699356247932));
#95431=CARTESIAN_POINT('Ctrl Pts',(2.30188641735399,-1.97012548915508,40.9290005286392));
#95432=CARTESIAN_POINT('Ctrl Pts',(2.90201111674604,0.870865661109529,41.0880654324855));
#95433=CARTESIAN_POINT('Ctrl Pts',(0.836802670652721,2.91201593604942,41.2471303363315));
#95434=CARTESIAN_POINT('Ctrl Pts',(-1.99696171978245,2.27864420459642,41.4061952401778));
#95435=CARTESIAN_POINT('Ctrl Pts',(-2.9966296688609,-0.447533405591092,
41.5652601440238));
#95436=CARTESIAN_POINT('Ctrl Pts',(-1.24406268159784,-2.76267688405161,
41.7243250478701));
#95437=CARTESIAN_POINT('Ctrl Pts',(1.65110554560885,-2.54045783249339,41.8833899517162));
#95438=CARTESIAN_POINT('Ctrl Pts',(3.02982667445275,0.0150281133849578,
42.0424548555624));
#95439=CARTESIAN_POINT('Ctrl Pts',(1.62582329411232,2.55671158673385,42.2015197594085));
#95440=CARTESIAN_POINT('Ctrl Pts',(-1.27140686592381,2.75020001139901,42.3605846632546));
#95441=CARTESIAN_POINT('Ctrl Pts',(-3.00092169861683,0.417785208196757,
42.5196495671008));
#95442=CARTESIAN_POINT('Ctrl Pts',(-1.97425960828754,-2.29834168924068,
42.678714470947));
#95443=CARTESIAN_POINT('Ctrl Pts',(0.865648317454662,-2.90357168189545,
42.837779374793));
#95444=CARTESIAN_POINT('Ctrl Pts',(2.91050720305651,-0.842035238201733,
42.9968442786393));
#95445=CARTESIAN_POINT('Ctrl Pts',(2.28222976822325,1.99286296730443,43.1559091824854));
#95446=CARTESIAN_POINT('Ctrl Pts',(-0.442146682826039,2.99742920388172,
43.3149740863316));
#95447=CARTESIAN_POINT('Ctrl Pts',(-2.76043640246926,1.2490261764028,43.4740389901777));
#95448=CARTESIAN_POINT('Ctrl Pts',(-2.54342134776202,-1.64653678038715,
43.6331038940239));
#95449=CARTESIAN_POINT('Ctrl Pts',(0.00958242249811193,-3.0298487913746,
43.79216879787));
#95450=CARTESIAN_POINT('Ctrl Pts',(2.55378527943441,-1.63041598003669,43.9512337017162));
#95451=CARTESIAN_POINT('Ctrl Pts',(2.75248073550596,1.26646173337338,44.1102986055624));
#95452=CARTESIAN_POINT('Ctrl Pts',(0.423178247552346,3.00016594411002,44.2693635094084));
#95453=CARTESIAN_POINT('Ctrl Pts',(-2.29478953637709,1.97838734962128,44.4284284132547));
#95454=CARTESIAN_POINT('Ctrl Pts',(-2.9051228671307,-0.860428177350863,
44.5874933171007));
#95455=CARTESIAN_POINT('Ctrl Pts',(-0.847265085550273,-2.90898906771414,
44.746558220947));
#95456=CARTESIAN_POINT('Ctrl Pts',(1.98875777688018,-2.28580795918964,44.9056231247931));
#95457=CARTESIAN_POINT('Ctrl Pts',(2.9982190558569,0.436758531780793,45.0646880286392));
#95458=CARTESIAN_POINT('Ctrl Pts',(1.25398563609222,2.75818700323134,45.2237529324854));
#95459=CARTESIAN_POINT('Ctrl Pts',(-1.6419626957523,2.54637664679984,45.3828178363316));
#95460=CARTESIAN_POINT('Ctrl Pts',(-3.02986112102816,-0.00413670110889247,
45.5418827401778));
#95461=CARTESIAN_POINT('Ctrl Pts',(-1.63500339780443,-2.55085072132126,
45.7009476440238));
#95462=CARTESIAN_POINT('Ctrl Pts',(1.26151250738515,-2.75475256943221,45.8600125478701));
#95463=CARTESIAN_POINT('Ctrl Pts',(2.99940050175171,-0.428569916692723,
46.0190774517161));
#95464=CARTESIAN_POINT('Ctrl Pts',(1.98250869195646,2.29122996424191,46.1781423555624));
#95465=CARTESIAN_POINT('Ctrl Pts',(-0.855205242657951,2.90666467887914,
46.3372072594085));
#95466=CARTESIAN_POINT('Ctrl Pts',(-2.90746156354653,0.85249217398433,46.4962721632546));
#95467=CARTESIAN_POINT('Ctrl Pts',(-2.28937871134263,-1.98464612015039,
46.6553370671008));
#95468=CARTESIAN_POINT('Ctrl Pts',(0.431368865721828,-2.99899930162892,
46.8144019709469));
#95469=CARTESIAN_POINT('Ctrl Pts',(2.75592889225626,-1.25894089319667,46.9734668747932));
#95470=CARTESIAN_POINT('Ctrl Pts',(2.54932334112256,1.63738301758705,47.1325317786392));
#95471=CARTESIAN_POINT('Ctrl Pts',(0.00130975603039247,3.02986421445121,
47.2915966824855));
#95472=CARTESIAN_POINT('Ctrl Pts',(-2.54790930072394,1.6395844813907,47.4506615863315));
#95473=CARTESIAN_POINT('Ctrl Pts',(-2.75701287562081,-1.25655719872552,
47.6097264901778));
#95474=CARTESIAN_POINT('Ctrl Pts',(-0.433965215459717,-2.9986291990659,
47.7687913940238));
#95475=CARTESIAN_POINT('Ctrl Pts',(2.28767255498402,-1.98661632552086,47.9278562978701));
#95476=CARTESIAN_POINT('Ctrl Pts',(2.90817885570603,0.849965611921472,48.0869212017162));
#95477=CARTESIAN_POINT('Ctrl Pts',(0.857751311695834,2.90595124535929,48.2459861055623));
#95478=CARTESIAN_POINT('Ctrl Pts',(-1.98059444140463,2.29289136777236,48.4050510094085));
#95479=CARTESIAN_POINT('Ctrl Pts',(-2.99964321327916,-0.42588109111496,
48.5641159132546));
#95480=CARTESIAN_POINT('Ctrl Pts',(-1.2641337121924,-2.75384638943867,48.7231808171008));
#95481=CARTESIAN_POINT('Ctrl Pts',(1.63325937176812,-2.55190963616655,48.8822457209469));
#95482=CARTESIAN_POINT('Ctrl Pts',(3.02897398663527,-0.00742973453303311,
49.0413106247932));
#95483=CARTESIAN_POINT('Ctrl Pts',(1.6458766818748,2.54625983835977,49.2003755286392));
#95484=CARTESIAN_POINT('Ctrl Pts',(-1.25514248441462,2.75664882626259,49.3594404324855));
#95485=CARTESIAN_POINT('Ctrl Pts',(-2.41099946670181,1.21592263637295,49.4654837017162));
#95486=CARTESIAN_POINT('Ctrl Pts',(-2.53475666268534,0.371481747532844,
49.5185053363316));
#95487=CARTESIAN_POINT('Ctrl Pts',(1.37702479013074,-1.93106208855785,0.));
#95488=CARTESIAN_POINT('Ctrl Pts',(2.02034799762934,-1.47231350142485,0.0530216346153847));
#95489=CARTESIAN_POINT('Ctrl Pts',(2.80114700154351,0.130837301153735,0.159064903846153));
#95490=CARTESIAN_POINT('Ctrl Pts',(1.40206621881702,2.43167759018441,0.318129807692308));
#95491=CARTESIAN_POINT('Ctrl Pts',(-1.28595649275605,2.49200065724321,0.477194711538461));
#95492=CARTESIAN_POINT('Ctrl Pts',(-2.79225776863625,0.267148017737648,
0.636259615384617));
#95493=CARTESIAN_POINT('Ctrl Pts',(-1.73436552900908,-2.20492577360607,
0.795324519230768));
#95494=CARTESIAN_POINT('Ctrl Pts',(0.916620294059412,-2.65092658244327,
0.954389423076924));
#95495=CARTESIAN_POINT('Ctrl Pts',(2.72564945922899,-0.662711191614906,
1.11345432692308));
#95496=CARTESIAN_POINT('Ctrl Pts',(2.03137230801958,1.93443429127041,1.27251923076923));
#95497=CARTESIAN_POINT('Ctrl Pts',(-0.528630951316314,2.75477110121152,
1.43158413461539));
#95498=CARTESIAN_POINT('Ctrl Pts',(-2.60310320693535,1.04507986133772,1.59064903846154));
#95499=CARTESIAN_POINT('Ctrl Pts',(-2.2867793378059,-1.62449666070042,1.7497139423077));
#95500=CARTESIAN_POINT('Ctrl Pts',(0.12982574190393,-2.80204465094187,1.90877884615384));
#95501=CARTESIAN_POINT('Ctrl Pts',(2.42719129243389,-1.40608362715869,2.06784375));
#95502=CARTESIAN_POINT('Ctrl Pts',(2.49531987128246,1.28129126381962,2.22690865384615));
#95503=CARTESIAN_POINT('Ctrl Pts',(0.271637692292844,2.79186965803179,2.38597355769231));
#95504=CARTESIAN_POINT('Ctrl Pts',(-2.20152807269878,1.73827513461474,2.54503846153846));
#95505=CARTESIAN_POINT('Ctrl Pts',(-2.65271491172666,-0.911827625924829,
2.70410336538462));
#95506=CARTESIAN_POINT('Ctrl Pts',(-0.667532999398916,-2.7244678431737,
2.86316826923077));
#95507=CARTESIAN_POINT('Ctrl Pts',(1.93074019393295,-2.03483859399145,3.02223317307692));
#95508=CARTESIAN_POINT('Ctrl Pts',(2.75573769451142,0.523674979307748,3.18129807692308));
#95509=CARTESIAN_POINT('Ctrl Pts',(1.04974590737629,2.60122262971082,3.34036298076923));
#95510=CARTESIAN_POINT('Ctrl Pts',(-1.62037814252565,2.28969438653921,3.49942788461539));
#95511=CARTESIAN_POINT('Ctrl Pts',(-2.80227647964017,-0.124788719351607,
3.65849278846154));
#95512=CARTESIAN_POINT('Ctrl Pts',(-1.41044229536976,-2.42466043275193,
3.8175576923077));
#95513=CARTESIAN_POINT('Ctrl Pts',(1.27680339699028,-2.49761862144671,3.97662259615385));
#95514=CARTESIAN_POINT('Ctrl Pts',(2.79137735375039,-0.276655306861728,
4.1356875));
#95515=CARTESIAN_POINT('Ctrl Pts',(1.74222902142711,2.19840026511027,4.29475240384616));
#95516=CARTESIAN_POINT('Ctrl Pts',(-0.907058170011317,2.65434948083033,
4.45381730769232));
#95517=CARTESIAN_POINT('Ctrl Pts',(-2.72326371290543,0.672428761754554,
4.61288221153846));
#95518=CARTESIAN_POINT('Ctrl Pts',(-2.03830549522154,-1.92707975904121,
4.77194711538462));
#95519=CARTESIAN_POINT('Ctrl Pts',(0.518721084171678,-2.75667446873791,
4.93101201923077));
#95520=CARTESIAN_POINT('Ctrl Pts',(2.59933167366719,-1.05441952748531,5.09007692307692));
#95521=CARTESIAN_POINT('Ctrl Pts',(2.29260307415327,1.61626013811133,5.24914182692309));
#95522=CARTESIAN_POINT('Ctrl Pts',(-0.119751836615735,2.80249624215965,
5.40820673076923));
#95523=CARTESIAN_POINT('Ctrl Pts',(-2.42212145562652,1.41479798694797,5.5672716346154));
#95524=CARTESIAN_POINT('Ctrl Pts',(-2.4999094523197,-1.27231223364438,5.72633653846154));
#95525=CARTESIAN_POINT('Ctrl Pts',(-0.281671949479292,-2.79087559782923,
5.8854014423077));
#95526=CARTESIAN_POINT('Ctrl Pts',(2.19526531462978,-1.74617750760439,6.04446634615385));
#95527=CARTESIAN_POINT('Ctrl Pts',(2.65597549661169,0.902285903180645,6.20353125));
#95528=CARTESIAN_POINT('Ctrl Pts',(0.677322340573879,2.7220507226428,6.36259615384616));
#95529=CARTESIAN_POINT('Ctrl Pts',(-1.92341309285148,2.04176584453944,6.52166105769231));
#95530=CARTESIAN_POINT('Ctrl Pts',(-2.75760234068335,-0.513765530507972,
6.68072596153848));
#95531=CARTESIAN_POINT('Ctrl Pts',(-1.05908973969091,-2.5974323115265,6.83979086538461));
#95532=CARTESIAN_POINT('Ctrl Pts',(1.61213691155191,-2.29550436028606,6.99885576923078));
#95533=CARTESIAN_POINT('Ctrl Pts',(2.80270695172092,0.114714569500639,7.15792067307693));
#95534=CARTESIAN_POINT('Ctrl Pts',(1.41914910781753,2.41957465259107,7.31698557692308));
#95535=CARTESIAN_POINT('Ctrl Pts',(-1.26781695999829,2.50219220796908,7.47605048076923));
#95536=CARTESIAN_POINT('Ctrl Pts',(-2.7903648261082,0.286687681804811,7.6351153846154));
#95537=CARTESIAN_POINT('Ctrl Pts',(-1.75012035275872,-2.19212327220441,
7.79418028846153));
#95538=CARTESIAN_POINT('Ctrl Pts',(0.897510721516925,-2.65759293241885,
7.9532451923077));
#95539=CARTESIAN_POINT('Ctrl Pts',(2.72082893886257,-0.682213731266401,
8.11231009615385));
#95540=CARTESIAN_POINT('Ctrl Pts',(2.04521959797142,1.91974021308981,8.27137500000001));
#95541=CARTESIAN_POINT('Ctrl Pts',(-0.508808317133133,2.75852130426731,
8.43043990384615));
#95542=CARTESIAN_POINT('Ctrl Pts',(-2.59552455843741,1.06375653052225,8.58950480769233));
#95543=CARTESIAN_POINT('Ctrl Pts',(-2.29839823084021,-1.60800847701467,
8.74856971153845));
#95544=CARTESIAN_POINT('Ctrl Pts',(0.109676931802227,-2.80290860719912,
8.90763461538463));
#95545=CARTESIAN_POINT('Ctrl Pts',(2.41702003317145,-1.42349564415503,9.06669951923077));
#95546=CARTESIAN_POINT('Ctrl Pts',(2.50446688033972,1.26331759069596,9.22576442307694));
#95547=CARTESIAN_POINT('Ctrl Pts',(0.291702487991934,2.78984504017334,9.38482932692308));
#95548=CARTESIAN_POINT('Ctrl Pts',(-2.18897414817153,1.75405754418639,9.54389423076923));
#95549=CARTESIAN_POINT('Ctrl Pts',(-2.65920178292864,-0.892732640463869,
9.7029591346154));
#95550=CARTESIAN_POINT('Ctrl Pts',(-0.687102918082009,-2.71959836550246,
9.86202403846154));
#95551=CARTESIAN_POINT('Ctrl Pts',(1.91606113164826,-2.04866674436504,10.0210889423077));
#95552=CARTESIAN_POINT('Ctrl Pts',(2.75943135650696,0.503849460063841,10.1801538461539));
#95553=CARTESIAN_POINT('Ctrl Pts',(1.06841988491078,2.59360842056154,10.33921875));
#95554=CARTESIAN_POINT('Ctrl Pts',(-1.60387484784032,2.30128467646784,10.4982836538462));
#95555=CARTESIAN_POINT('Ctrl Pts',(-2.80310120794078,-0.104638939794822,
10.6573485576923));
#95556=CARTESIAN_POINT('Ctrl Pts',(-1.4278375819202,-2.4144576056201,10.8164134615385));
#95557=CARTESIAN_POINT('Ctrl Pts',(1.25881414027309,-2.50673346208347,10.9754783653846));
#95558=CARTESIAN_POINT('Ctrl Pts',(2.78931624170351,-0.296716351840369,
11.1345432692308));
#95559=CARTESIAN_POINT('Ctrl Pts',(1.75798906916851,2.18581795270431,11.2936081730769));
#95560=CARTESIAN_POINT('Ctrl Pts',(-0.887951675457031,2.66080204294372,
11.4526730769231));
#95561=CARTESIAN_POINT('Ctrl Pts',(-2.71835900653777,0.691989885226263,
11.6117379807692));
#95562=CARTESIAN_POINT('Ctrl Pts',(-2.05210727258437,-1.91237586041207,
11.7708028846154));
#95563=CARTESIAN_POINT('Ctrl Pts',(0.498888975319622,-2.76033249446239,
11.9298677884616));
#95564=CARTESIAN_POINT('Ctrl Pts',(2.59168390408889,-1.07307978779166,12.0889326923077));
#95565=CARTESIAN_POINT('Ctrl Pts',(2.30416368784436,1.59973603738241,12.2479975961539));
#95566=CARTESIAN_POINT('Ctrl Pts',(-0.0996006097535288,2.80328475332372,
12.4070625));
#95567=CARTESIAN_POINT('Ctrl Pts',(-2.41188737821489,1.43217490708647,12.5661274038462));
#95568=CARTESIAN_POINT('Ctrl Pts',(-2.50899194587818,-1.25430662327794,
12.7251923076923));
#95569=CARTESIAN_POINT('Ctrl Pts',(-0.301729257152967,-2.78877843240699,
12.8842572115385));
#95570=CARTESIAN_POINT('Ctrl Pts',(2.18265469599876,-1.76191491500441,13.0433221153847));
#95571=CARTESIAN_POINT('Ctrl Pts',(2.66239370729449,0.88316784194122,13.2023870192308));
#95572=CARTESIAN_POINT('Ctrl Pts',(0.696874616911946,2.71711086597222,13.361451923077));
#95573=CARTESIAN_POINT('Ctrl Pts',(-1.90868441128639,2.05554117151489,13.5205168269231));
#95574=CARTESIAN_POINT('Ctrl Pts',(-2.76122471522252,-0.493926878925183,
13.6795817307693));
#95575=CARTESIAN_POINT('Ctrl Pts',(-1.07773622411112,-2.58975101523663,
13.8386466346154));
#95576=CARTESIAN_POINT('Ctrl Pts',(1.59559205901132,-2.30703525566917,13.9977115384616));
#95577=CARTESIAN_POINT('Ctrl Pts',(2.80345924275497,0.094561957954597,14.1567764423077));
#95578=CARTESIAN_POINT('Ctrl Pts',(1.43650760564222,2.40930935925889,14.3158413461539));
#95579=CARTESIAN_POINT('Ctrl Pts',(-1.24979505427195,2.51124232442785,14.47490625));
#95580=CARTESIAN_POINT('Ctrl Pts',(-2.78823161402115,0.306741187735644,
14.6339711538462));
#95581=CARTESIAN_POINT('Ctrl Pts',(-1.76583506901173,-2.17948438827371,
14.7930360576923));
#95582=CARTESIAN_POINT('Ctrl Pts',(0.878381155370515,-2.66397677083911,
14.9521009615385));
#95583=CARTESIAN_POINT('Ctrl Pts',(2.7158539478379,-0.701757097359029,15.1111658653846));
#95584=CARTESIAN_POINT('Ctrl Pts',(2.05896843006344,1.90498679619639,15.2702307692308));
#95585=CARTESIAN_POINT('Ctrl Pts',(-0.488963186910485,2.76210801590502,
15.429295673077));
#95586=CARTESIAN_POINT('Ctrl Pts',(-2.58780976024888,1.08238917882668,15.5883605769231));
#95587=CARTESIAN_POINT('Ctrl Pts',(-2.30989937066573,-1.59144292611408,
15.7474254807692));
#95588=CARTESIAN_POINT('Ctrl Pts',(0.0895230006752742,-2.80362467567087,
15.9064903846154));
#95589=CARTESIAN_POINT('Ctrl Pts',(2.40672355708034,-1.44083566359076,16.0655552884616));
#95590=CARTESIAN_POINT('Ctrl Pts',(2.5134845904627,1.24527944782968,16.2246201923077));
#95591=CARTESIAN_POINT('Ctrl Pts',(0.311752127397432,2.78767578831249,16.3836850961539));
#95592=CARTESIAN_POINT('Ctrl Pts',(-2.17630703977077,1.76974951852646,16.54275));
#95593=CARTESIAN_POINT('Ctrl Pts',(-2.66555122846353,-0.873591631208197,
16.7018149038462));
#95594=CARTESIAN_POINT('Ctrl Pts',(-0.706637310794764,-2.71458825619525,
16.8608798076923));
#95595=CARTESIAN_POINT('Ctrl Pts',(1.9012830270871,-2.06238903715836,17.0199447115385));
#95596=CARTESIAN_POINT('Ctrl Pts',(2.76298239365644,0.483997915310618,17.1790096153846));
#95597=CARTESIAN_POINT('Ctrl Pts',(1.08703863690706,2.58586014539682,17.3380745192308));
#95598=CARTESIAN_POINT('Ctrl Pts',(-1.58728865209436,2.31275602358159,17.4971394230769));
#95599=CARTESIAN_POINT('Ctrl Pts',(-2.80378105153698,-0.0844837541937897,
17.6562043269231));
#95600=CARTESIAN_POINT('Ctrl Pts',(-1.44515906695039,-2.4041299800326,17.8152692307692));
#95601=CARTESIAN_POINT('Ctrl Pts',(1.24075981853869,-2.51571873673912,17.9743341346154));
#95602=CARTESIAN_POINT('Ctrl Pts',(2.78711095707658,-0.316762059950613,
18.1333990384615));
#95603=CARTESIAN_POINT('Ctrl Pts',(1.77365825090308,2.17312266075431,18.2924639423077));
#95604=CARTESIAN_POINT('Ctrl Pts',(-0.868799284926716,2.66711707508149,
18.4515288461538));
#95605=CARTESIAN_POINT('Ctrl Pts',(-2.71331379513307,0.711515241453737,
18.61059375));
#95606=CARTESIAN_POINT('Ctrl Pts',(-2.06580298174944,-1.8975731159235,18.7696586538462));
#95607=CARTESIAN_POINT('Ctrl Pts',(0.479031080165797,-2.76384784565209,
18.9287235576923));
#95608=CARTESIAN_POINT('Ctrl Pts',(2.58390217697866,-1.09168458333227,19.0877884615385));
#95609=CARTESIAN_POINT('Ctrl Pts',(2.31560520518838,1.58312925037248,19.2468533653847));
#95610=CARTESIAN_POINT('Ctrl Pts',(-0.0794442347893398,2.80392836984813,
19.4059182692308));
#95611=CARTESIAN_POINT('Ctrl Pts',(-2.40152863649417,1.44947780175445,19.5649831730769));
#95612=CARTESIAN_POINT('Ctrl Pts',(-2.51794475603978,-1.2362361809995,19.7240480769231));
#95613=CARTESIAN_POINT('Ctrl Pts',(-0.321770969210761,-2.78653712213808,
19.8831129807692));
#95614=CARTESIAN_POINT('Ctrl Pts',(2.16993126151137,-1.77756125351454,20.0421778846154));
#95615=CARTESIAN_POINT('Ctrl Pts',(2.66867430563458,0.864004132007661,20.2012427884615));
#95616=CARTESIAN_POINT('Ctrl Pts',(0.716390873577828,2.7120305687685,20.3603076923077));
#95617=CARTESIAN_POINT('Ctrl Pts',(-1.8938570746904,2.06921025280796,20.5193725961538));
#95618=CARTESIAN_POINT('Ctrl Pts',(-2.76470436909614,-0.474062697521268,
20.6784375));
#95619=CARTESIAN_POINT('Ctrl Pts',(-1.09632700309372,-2.58193586131958,
20.8375024038462));
#95620=CARTESIAN_POINT('Ctrl Pts',(1.5789647343853,-2.31844690628189,20.9965673076923));
#95621=CARTESIAN_POINT('Ctrl Pts',(2.80406663012842,0.0744044587420362,
21.1556322115385));
#95622=CARTESIAN_POINT('Ctrl Pts',(1.4537918540513,2.39891953486867,21.3146971153846));
#95623=CARTESIAN_POINT('Ctrl Pts',(-1.23170854982573,2.52016264117351,21.4737620192308));
#95624=CARTESIAN_POINT('Ctrl Pts',(-2.7859542853508,0.326778838996557,21.6328269230769));
#95625=CARTESIAN_POINT('Ctrl Pts',(-1.78145851375219,-2.16673285235174,
21.7918918269231));
#95626=CARTESIAN_POINT('Ctrl Pts',(0.859206187941647,-2.67022291509215,
21.9509567307692));
#95627=CARTESIAN_POINT('Ctrl Pts',(2.71073858124696,-0.721264191416516,
22.1100216346154));
#95628=CARTESIAN_POINT('Ctrl Pts',(2.07261083932685,1.89013491539238,22.2690865384616));
#95629=CARTESIAN_POINT('Ctrl Pts',(-0.469092783427355,2.76555196122163,
22.4281514423077));
#95630=CARTESIAN_POINT('Ctrl Pts',(-2.57996120477168,1.1009658811941,22.5872163461539));
#95631=CARTESIAN_POINT('Ctrl Pts',(-2.32128111768206,-1.57479511758614,
22.74628125));
#95632=CARTESIAN_POINT('Ctrl Pts',(0.0693644423326341,-2.8041958319312,
22.9053461538462));
#95633=CARTESIAN_POINT('Ctrl Pts',(2.39630268358469,-1.45810120990461,23.0644110576923));
#95634=CARTESIAN_POINT('Ctrl Pts',(2.52237238497556,1.22717693964369,23.2234759615385));
#95635=CARTESIAN_POINT('Ctrl Pts',(0.331785653130296,2.78536244859756,23.3825408653846));
#95636=CARTESIAN_POINT('Ctrl Pts',(-2.16352744360781,1.78535001902604,23.5416057692308));
#95637=CARTESIAN_POINT('Ctrl Pts',(-2.67176289845148,-0.854405468228408,
23.7006706730769));
#95638=CARTESIAN_POINT('Ctrl Pts',(-0.726135179226555,-2.70943783674216,
23.8597355769231));
#95639=CARTESIAN_POINT('Ctrl Pts',(1.88640665005374,-2.07600473032059,24.0188004807692));
#95640=CARTESIAN_POINT('Ctrl Pts',(2.76639061929044,0.464121353939118,24.1778653846154));
#95641=CARTESIAN_POINT('Ctrl Pts',(1.10560120264771,2.57797821371406,24.3369302884615));
#95642=CARTESIAN_POINT('Ctrl Pts',(-1.57062041344493,2.32410783023306,24.4959951923077));
#95643=CARTESIAN_POINT('Ctrl Pts',(-2.8043159748391,-0.0643242018429354,
24.6550600961538));
#95644=CARTESIAN_POINT('Ctrl Pts',(-1.46240585539294,-2.39367809109597,
24.8141250000001));
#95645=CARTESIAN_POINT('Ctrl Pts',(1.2226413650927,-2.52457398030731,24.9731899038461));
#95646=CARTESIAN_POINT('Ctrl Pts',(2.78476161379025,-0.336791395437584,
25.1322548076924));
#95647=CARTESIAN_POINT('Ctrl Pts',(1.78923575676476,2.16031504563452,25.2913197115385));
#95648=CARTESIAN_POINT('Ctrl Pts',(-0.849601988376427,2.6732942507377,25.4503846153846));
#95649=CARTESIAN_POINT('Ctrl Pts',(-2.70812833945618,0.731003821272407,
25.6094495192308));
#95650=CARTESIAN_POINT('Ctrl Pts',(-2.07939191482527,-1.88267229071865,
25.7685144230769));
#95651=CARTESIAN_POINT('Ctrl Pts',(0.459148425116812,-2.76722034059328,
25.9275793269231));
#95652=CARTESIAN_POINT('Ctrl Pts',(2.57598689455279,-1.11023295248012,26.0866442307693));
#95653=CARTESIAN_POINT('Ctrl Pts',(2.32692703480318,1.56644063544793,26.2457091346154));
#95654=CARTESIAN_POINT('Ctrl Pts',(-0.0592837535552358,2.80442705846396,
26.4047740384616));
#95655=CARTESIAN_POINT('Ctrl Pts',(-2.39104576588115,1.46670577661039,26.5638389423077));
#95656=CARTESIAN_POINT('Ctrl Pts',(-2.52676742005664,-1.21810184082479,
26.7229038461538));
#95657=CARTESIAN_POINT('Ctrl Pts',(-0.34179604974745,-2.78415178286989,
26.8819687500001));
#95658=CARTESIAN_POINT('Ctrl Pts',(2.15709566880955,-1.79311571441545,27.0410336538462));
#95659=CARTESIAN_POINT('Ctrl Pts',(2.67481696700378,0.844795763903405,27.2000985576923));
#95660=CARTESIAN_POINT('Ctrl Pts',(0.73587010182595,2.70681009361926,27.3591634615385));
#95661=CARTESIAN_POINT('Ctrl Pts',(-1.87893184945079,2.08277238189867,27.5182283653846));
#95662=CARTESIAN_POINT('Ctrl Pts',(-2.76804112244977,-0.454174013025224,
27.6772932692308));
#95663=CARTESIAN_POINT('Ctrl Pts',(-1.1148611157287,-2.57398725372069,27.8363581730769));
#95664=CARTESIAN_POINT('Ctrl Pts',(1.56225579709783,-2.32973872228513,27.9954230769231));
#95665=CARTESIAN_POINT('Ctrl Pts',(2.80452908244698,0.0542431137526706,
28.1544879807693));
#95666=CARTESIAN_POINT('Ctrl Pts',(1.47100095966601,2.38840571644395,28.3135528846154));
#95667=CARTESIAN_POINT('Ctrl Pts',(-1.21355838150491,2.52895269713762,28.4726177884615));
#95668=CARTESIAN_POINT('Ctrl Pts',(-2.78353295780648,0.34679959989242,28.6316826923077));
#95669=CARTESIAN_POINT('Ctrl Pts',(-1.79698987944403,-2.15386932353293,
28.7907475961538));
#95670=CARTESIAN_POINT('Ctrl Pts',(0.839986810335585,-2.67633104233065,
28.9498125000001));
#95671=CARTESIAN_POINT('Ctrl Pts',(2.70548310349,-0.740734005166865,29.1088774038461));
#95672=CARTESIAN_POINT('Ctrl Pts',(2.08614612062029,1.87518533833364,29.2679423076924));
#95673=CARTESIAN_POINT('Ctrl Pts',(-0.449198133734217,2.7688529622084,29.4270072115385));
#95674=CARTESIAN_POINT('Ctrl Pts',(-2.57197929767765,1.11948567744212,29.5860721153846));
#95675=CARTESIAN_POINT('Ctrl Pts',(-2.33254288359573,-1.55806591191366,
29.7451370192308));
#95676=CARTESIAN_POINT('Ctrl Pts',(0.0492022987188458,-2.80462204645853,
29.9042019230769));
#95677=CARTESIAN_POINT('Ctrl Pts',(2.38575795131293,-1.47529139068443,30.0632668269231));
#95678=CARTESIAN_POINT('Ctrl Pts',(2.53112980449082,1.20901100181045,30.2223317307692));
#95679=CARTESIAN_POINT('Ctrl Pts',(0.351802029708706,2.78290514059918,30.3813966346154));
#95680=CARTESIAN_POINT('Ctrl Pts',(-2.15063602022738,1.80085823933508,30.5404615384615));
#95681=CARTESIAN_POINT('Ctrl Pts',(-2.67783647182709,-0.835175143208346,
30.6995264423077));
#95682=CARTESIAN_POINT('Ctrl Pts',(-0.74559551558228,-2.70414737335524,
30.8585913461539));
#95683=CARTESIAN_POINT('Ctrl Pts',(1.87143276947021,-2.08951312009126,31.01765625));
#95684=CARTESIAN_POINT('Ctrl Pts',(2.76965585724649,0.444220803318177,31.1767211538462));
#95685=CARTESIAN_POINT('Ctrl Pts',(1.12410662268099,2.56996303291023,31.3357860576923));
#95686=CARTESIAN_POINT('Ctrl Pts',(-1.55387099343073,2.33533950967628,31.4948509615385));
#95687=CARTESIAN_POINT('Ctrl Pts',(-2.80470595019833,-0.0441613247380469,
31.6539158653847));
#95688=CARTESIAN_POINT('Ctrl Pts',(-1.4795770558054,-2.38310247904171,31.8129807692308));
#95689=CARTESIAN_POINT('Ctrl Pts',(1.20445971643178,-2.53329873508307,31.972045673077));
#95690=CARTESIAN_POINT('Ctrl Pts',(2.78226833327609,-0.356803323035994,
32.1311105769231));
#95691=CARTESIAN_POINT('Ctrl Pts',(1.80472078159196,2.14739576933795,32.2901754807693));
#95692=CARTESIAN_POINT('Ctrl Pts',(-0.83036077806552,2.67933325062988,32.4492403846154));
#95693=CARTESIAN_POINT('Ctrl Pts',(-2.70280290752998,0.750454617367339,
32.6083052884616));
#95694=CARTESIAN_POINT('Ctrl Pts',(-2.09287336943466,-1.86767415498305,
32.7673701923077));
#95695=CARTESIAN_POINT('Ctrl Pts',(0.439242037856295,-2.77044980497037,
32.9264350961539));
#95696=CARTESIAN_POINT('Ctrl Pts',(2.56793846593204,-1.12872393651732,33.0855));
#95697=CARTESIAN_POINT('Ctrl Pts',(2.33812859149225,1.54967105520072,33.2445649038462));
#95698=CARTESIAN_POINT('Ctrl Pts',(-0.0391202080950587,2.80478079339528,
33.4036298076924));
#95699=CARTESIAN_POINT('Ctrl Pts',(-2.38043930820866,1.48385794118423,33.5626947115384));
#95700=CARTESIAN_POINT('Ctrl Pts',(-2.53545948190777,-1.19990454007159,
33.7217596153847));
#95701=CARTESIAN_POINT('Ctrl Pts',(-0.361803463717808,-2.78162253789443,
33.8808245192308));
#95702=CARTESIAN_POINT('Ctrl Pts',(2.14414858133226,-1.80857749373683,34.039889423077));
#95703=CARTESIAN_POINT('Ctrl Pts',(2.68082137390367,0.825543730459955,34.1989543269231));
#95704=CARTESIAN_POINT('Ctrl Pts',(0.755311294824669,2.70144971035752,34.3580192307693));
#95705=CARTESIAN_POINT('Ctrl Pts',(-1.86390950701438,2.09622685779518,34.5170841346154));
#95706=CARTESIAN_POINT('Ctrl Pts',(-2.77123480281515,-0.4342618534324,34.6761490384615));
#95707=CARTESIAN_POINT('Ctrl Pts',(-1.13333760403503,-2.56590560328329,
34.8352139423077));
#95708=CARTESIAN_POINT('Ctrl Pts',(1.54546611079131,-2.34091012003366,34.9942788461539));
#95709=CARTESIAN_POINT('Ctrl Pts',(2.80484657580764,0.0340789650750163,
35.15334375));
#95710=CARTESIAN_POINT('Ctrl Pts',(1.48813403299161,2.37776844741717,35.3124086538462));
#95711=CARTESIAN_POINT('Ctrl Pts',(-1.1953454874454,2.53761203798461,35.4714735576924));
#95712=CARTESIAN_POINT('Ctrl Pts',(-2.78096775654043,0.36680243560116,35.6305384615384));
#95713=CARTESIAN_POINT('Ctrl Pts',(-1.81242836331058,-2.14089446670025,
35.7896033653847));
#95714=CARTESIAN_POINT('Ctrl Pts',(0.820724015952912,-2.68230083684112,
35.9486682692308));
#95715=CARTESIAN_POINT('Ctrl Pts',(2.70008778620931,-0.760165532265031,
36.107733173077));
#95716=CARTESIAN_POINT('Ctrl Pts',(2.09957357433953,1.86013883772571,36.2667980769231));
#95717=CARTESIAN_POINT('Ctrl Pts',(-0.429280266134804,2.77201084824496,
36.4258629807693));
#95718=CARTESIAN_POINT('Ctrl Pts',(-2.5638644515312,1.13794761032974,36.5849278846154));
#95719=CARTESIAN_POINT('Ctrl Pts',(-2.34368408631476,-1.54125617378662,
36.7439927884616));
#95720=CARTESIAN_POINT('Ctrl Pts',(0.0290376119636847,-2.8049032972229,
36.9030576923078));
#95721=CARTESIAN_POINT('Ctrl Pts',(2.37508990529535,-1.49240531741365,37.0621225961539));
#95722=CARTESIAN_POINT('Ctrl Pts',(2.53975639635982,1.19078257328104,37.2211875));
#95723=CARTESIAN_POINT('Ctrl Pts',(0.371800222537135,2.78030399132932,37.3802524038462));
#95724=CARTESIAN_POINT('Ctrl Pts',(-2.13763343595425,1.81627337787318,37.5393173076923));
#95725=CARTESIAN_POINT('Ctrl Pts',(-2.68377163466288,-0.81590165011443,
37.6983822115385));
#95726=CARTESIAN_POINT('Ctrl Pts',(-0.765017314006785,-2.69871713948505,
37.8574471153846));
#95727=CARTESIAN_POINT('Ctrl Pts',(1.8563621592982,-2.10291350825614,38.0165120192308));
#95728=CARTESIAN_POINT('Ctrl Pts',(2.77277793875275,0.424297292056489,38.175576923077));
#95729=CARTESIAN_POINT('Ctrl Pts',(1.14255394050895,2.56181501726957,38.3346418269231));
#95730=CARTESIAN_POINT('Ctrl Pts',(-1.53704125778664,2.34645048137439,38.4937067307693));
#95731=CARTESIAN_POINT('Ctrl Pts',(-2.80495095745781,-0.0239961650468875,
38.6527716346154));
#95732=CARTESIAN_POINT('Ctrl Pts',(-1.49667178065217,-2.37240369049618,
38.8118365384616));
#95733=CARTESIAN_POINT('Ctrl Pts',(1.18621581231896,-2.54189255010612,38.9709014423077));
#95734=CARTESIAN_POINT('Ctrl Pts',(2.77963124440541,-0.376796808380384,
39.1299663461539));
#95735=CARTESIAN_POINT('Ctrl Pts',(1.82011252500328,2.13436549962901,39.28903125));
#95736=CARTESIAN_POINT('Ctrl Pts',(-0.811076648523027,2.68523376261753,
39.4480961538463));
#95737=CARTESIAN_POINT('Ctrl Pts',(-2.69733777461252,0.769866624376458,
39.6071610576923));
#95738=CARTESIAN_POINT('Ctrl Pts',(-2.10624664875555,-1.85257948393219,
39.7662259615385));
#95739=CARTESIAN_POINT('Ctrl Pts',(0.419312947294725,-2.77353607186051,
39.9252908653846));
#95740=CARTESIAN_POINT('Ctrl Pts',(2.55975730711914,-1.14715657969204,40.0843557692308));
#95741=CARTESIAN_POINT('Ctrl Pts',(2.34920929627571,1.53282137640764,40.243420673077));
#95742=CARTESIAN_POINT('Ctrl Pts',(-0.0189546406110363,2.80498955635841,
40.4024855769231));
#95743=CARTESIAN_POINT('Ctrl Pts',(-2.36970981169745,1.50093340892436,40.5615504807693));
#95744=CARTESIAN_POINT('Ctrl Pts',(-2.54402049232267,-1.18164521931195,
40.7206153846154));
#95745=CARTESIAN_POINT('Ctrl Pts',(-0.381792176989602,-2.77894951794198,
40.8796802884616));
#95746=CARTESIAN_POINT('Ctrl Pts',(2.13109066828147,-1.82394579229869,41.0387451923077));
#95747=CARTESIAN_POINT('Ctrl Pts',(2.68668721598173,0.806249026765786,41.1978100961539));
#95748=CARTESIAN_POINT('Ctrl Pts',(0.774713447708398,2.69594969604779,41.356875));
#95749=CARTESIAN_POINT('Ctrl Pts',(-1.84879082384766,2.10957298506999,41.5159399038462));
#95750=CARTESIAN_POINT('Ctrl Pts',(-2.77428524511908,-0.41432724795145,
41.6750048076923));
#95751=CARTESIAN_POINT('Ctrl Pts',(-1.15175551301023,-2.55769132772724,
41.8340697115385));
#95752=CARTESIAN_POINT('Ctrl Pts',(1.52859654328181,-2.35196052210647,41.9931346153846));
#95753=CARTESIAN_POINT('Ctrl Pts',(2.8050190938,0.0139130549425746,42.1521995192308));
#95754=CARTESIAN_POINT('Ctrl Pts',(1.50519018846317,2.36700827760163,42.311264423077));
#95755=CARTESIAN_POINT('Ctrl Pts',(-1.17707080902522,2.54614021613523,42.4703293269231));
#95756=CARTESIAN_POINT('Ctrl Pts',(-2.77825881414133,0.386786312227329,
42.6293942307692));
#95757=CARTESIAN_POINT('Ctrl Pts',(-1.82777316737607,-2.12780895249092,
42.7884591346155));
#95758=CARTESIAN_POINT('Ctrl Pts',(0.801418800438249,-2.68813199006011,
42.9475240384615));
#95759=CARTESIAN_POINT('Ctrl Pts',(2.69455290827499,-0.779557768345067,
43.1065889423078));
#95760=CARTESIAN_POINT('Ctrl Pts',(2.11289250645387,1.84499619128384,43.2656538461538));
#95761=CARTESIAN_POINT('Ctrl Pts',(-0.409340210132954,2.7750254561082,43.4247187500001));
#95762=CARTESIAN_POINT('Ctrl Pts',(-2.55561708576786,1.15635072560681,43.5837836538462));
#95763=CARTESIAN_POINT('Ctrl Pts',(-2.3547041499791,-1.5243667720576,43.7428485576924));
#95764=CARTESIAN_POINT('Ctrl Pts',(0.00887142432873881,-2.80503956968683,
43.9019134615385));
#95765=CARTESIAN_POINT('Ctrl Pts',(2.36429909693514,-1.50944210551781,44.0609783653846));
#95766=CARTESIAN_POINT('Ctrl Pts',(2.54825171469771,1.17249259623757,44.2200432692308));
#95767=CARTESIAN_POINT('Ctrl Pts',(0.391779197956932,2.77755913523241,44.3791081730769));
#95768=CARTESIAN_POINT('Ctrl Pts',(-2.12452036285295,1.8315946378757,44.5381730769232));
#95769=CARTESIAN_POINT('Ctrl Pts',(-2.68956808019675,-0.796585985153158,
44.6972379807693));
#95770=CARTESIAN_POINT('Ctrl Pts',(-0.784399570615147,-2.69314741578982,
44.8563028846154));
#95771=CARTESIAN_POINT('Ctrl Pts',(1.84119559845759,-2.11620520221519,45.0153677884616));
#95772=CARTESIAN_POINT('Ctrl Pts',(2.7757567025159,0.404351850010035,45.1744326923077));
#95773=CARTESIAN_POINT('Ctrl Pts',(1.16094220248601,2.55353458782659,45.3334975961539));
#95774=CARTESIAN_POINT('Ctrl Pts',(-1.52013207611093,2.35744017125017,45.4925625));
#95775=CARTESIAN_POINT('Ctrl Pts',(-2.80505098450271,-0.00382976547574787,
45.6516274038463));
#95776=CARTESIAN_POINT('Ctrl Pts',(-1.51368914530336,-2.36158227765018,
45.8106923076923));
#95777=CARTESIAN_POINT('Ctrl Pts',(1.16791059373771,-2.55035498271459,45.9697572115385));
#95778=CARTESIAN_POINT('Ctrl Pts',(2.77685048729278,-0.396770815138777,
46.1288221153846));
#95779=CARTESIAN_POINT('Ctrl Pts',(1.83541018417072,2.12122490443972,46.2878870192308));
#95780=CARTESIAN_POINT('Ctrl Pts',(-0.791750582632343,2.69099549234209,
46.446951923077));
#95781=CARTESIAN_POINT('Ctrl Pts',(-2.69173324962905,0.789238818677136,
46.6060168269231));
#95782=CARTESIAN_POINT('Ctrl Pts',(-2.11951101110941,-1.83738901911381,
46.7650817307693));
#95783=CARTESIAN_POINT('Ctrl Pts',(0.399362087284636,-2.7764790554831,46.9241466346154));
#95784=CARTESIAN_POINT('Ctrl Pts',(2.55144402454308,-1.16552978860435,47.0832115384616));
#95785=CARTESIAN_POINT('Ctrl Pts',(2.36016822626022,1.51589220166356,47.2422764423077));
#95786=CARTESIAN_POINT('Ctrl Pts',(0.00121257453600308,2.80505384839945,
47.4013413461539));
#95787=CARTESIAN_POINT('Ctrl Pts',(-2.35885910506479,1.51793032089209,47.56040625));
#95788=CARTESIAN_POINT('Ctrl Pts',(-2.55244757833081,-1.16332295988949,
47.7194711538462));
#95789=CARTESIAN_POINT('Ctrl Pts',(-0.401765792635603,-2.77613641385121,
47.8785360576923));
#95790=CARTESIAN_POINT('Ctrl Pts',(2.11793144842226,-1.83921303886061,48.0376009615385));
#95791=CARTESIAN_POINT('Ctrl Pts',(2.69239732002637,0.78689972288376,48.1966658653846));
#95792=CARTESIAN_POINT('Ctrl Pts',(0.794107738018986,2.69033499428045,48.3557307692309));
#95793=CARTESIAN_POINT('Ctrl Pts',(-1.83363796749767,2.12276303487646,48.5147956730769));
#95794=CARTESIAN_POINT('Ctrl Pts',(-2.77707519007022,-0.394281495485595,
48.6738605769232));
#95795=CARTESIAN_POINT('Ctrl Pts',(-1.17033730995746,-2.54951603961395,
48.8329254807692));
#95796=CARTESIAN_POINT('Ctrl Pts',(1.51207452279905,-2.36256262295682,48.9919903846154));
#95797=CARTESIAN_POINT('Ctrl Pts',(2.80422967385422,-0.00687846186160384,
49.1510552884616));
#95798=CARTESIAN_POINT('Ctrl Pts',(1.52375565164409,2.35733202978189,49.3101201923077));
#95799=CARTESIAN_POINT('Ctrl Pts',(-1.16201321478499,2.55211054076708,49.4691850961539));
#95800=CARTESIAN_POINT('Ctrl Pts',(-2.23210772954909,1.12570340751462,49.5752283653847));
#95801=CARTESIAN_POINT('Ctrl Pts',(-2.34668236863857,0.343918483395232,
49.62825));
#95802=CARTESIAN_POINT('',(1.37702479013102,-1.93106208855765,0.));
#95803=CARTESIAN_POINT('Ctrl Pts',(1.37702479013074,-1.93106208855785,0.));
#95804=CARTESIAN_POINT('Ctrl Pts',(2.02034799762934,-1.47231350142485,0.0530216346153847));
#95805=CARTESIAN_POINT('Ctrl Pts',(2.80114700154351,0.130837301153735,0.159064903846153));
#95806=CARTESIAN_POINT('Ctrl Pts',(1.40206621881702,2.43167759018441,0.318129807692308));
#95807=CARTESIAN_POINT('Ctrl Pts',(-1.28595649275605,2.49200065724321,0.477194711538461));
#95808=CARTESIAN_POINT('Ctrl Pts',(-2.33798102191255,0.938128541486862,
0.588288145006008));
#95809=CARTESIAN_POINT('Ctrl Pts',(-2.37525168063667,0.0764476031090624,
0.646359943858168));
#95810=CARTESIAN_POINT('Ctrl Pts',(-2.37475566780996,0.00146584572226396,
0.651410108094944));
#95811=CARTESIAN_POINT('Ctrl Pts',(1.29201570592006,2.64858957748139,-1.12757025938492E-16));
#95812=CARTESIAN_POINT('Ctrl Pts',(1.35047965203311,2.6133373327088,-1.12757025938492E-16));
#95813=CARTESIAN_POINT('Ctrl Pts',(1.40754132366598,2.57595763103654,2.13489512922672E-16));
#95814=CARTESIAN_POINT('Ctrl Pts',(1.46306877857888,2.53644300429327,1.17961196366423E-16));
#95815=CARTESIAN_POINT('Ctrl Pts',(1.54265755239867,2.47980578410417,-2.28698325172702E-17));
#95816=CARTESIAN_POINT('Ctrl Pts',(1.61909632492994,2.4187835354811,-2.47637160981643E-16));
#95817=CARTESIAN_POINT('Ctrl Pts',(1.69220921223578,2.35375552712431,-3.40005801291454E-16));
#95818=CARTESIAN_POINT('Ctrl Pts',(1.73112408478278,2.31914389092118,-3.89169690141314E-16));
#95819=CARTESIAN_POINT('Ctrl Pts',(1.76909604502006,2.28339686212,-3.9497258110791E-16));
#95820=CARTESIAN_POINT('Ctrl Pts',(1.80609349552389,2.24656857838508,-2.70616862252382E-16));
#95821=CARTESIAN_POINT('Ctrl Pts',(1.82369497454583,2.229047580188,-2.11454824142015E-16));
#95822=CARTESIAN_POINT('Ctrl Pts',(1.8410758325068,2.21128182971957,-7.03914766414606E-16));
#95823=CARTESIAN_POINT('Ctrl Pts',(1.85823236581716,2.19327704183541,-7.07767178198537E-16));
#95824=CARTESIAN_POINT('Ctrl Pts',(1.8762119379848,2.17440852234662,-7.11804399147296E-16));
#95825=CARTESIAN_POINT('Ctrl Pts',(1.89394940284166,2.15527254575146,-2.20692458830647E-16));
#95826=CARTESIAN_POINT('Ctrl Pts',(1.91141683968546,2.13590224832762,-2.56739074444567E-16));
#95827=CARTESIAN_POINT('Ctrl Pts',(1.97654793536834,2.06367592764876,-3.91146634728832E-16));
#95828=CARTESIAN_POINT('Ctrl Pts',(2.03798087273529,1.98814233841135,-4.75975953068255E-17));
#95829=CARTESIAN_POINT('Ctrl Pts',(2.09554087281375,1.90967640222123,-3.46944695195361E-17));
#95830=CARTESIAN_POINT('Ctrl Pts',(2.14262943686529,1.8454851538349,-2.41387074578314E-17));
#95831=CARTESIAN_POINT('Ctrl Pts',(2.18712531645739,1.77933058201533,-9.28299200764564E-18));
#95832=CARTESIAN_POINT('Ctrl Pts',(2.22890868996356,1.71140843266836,-2.77555756156289E-17));
#95833=CARTESIAN_POINT('Ctrl Pts',(2.24792938225854,1.68048880616784,-3.61646938657112E-17));
#95834=CARTESIAN_POINT('Ctrl Pts',(2.26638765990956,1.64920281103461,-3.05448741047574E-16));
#95835=CARTESIAN_POINT('Ctrl Pts',(2.2842706081915,1.61756865561342,-2.91433543964104E-16));
#95836=CARTESIAN_POINT('Ctrl Pts',(2.29484156490064,1.59886909432101,-2.83148889817395E-16));
#95837=CARTESIAN_POINT('Ctrl Pts',(2.30521146927951,1.58004787629747,4.42982721947554E-17));
#95838=CARTESIAN_POINT('Ctrl Pts',(2.31537748039068,1.56110875696981,6.93889390390723E-17));
#95839=CARTESIAN_POINT('Ctrl Pts',(2.32260089416002,1.54765165035891,8.72170002504184E-17));
#95840=CARTESIAN_POINT('Ctrl Pts',(2.32972104671691,1.53413546224949,-2.90001761152889E-16));
#95841=CARTESIAN_POINT('Ctrl Pts',(2.33673088705629,1.52057364590497,-2.77555756156289E-16));
#95842=CARTESIAN_POINT('Ctrl Pts',(2.38039267025554,1.43610195234924,-2.00034051588298E-16));
#95843=CARTESIAN_POINT('Ctrl Pts',(2.41984393470611,1.34974138975305,-3.54536939389555E-16));
#95844=CARTESIAN_POINT('Ctrl Pts',(2.45491901736627,1.26183770540906,-3.60822483003176E-16));
#95845=CARTESIAN_POINT('Ctrl Pts',(2.49095039506518,1.17153739500316,-3.67279397108831E-16));
#95846=CARTESIAN_POINT('Ctrl Pts',(2.52236430096921,1.07960768483293,1.90948379502136E-16));
#95847=CARTESIAN_POINT('Ctrl Pts',(2.54892424395783,0.986413230220722,2.08166817117217E-16));
#95848=CARTESIAN_POINT('Ctrl Pts',(2.57369277004672,0.899504561727304,2.24223904342959E-16));
#95849=CARTESIAN_POINT('Ctrl Pts',(2.5942397122875,0.811495234712604,-2.90917053419974E-16));
#95850=CARTESIAN_POINT('Ctrl Pts',(2.61032409035078,0.722685000091402,-3.33066907387547E-16));
#95851=CARTESIAN_POINT('Ctrl Pts',(2.61939480520976,0.672600855610439,-3.5683713370175E-16));
#95852=CARTESIAN_POINT('Ctrl Pts',(2.62704538989607,0.622262130851272,-4.79791839152818E-16));
#95853=CARTESIAN_POINT('Ctrl Pts',(2.63322550736737,0.571724499349377,-4.9960036108132E-16));
#95854=CARTESIAN_POINT('Ctrl Pts',(2.63576498704184,0.550958019004824,-5.07739905200389E-16));
#95855=CARTESIAN_POINT('Ctrl Pts',(2.63805663524629,0.530151373647901,6.55971552207216E-16));
#95856=CARTESIAN_POINT('Ctrl Pts',(2.64009358497002,0.509344318092916,6.10622663543836E-16));
#95857=CARTESIAN_POINT('Ctrl Pts',(2.64878126462266,0.420601316206363,4.17207670174275E-16));
#95858=CARTESIAN_POINT('Ctrl Pts',(2.65285456203884,0.331754436353281,-3.00385640345007E-16));
#95859=CARTESIAN_POINT('Ctrl Pts',(2.65212953715791,0.243094007921421,-2.4980018054066E-16));
#95860=CARTESIAN_POINT('Ctrl Pts',(2.6518119314253,0.204255257601141,-2.27640620995021E-16));
#95861=CARTESIAN_POINT('Ctrl Pts',(2.65057287851832,0.165452331247355,1.32747360840593E-16));
#95862=CARTESIAN_POINT('Ctrl Pts',(2.64839376652478,0.126710099518821,1.11022302462516E-16));
#95863=CARTESIAN_POINT('Ctrl Pts',(2.64331550885207,0.0364242233839251,
3.36506741470677E-17));
#95864=CARTESIAN_POINT('Ctrl Pts',(2.6331350383468,-0.0535335684357302,
2.32891675937926E-17));
#95865=CARTESIAN_POINT('Ctrl Pts',(2.61804895698347,-0.142830691087905,
0.));
#95866=CARTESIAN_POINT('Ctrl Pts',(2.60250975672972,-0.234809902757026,
-2.39886707665931E-17));
#95867=CARTESIAN_POINT('Ctrl Pts',(2.58176536987519,-0.326089235663464,
-1.3663112480103E-16));
#95868=CARTESIAN_POINT('Ctrl Pts',(2.55598340453964,-0.41627347846358,0.));
#95869=CARTESIAN_POINT('Ctrl Pts',(2.55178247440597,-0.430968157407989,
2.22627639865488E-17));
#95870=CARTESIAN_POINT('Ctrl Pts',(2.54744770854094,-0.445633674797536,
-6.91067322917457E-17));
#95871=CARTESIAN_POINT('Ctrl Pts',(2.54297973154851,-0.460268213187004,
-5.55111512312578E-17));
#95872=CARTESIAN_POINT('Ctrl Pts',(2.5389302343891,-0.473532050878587,-4.31889600073214E-17));
#95873=CARTESIAN_POINT('Ctrl Pts',(2.53477298110434,-0.486764833902074,
-6.0951382644997E-16));
#95874=CARTESIAN_POINT('Ctrl Pts',(2.53051107740137,-0.499958263234954,
-5.82867087928207E-16));
#95875=CARTESIAN_POINT('Ctrl Pts',(2.5032317931632,-0.584405809198302,-4.12308575860242E-16));
#95876=CARTESIAN_POINT('Ctrl Pts',(2.47164137946824,-0.667333741906229,
-3.15553173727667E-16));
#95877=CARTESIAN_POINT('Ctrl Pts',(2.43595239984652,-0.748438750214095,
-1.94289029309402E-16));
#95878=CARTESIAN_POINT('Ctrl Pts',(2.40031431849794,-0.829428089626163,
-7.31978272282084E-17));
#95879=CARTESIAN_POINT('Ctrl Pts',(2.36058869270874,-0.908600483118366,
6.82754206395419E-17));
#95880=CARTESIAN_POINT('Ctrl Pts',(2.31694497829497,-0.985624034856247,
1.94289029309402E-16));
#95881=CARTESIAN_POINT('Ctrl Pts',(2.27399614291603,-1.06142124616893,3.18296296036431E-16));
#95882=CARTESIAN_POINT('Ctrl Pts',(2.22725231457587,-1.13513811558509,-6.23795482104556E-16));
#95883=CARTESIAN_POINT('Ctrl Pts',(2.17684411225952,-1.20641915833307,-7.21644966006352E-16));
#95884=CARTESIAN_POINT('Ctrl Pts',(2.16022671274044,-1.22991742867499,-7.5390169987135E-16));
#95885=CARTESIAN_POINT('Ctrl Pts',(2.14321088331498,-1.25315062930938,-3.34983149003289E-16));
#95886=CARTESIAN_POINT('Ctrl Pts',(2.12580073890458,-1.27610489756701,-3.33066907387547E-16));
#95887=CARTESIAN_POINT('Ctrl Pts',(2.11280904752226,-1.29323369110718,-3.31636981299695E-16));
#95888=CARTESIAN_POINT('Ctrl Pts',(2.09959778216782,-1.31020715351732,-5.6152853452759E-16));
#95889=CARTESIAN_POINT('Ctrl Pts',(2.08616856960686,-1.32701929923775,-6.10622663543836E-16));
#95890=CARTESIAN_POINT('Ctrl Pts',(2.07805318318902,-1.33717902069682,-6.40290659787479E-16));
#95891=CARTESIAN_POINT('Ctrl Pts',(2.06986448397218,-1.34727196523556,4.59211246770366E-16));
#95892=CARTESIAN_POINT('Ctrl Pts',(2.06160311038263,-1.35729714638091,4.44089209850063E-16));
#95893=CARTESIAN_POINT('Ctrl Pts',(2.00737870704495,-1.42309848801806,3.44834113785818E-16));
#95894=CARTESIAN_POINT('Ctrl Pts',(1.95002592106155,-1.48598389603456,6.1896723624897E-16));
#95895=CARTESIAN_POINT('Ctrl Pts',(1.8897024430572,-1.54565686846859,4.44089209850063E-16));
#95896=CARTESIAN_POINT('Ctrl Pts',(1.83033018451105,-1.60438887903527,2.71968772818087E-16));
#95897=CARTESIAN_POINT('Ctrl Pts',(1.76807954519956,-1.66000948217716,3.80823319481553E-16));
#95898=CARTESIAN_POINT('Ctrl Pts',(1.70307501002074,-1.71219354094858,4.44089209850063E-16));
#95899=CARTESIAN_POINT('Ctrl Pts',(1.64009787967249,-1.76275004846468,5.05381921402809E-16));
#95900=CARTESIAN_POINT('Ctrl Pts',(1.57453538849668,-1.81008131772167,1.79680524881221E-16));
#95901=CARTESIAN_POINT('Ctrl Pts',(1.50648507168998,-1.85384593634628,2.22044604925031E-16));
#95902=CARTESIAN_POINT('Ctrl Pts',(1.46428163718096,-1.88098787047103,2.48317953258481E-16));
#95903=CARTESIAN_POINT('Ctrl Pts',(1.42112105178449,-1.90675706879086,-1.67702223404997E-17));
#95904=CARTESIAN_POINT('Ctrl Pts',(1.37702479013074,-1.93106208855785,0.));
#95905=CARTESIAN_POINT('Ctrl Pts',(0.260739855805175,2.92492329228916,49.058));
#95906=CARTESIAN_POINT('Ctrl Pts',(0.736266525833309,2.88315289962924,49.0322954004341));
#95907=CARTESIAN_POINT('Ctrl Pts',(1.20206891229148,2.73208629432238,49.0065908008682));
#95908=CARTESIAN_POINT('Ctrl Pts',(1.59958942631121,2.47560915657343,48.9808862013024));
#95909=CARTESIAN_POINT('Ctrl Pts',(2.41956669895652,1.9465662103852,48.927864566687));
#95910=CARTESIAN_POINT('Ctrl Pts',(2.94901465557698,0.969016965254652,48.8748429320716));
#95911=CARTESIAN_POINT('Ctrl Pts',(2.94659971013865,-0.00676955442900931,
48.8218212974562));
#95912=CARTESIAN_POINT('Ctrl Pts',(2.94418476470032,-0.982556074112615,
48.7687996628408));
#95913=CARTESIAN_POINT('Ctrl Pts',(2.40990691720327,-1.95657986834934,48.7157780282254));
#95914=CARTESIAN_POINT('Ctrl Pts',(1.58820872905997,-2.48224233655137,48.66275639361));
#95915=CARTESIAN_POINT('Ctrl Pts',(0.766510540916721,-3.00790480475337,
48.6097347589946));
#95916=CARTESIAN_POINT('Ctrl Pts',(-0.342607987872747,-3.08520594692074,
48.5567131243793));
#95917=CARTESIAN_POINT('Ctrl Pts',(-1.22934270943994,-2.67828538355204,
48.5036914897639));
#95918=CARTESIAN_POINT('Ctrl Pts',(-2.11607743100718,-2.27136482018332,
48.4506698551485));
#95919=CARTESIAN_POINT('Ctrl Pts',(-2.78042834535212,-1.38022255127848,
48.3976482205331));
#95920=CARTESIAN_POINT('Ctrl Pts',(-2.91755849077816,-0.414280030836403,
48.3446265859177));
#95921=CARTESIAN_POINT('Ctrl Pts',(-2.93691308114256,-0.277946610197007,
48.3371430963083));
#95922=CARTESIAN_POINT('Ctrl Pts',(-2.94576512520083,-0.140123124765416,
48.3296596066989));
#95923=CARTESIAN_POINT('Ctrl Pts',(-2.94461792262617,-0.00215304676840083,
48.3221761170895));
#95924=CARTESIAN_POINT('Origin',(0.,0.,-1.84858989190512));
#95925=CARTESIAN_POINT('',(-1.37702479013129,-1.93106208855745,0.));
#95926=CARTESIAN_POINT('Ctrl Pts',(-1.38001442237635,-1.93381244560189,
4.37638206923774E-15));
#95927=CARTESIAN_POINT('Ctrl Pts',(-0.781458010274238,-2.35626571080451,
0.049355603818813));
#95928=CARTESIAN_POINT('Ctrl Pts',(0.901264645133876,-2.62481382078411,
0.151744630133381));
#95929=CARTESIAN_POINT('Ctrl Pts',(2.71060447735492,-0.722409270309101,
0.307167078943709));
#95930=CARTESIAN_POINT('Ctrl Pts',(2.07285013055992,1.89055543244044,0.466267346430989));
#95931=CARTESIAN_POINT('Ctrl Pts',(-0.469810478716988,2.76551378306258,
0.625367613918266));
#95932=CARTESIAN_POINT('Ctrl Pts',(-2.16059338637857,1.43138769003934,0.752808462409609));
#95933=CARTESIAN_POINT('Ctrl Pts',(-2.36987959467941,0.320783635789767,
0.82721588840519));
#95934=CARTESIAN_POINT('Ctrl Pts',(-2.36841685556579,0.00122403911035841,
0.848589891905012));
#95935=CARTESIAN_POINT('Origin',(0.,0.,0.));
#95936=CARTESIAN_POINT('Ctrl Pts',(-1.03908919352446,2.13201587949074,-0.329233991005407));
#95937=CARTESIAN_POINT('Ctrl Pts',(-1.74951701127321,1.7857718034953,-0.276200568509647));
#95938=CARTESIAN_POINT('Ctrl Pts',(-2.78455395807173,0.333124289911143,
-0.170133723518128));
#95939=CARTESIAN_POINT('Ctrl Pts',(-1.78369205252407,-2.16759894682849,
-0.0110334560308489));
#95940=CARTESIAN_POINT('Ctrl Pts',(0.858449569970475,-2.66983112066845,
0.14806681145643));
#95941=CARTESIAN_POINT('Ctrl Pts',(2.71060447735492,-0.722409270309101,
0.307167078943709));
#95942=CARTESIAN_POINT('Ctrl Pts',(2.07285013055992,1.89055543244044,0.466267346430989));
#95943=CARTESIAN_POINT('Ctrl Pts',(-0.469810478716988,2.76551378306258,
0.625367613918266));
#95944=CARTESIAN_POINT('Ctrl Pts',(-2.58062515122094,1.09995818786284,0.784467881405546));
#95945=CARTESIAN_POINT('Ctrl Pts',(-2.3204090178813,-1.57651378416218,0.943568148892824));
#95946=CARTESIAN_POINT('Ctrl Pts',(0.0718874078444588,-2.8043235471302,
1.1026684163801));
#95947=CARTESIAN_POINT('Ctrl Pts',(2.39810709656883,-1.45554260356973,1.26176868386738));
#95948=CARTESIAN_POINT('Ctrl Pts',(2.52091778453322,1.23065290615308,1.42086895135466));
#95949=CARTESIAN_POINT('Ctrl Pts',(0.327458637825707,2.78608392325822,1.57996921884194));
#95950=CARTESIAN_POINT('Ctrl Pts',(-2.16687151941952,1.7816229585196,1.73906948632922));
#95951=CARTESIAN_POINT('Ctrl Pts',(-2.67024455303756,-0.859829308452707,
1.8981697538165));
#95952=CARTESIAN_POINT('Ctrl Pts',(-0.720149694819682,-2.71125275032746,
2.05727002130378));
#95953=CARTESIAN_POINT('Ctrl Pts',(1.89163063518288,-2.07153172086814,2.21637028879105));
#95954=CARTESIAN_POINT('Ctrl Pts',(2.76534828940725,0.471549254232345,2.37547055627834));
#95955=CARTESIAN_POINT('Ctrl Pts',(1.09821595227919,2.58136221632247,2.53457082376561));
#95956=CARTESIAN_POINT('Ctrl Pts',(-1.5779761243933,2.31937512843085,2.69367109125289));
#95957=CARTESIAN_POINT('Ctrl Pts',(-2.80429647983432,-0.0736940611091368,
2.85277135874017));
#95958=CARTESIAN_POINT('Ctrl Pts',(-1.45398069647754,-2.39905181471807,
3.01187162622745));
#95959=CARTESIAN_POINT('Ctrl Pts',(1.23227769270891,-2.52011928935842,3.17097189371473));
#95960=CARTESIAN_POINT('Ctrl Pts',(2.78629802603849,-0.325657548824043,
3.330072161202));
#95961=CARTESIAN_POINT('Ctrl Pts',(1.78021952909652,2.16802397289482,3.48917242868929));
#95962=CARTESIAN_POINT('Ctrl Pts',(-0.861555466122802,2.66968756742434,
3.64827269617656));
#95963=CARTESIAN_POINT('Ctrl Pts',(-2.71171839560361,0.718396039047425,
3.80737296366385));
#95964=CARTESIAN_POINT('Ctrl Pts',(-2.07030755199707,-1.89297019654229,
3.96647323115112));
#95965=CARTESIAN_POINT('Ctrl Pts',(0.473337684987186,-2.76504266915617,
4.12557349863841));
#95966=CARTESIAN_POINT('Ctrl Pts',(2.58207206872294,-1.09654610377387,4.28467376612568));
#95967=CARTESIAN_POINT('Ctrl Pts',(2.31835396766711,1.57947599104097,4.44377403361296));
#95968=CARTESIAN_POINT('Ctrl Pts',(-0.075507864702191,2.804248221581,4.60287430110024));
#95969=CARTESIAN_POINT('Ctrl Pts',(-2.39999176476856,1.45242867461087,4.76197456858752));
#95970=CARTESIAN_POINT('Ctrl Pts',(-2.51932171322798,-1.23390746453664,
4.9210748360748));
#95971=CARTESIAN_POINT('Ctrl Pts',(-0.323855289127461,-2.78650807957066,
5.08017510356208));
#95972=CARTESIAN_POINT('Ctrl Pts',(2.16917497708905,-1.77881686650588,5.23927537104935));
#95973=CARTESIAN_POINT('Ctrl Pts',(2.66912974919035,0.863282055751294,5.39837563853664));
#95974=CARTESIAN_POINT('Ctrl Pts',(0.716641933714364,2.71218249102838,5.55747590602391));
#95975=CARTESIAN_POINT('Ctrl Pts',(-1.89430888784795,2.06908273474431,5.71657617351119));
#95976=CARTESIAN_POINT('Ctrl Pts',(-2.76473593307623,-0.475126031863108,
5.87567644099847));
#95977=CARTESIAN_POINT('Ctrl Pts',(-1.09487577505419,-2.58278078105689,
6.03477670848575));
#95978=CARTESIAN_POINT('Ctrl Pts',(1.58097518564988,-2.31733186836853,6.19387697597303));
#95979=CARTESIAN_POINT('Ctrl Pts',(2.80419879604699,0.0773216531487339,
6.3529772434603));
#95980=CARTESIAN_POINT('Ctrl Pts',(1.45087604201706,2.40093070214407,6.51207751094759));
#95981=CARTESIAN_POINT('Ctrl Pts',(-1.23553671852851,2.51852308763786,6.67117777843485));
#95982=CARTESIAN_POINT('Ctrl Pts',(-2.78671696819491,0.322052891574838,
6.83027804592215));
#95983=CARTESIAN_POINT('Ctrl Pts',(-1.77741345928775,-2.17032507255016,
6.98937831340941));
#95984=CARTESIAN_POINT('Ctrl Pts',(0.865008283985421,-2.66857081495577,
7.14847858089671));
#95985=CARTESIAN_POINT('Ctrl Pts',(2.71264545191261,-0.714887528227297,
7.30757884838397));
#95986=CARTESIAN_POINT('Ctrl Pts',(2.0678570518103,1.89564678647566,7.46667911587126));
#95987=CARTESIAN_POINT('Ctrl Pts',(-0.476914179932666,2.76442804044096,
7.62577938335854));
#95988=CARTESIAN_POINT('Ctrl Pts',(-2.58348841288175,1.09320498823544,7.78487965084581));
#95989=CARTESIAN_POINT('Ctrl Pts',(-2.31630879958662,-1.58247371881959,
7.94397991833311));
#95990=CARTESIAN_POINT('Ctrl Pts',(0.0791354092423232,-2.80414819736781,
8.10308018582037));
#95991=CARTESIAN_POINT('Ctrl Pts',(2.40186863507383,-1.44932280243071,8.26218045330766));
#95992=CARTESIAN_POINT('Ctrl Pts',(2.51772340840239,1.23716545562014,8.42128072079493));
#95993=CARTESIAN_POINT('Ctrl Pts',(0.320250359289559,2.78692469097606,8.58038098828221));
#95994=CARTESIAN_POINT('Ctrl Pts',(-2.17147426003902,1.77600930847366,8.73948125576949));
#95995=CARTESIAN_POINT('Ctrl Pts',(-2.66801076430334,-0.866734150335981,
8.89858152325677));
#95996=CARTESIAN_POINT('Ctrl Pts',(-0.713132823661497,-2.71310727794049,
9.05768179074405));
#95997=CARTESIAN_POINT('Ctrl Pts',(1.89698389204465,-2.06663050377184,9.21678205823132));
#95998=CARTESIAN_POINT('Ctrl Pts',(2.76411899128539,0.478702128481346,9.37588232571861));
#95999=CARTESIAN_POINT('Ctrl Pts',(1.09153374406576,2.5841949638839,9.53498259320587));
#96000=CARTESIAN_POINT('Ctrl Pts',(-1.58397158994894,2.31528476175863,9.69408286069318));
#96001=CARTESIAN_POINT('Ctrl Pts',(-2.8040964255511,-0.08094913222896,9.85318312818042));
#96002=CARTESIAN_POINT('Ctrl Pts',(-1.44776895650877,-2.4028055631629,10.0122833956677));
#96003=CARTESIAN_POINT('Ctrl Pts',(1.23879367513383,-2.51692267585747,10.171383663155));
#96004=CARTESIAN_POINT('Ctrl Pts',(2.78713124782529,-0.318447693025035,
10.3304839306423));
#96005=CARTESIAN_POINT('Ctrl Pts',(1.77460441465207,2.1726225390745,10.4895841981295));
#96006=CARTESIAN_POINT('Ctrl Pts',(-0.868459654081467,2.66744959746755,
10.6486844656168));
#96007=CARTESIAN_POINT('Ctrl Pts',(-2.71356796891854,0.711377820750957,
10.8077847331041));
#96008=CARTESIAN_POINT('Ctrl Pts',(-2.0654030911422,-1.89832020399546,10.9668850005914));
#96009=CARTESIAN_POINT('Ctrl Pts',(0.480489876761207,-2.76380878573882,
11.1259852680787));
#96010=CARTESIAN_POINT('Ctrl Pts',(2.58490043376768,-1.08986204324435,11.2850855355659));
#96011=CARTESIAN_POINT('Ctrl Pts',(2.31425975531301,1.58546879841127,11.4441858030532));
#96012=CARTESIAN_POINT('Ctrl Pts',(-0.0827628213498791,2.80404348061853,
11.6032860705405));
#96013=CARTESIAN_POINT('Ctrl Pts',(-2.40374148601931,1.44621450490125,11.7623863380278));
#96014=CARTESIAN_POINT('Ctrl Pts',(-2.5161208903381,-1.24042137638842,11.921486605515));
#96015=CARTESIAN_POINT('Ctrl Pts',(-0.316644893535377,-2.78733663865617,
12.0805868730024));
#96016=CARTESIAN_POINT('Ctrl Pts',(2.17376990917619,-1.7731987784107,12.2396871404896));
#96017=CARTESIAN_POINT('Ctrl Pts',(2.66688731468318,0.870184794500003,12.3987874079769));
#96018=CARTESIAN_POINT('Ctrl Pts',(0.709622520229888,2.71402752465403,12.5578876754642));
#96019=CARTESIAN_POINT('Ctrl Pts',(-1.89965572176903,2.06417481443488,12.7169879429515));
#96020=CARTESIAN_POINT('Ctrl Pts',(-2.76349742393105,-0.482277424024338,
12.8760882104387));
#96021=CARTESIAN_POINT('Ctrl Pts',(-1.08818988647055,-2.58560482223799,
13.035188477926));
#96022=CARTESIAN_POINT('Ctrl Pts',(1.58696534358022,-2.31323378067855,13.1942887454133));
#96023=CARTESIAN_POINT('Ctrl Pts',(2.80398936259225,0.0845764758463313,
13.3533890129006));
#96024=CARTESIAN_POINT('Ctrl Pts',(1.44465944825848,2.40467640325151,13.5124892803878));
#96025=CARTESIAN_POINT('Ctrl Pts',(-1.24204855870295,2.51531805217969,13.6715895478751));
#96026=CARTESIAN_POINT('Ctrl Pts',(-2.78754086338278,0.314841961574842,
13.8306898153624));
#96027=CARTESIAN_POINT('Ctrl Pts',(-1.77179240033766,-2.1749163698641,13.9897900828497));
#96028=CARTESIAN_POINT('Ctrl Pts',(0.87190957086987,-2.66632391618547,14.148890350337));
#96029=CARTESIAN_POINT('Ctrl Pts',(2.71448594495469,-0.707866922832642,
14.3079906178242));
#96030=CARTESIAN_POINT('Ctrl Pts',(2.06294567416375,1.90099044480665,14.4670908853115));
#96031=CARTESIAN_POINT('Ctrl Pts',(-0.484064769522908,2.76318490599233,
14.6261911527988));
#96032=CARTESIAN_POINT('Ctrl Pts',(-2.58630812900012,1.08651727444391,14.7852914202861));
#96033=CARTESIAN_POINT('Ctrl Pts',(-2.31220683828449,-1.58846122482972,
14.9443916877734));
#96034=CARTESIAN_POINT('Ctrl Pts',(0.0863900949595627,-2.8039340714949,
15.1034919552607));
#96035=CARTESIAN_POINT('Ctrl Pts',(2.40561031446837,-1.44310378723102,15.2625922227479));
#96036=CARTESIAN_POINT('Ctrl Pts',(2.51451416171814,1.24367522139665,15.4216924902352));
#96037=CARTESIAN_POINT('Ctrl Pts',(0.313038897897693,2.78774392191968,15.5807927577225));
#96038=CARTESIAN_POINT('Ctrl Pts',(-2.17606192065859,1.77038528102128,15.7398930252098));
#96039=CARTESIAN_POINT('Ctrl Pts',(-2.66575940221011,-0.873633982469486,
15.898993292697));
#96040=CARTESIAN_POINT('Ctrl Pts',(-0.706111029293687,-2.71494322962874,
16.0580935601843));
#96041=CARTESIAN_POINT('Ctrl Pts',(1.90232437254992,-2.06171567084302,16.2171938276716));
#96042=CARTESIAN_POINT('Ctrl Pts',(2.7628712320534,0.485851912509174,16.3762940951588));
#96043=CARTESIAN_POINT('Ctrl Pts',(1.08484420786421,2.58701035375983,16.5353943626462));
#96044=CARTESIAN_POINT('Ctrl Pts',(-1.58995644153392,2.31117892856046,16.6944946301334));
#96045=CARTESIAN_POINT('Ctrl Pts',(-2.80387760734961,-0.0882036779308033,
16.8535948976207));
#96046=CARTESIAN_POINT('Ctrl Pts',(-1.44154752246972,-2.40654321927916,
17.012695165108));
#96047=CARTESIAN_POINT('Ctrl Pts',(1.24530136378902,-2.51370921928975,17.1717954325953));
#96048=CARTESIAN_POINT('Ctrl Pts',(2.78794581418191,-0.311235703258245,
17.3308957000825));
#96049=CARTESIAN_POINT('Ctrl Pts',(1.76897742105025,2.17720656108039,17.4899959675698));
#96050=CARTESIAN_POINT('Ctrl Pts',(-0.875358028577435,2.66519377299328,
17.6490962350571));
#96051=CARTESIAN_POINT('Ctrl Pts',(-2.71539937848487,0.704354840347607,
17.8081965025444));
#96052=CARTESIAN_POINT('Ctrl Pts',(-2.06048480498726,-1.90365750444079,
17.9672967700317));
#96053=CARTESIAN_POINT('Ctrl Pts',(0.487638852235446,-2.7625564022455,18.1263970375189));
#96054=CARTESIAN_POINT('Ctrl Pts',(2.58771149622336,-1.08317068743137,18.2854973050062));
#96055=CARTESIAN_POINT('Ctrl Pts',(2.3101500519365,1.5914509930673,18.4445975724935));
#96056=CARTESIAN_POINT('Ctrl Pts',(-0.0900172240013499,2.80381997018001,
18.6036978399808));
#96057=CARTESIAN_POINT('Ctrl Pts',(-2.40747511729362,1.43999065462563,18.7627981074681));
#96058=CARTESIAN_POINT('Ctrl Pts',(-2.51290322523128,-1.24692698519977,
18.9218983749553));
#96059=CARTESIAN_POINT('Ctrl Pts',(-0.309432378410861,-2.78814654008503,
19.0809986424426));
#96060=CARTESIAN_POINT('Ctrl Pts',(2.17835029065068,-1.76756882101353,19.2400989099299));
#96061=CARTESIAN_POINT('Ctrl Pts',(2.66462702877159,0.877081708472472,19.3991991774172));
#96062=CARTESIAN_POINT('Ctrl Pts',(0.702598356729098,2.71585439133226,19.5582994449045));
#96063=CARTESIAN_POINT('Ctrl Pts',(-1.90498983992151,2.05925307711142,19.7173997123917));
#96064=CARTESIAN_POINT('Ctrl Pts',(-2.76224041670033,-0.489425587954166,
19.876499979879));
#96065=CARTESIAN_POINT('Ctrl Pts',(-1.08149671384552,-2.58841155609738,
20.0356002473663));
#96066=CARTESIAN_POINT('Ctrl Pts',(1.59294487880464,-2.30912020884302,20.1947005148536));
#96067=CARTESIAN_POINT('Ctrl Pts',(2.80376116001019,0.0918307324124995,
20.3538007823408));
#96068=CARTESIAN_POINT('Ctrl Pts',(1.43843318435008,2.40840600812187,20.5129010498282));
#96069=CARTESIAN_POINT('Ctrl Pts',(-1.24855208494876,2.51209617987991,20.6720013173154));
#96070=CARTESIAN_POINT('Ctrl Pts',(-2.78834609954504,0.307628924110014,
20.8311015848027));
#96071=CARTESIAN_POINT('Ctrl Pts',(-1.76615948150047,-2.17949310889092,
20.9902018522899));
#96072=CARTESIAN_POINT('Ctrl Pts',(0.878805021433445,-2.66405916978217,
21.1493021197773));
#96073=CARTESIAN_POINT('Ctrl Pts',(2.71630826798053,-0.70084157917304,21.3084023872645));
#96074=CARTESIAN_POINT('Ctrl Pts',(2.05802048773081,1.90632137843475,21.4675026547518));
#96075=CARTESIAN_POINT('Ctrl Pts',(-0.491212118917867,2.76192327555009,
21.6266029222391));
#96076=CARTESIAN_POINT('Ctrl Pts',(-2.589110533089,1.07982228780697,21.7857031897264));
#96077=CARTESIAN_POINT('Ctrl Pts',(-2.30808939971089,-1.59443809812089,
21.9448034572136));
#96078=CARTESIAN_POINT('Ctrl Pts',(0.0936442024055214,-2.80370117686478,
22.1039037247009));
#96079=CARTESIAN_POINT('Ctrl Pts',(2.40933589137447,-1.43687511229467,22.2630039921882));
#96080=CARTESIAN_POINT('Ctrl Pts',(2.51128808357329,1.25017666235613,22.4221042596755));
#96081=CARTESIAN_POINT('Ctrl Pts',(0.305825341110179,2.78854449247846,22.5812045271628));
#96082=CARTESIAN_POINT('Ctrl Pts',(-2.18063501532304,1.76474940310066,22.74030479465));
#96083=CARTESIAN_POINT('Ctrl Pts',(-2.66349019626259,-0.880527966739403,
22.8994050621373));
#96084=CARTESIAN_POINT('Ctrl Pts',(-0.699084508414374,-2.7167610082398,
23.0585053296246));
#96085=CARTESIAN_POINT('Ctrl Pts',(1.90765211942334,-2.05678703736111,23.2176055971119));
#96086=CARTESIAN_POINT('Ctrl Pts',(2.76160497892747,0.49299844437904,23.3767058645991));
#96087=CARTESIAN_POINT('Ctrl Pts',(1.07814741001629,2.5898084269058,23.5358061320864));
#96088=CARTESIAN_POINT('Ctrl Pts',(-1.59593065039136,2.30705762497135,23.6949063995737));
#96089=CARTESIAN_POINT('Ctrl Pts',(-2.80364002076886,-0.0954576332217178,
23.854006667061));
#96090=CARTESIAN_POINT('Ctrl Pts',(-1.43531643911124,-2.4102647666624,24.0131069345482));
#96091=CARTESIAN_POINT('Ctrl Pts',(1.2518007167422,-2.51047893664949,24.1722072020356));
#96092=CARTESIAN_POINT('Ctrl Pts',(2.78874171880229,-0.304021630165937,
24.3313074695228));
#96093=CARTESIAN_POINT('Ctrl Pts',(1.76333858640404,2.18177600946929,24.4904077370101));
#96094=CARTESIAN_POINT('Ctrl Pts',(-0.882250543669541,2.66292010845086,
24.6495080044974));
#96095=CARTESIAN_POINT('Ctrl Pts',(-2.71721261192068,0.697327145188193,
24.8086082719847));
#96096=CARTESIAN_POINT('Ctrl Pts',(-2.05555272651832,-1.90898206233064,
24.9677085394719));
#96097=CARTESIAN_POINT('Ctrl Pts',(0.494784563590454,-2.76128552696561,
25.1268088069592));
#96098=CARTESIAN_POINT('Ctrl Pts',(2.59050523725581,-1.07647208117411,25.2859090744465));
#96099=CARTESIAN_POINT('Ctrl Pts',(2.30602488505606,1.59742253499168,25.4450093419338));
#96100=CARTESIAN_POINT('Ctrl Pts',(-0.0972710241024927,2.80357769174802,
25.6041096094211));
#96101=CARTESIAN_POINT('Ctrl Pts',(-2.41119263359704,1.43375716545184,25.7632098769083));
#96102=CARTESIAN_POINT('Ctrl Pts',(-2.50966873944702,-1.2534242474276,25.9223101443956));
#96103=CARTESIAN_POINT('Ctrl Pts',(-0.302217792031812,-2.78893777843403,
26.0814104118829));
#96104=CARTESIAN_POINT('Ctrl Pts',(2.18291609085233,-1.76192703200078,26.2405106793702));
#96105=CARTESIAN_POINT('Ctrl Pts',(2.66234890658549,0.883972751503175,26.3996109468574));
#96106=CARTESIAN_POINT('Ctrl Pts',(0.695569490229732,2.71766307883422,26.5587112143448));
#96107=CARTESIAN_POINT('Ctrl Pts',(-1.91031120660023,2.05431755571885,26.717811481832));
#96108=CARTESIAN_POINT('Ctrl Pts',(-2.76096491979815,-0.496570475804816,
26.8769117493193));
#96109=CARTESIAN_POINT('Ctrl Pts',(-1.07479630198138,-2.59120096384751,
27.0360120168066));
#96110=CARTESIAN_POINT('Ctrl Pts',(1.59891375129768,-2.30499118039708,27.1951122842938));
#96111=CARTESIAN_POINT('Ctrl Pts',(2.80351418982834,0.0990843742891699,
27.3542125517811));
#96112=CARTESIAN_POINT('Ctrl Pts',(1.43219729196881,2.41211949179022,27.5133128192684));
#96113=CARTESIAN_POINT('Ctrl Pts',(-1.25504725373308,2.50885749230484,27.6724130867557));
#96114=CARTESIAN_POINT('Ctrl Pts',(-2.78913267129164,0.300413827462487,
27.8315133542429));
#96115=CARTESIAN_POINT('Ctrl Pts',(-1.76051474048145,-2.18405525899521,
27.9906136217303));
#96116=CARTESIAN_POINT('Ctrl Pts',(0.885694589519864,-2.66177659090546,
28.1497138892175));
#96117=CARTESIAN_POINT('Ctrl Pts',(2.71811240879197,-0.693811544274251,
28.3088141567048));
#96118=CARTESIAN_POINT('Ctrl Pts',(2.05308152547941,1.91163955167607,28.4679144241921));
#96119=CARTESIAN_POINT('Ctrl Pts',(-0.498356180275029,2.76064315755925,
28.6270146916793));
#96120=CARTESIAN_POINT('Ctrl Pts',(-2.59189560638986,1.0731200731391,28.7861149591667));
#96121=CARTESIAN_POINT('Ctrl Pts',(-2.30395651142684,-1.60040429868549,
28.9452152266539));
#96122=CARTESIAN_POINT('Ctrl Pts',(0.10089768302309,-2.80344951503636,29.1043154941412));
#96123=CARTESIAN_POINT('Ctrl Pts',(2.41304534085417,-1.43063681931478,29.2634157616285));
#96124=CARTESIAN_POINT('Ctrl Pts',(2.50804519556235,1.25666973497962,29.4225160291157));
#96125=CARTESIAN_POINT('Ctrl Pts',(0.298609737212693,2.78932639729359,29.581616296603));
#96126=CARTESIAN_POINT('Ctrl Pts',(-2.18519351342132,1.75910171243692,29.7407165640903));
#96127=CARTESIAN_POINT('Ctrl Pts',(-2.66120316165021,-0.887416056999214,
29.8998168315776));
#96128=CARTESIAN_POINT('Ctrl Pts',(-0.692053308057238,-2.71856060160596,
30.0589170990649));
#96129=CARTESIAN_POINT('Ctrl Pts',(1.91296709700241,-2.05184463631711,30.2180173665521));
#96130=CARTESIAN_POINT('Ctrl Pts',(2.76032024038351,0.500141676254002,30.3771176340394));
#96131=CARTESIAN_POINT('Ctrl Pts',(1.07144339534857,2.59258916459223,30.5362179015267));
#96132=CARTESIAN_POINT('Ctrl Pts',(-1.60189417653155,2.30292087857821,30.695318169014));
#96133=CARTESIAN_POINT('Ctrl Pts',(-2.80338366739918,-0.102710949545695,
30.8544184365013));
#96134=CARTESIAN_POINT('Ctrl Pts',(-1.42907574814251,-2.41397018040158,
31.0135187039885));
#96135=CARTESIAN_POINT('Ctrl Pts',(1.25829169048848,-2.50723184955934,31.1726189714758));
#96136=CARTESIAN_POINT('Ctrl Pts',(2.78951895635884,-0.296805522037135,
31.3317192389631));
#96137=CARTESIAN_POINT('Ctrl Pts',(1.75768794845828,2.18633085365451,31.4908195064504));
#96138=CARTESIAN_POINT('Ctrl Pts',(-0.889137153221077,2.66062861905961,
31.6499197739376));
#96139=CARTESIAN_POINT('Ctrl Pts',(-2.71900765708865,0.690294782314285,
31.809020041425));
#96140=CARTESIAN_POINT('Ctrl Pts',(-2.05060688874944,-1.91429384202386,
31.9681203089122));
#96141=CARTESIAN_POINT('Ctrl Pts',(0.501926962994743,-2.75999616840604,
32.1272205763995));
#96142=CARTESIAN_POINT('Ctrl Pts',(2.59328163816445,-1.06976626931127,32.2863208438868));
#96143=CARTESIAN_POINT('Ctrl Pts',(2.30188428228449,1.60338338421251,32.445421111374));
#96144=CARTESIAN_POINT('Ctrl Pts',(-0.104524173098342,2.80331664694433,
32.6045213788614));
#96145=CARTESIAN_POINT('Ctrl Pts',(-2.4148940100455,1.42751407910515,32.7636216463486));
#96146=CARTESIAN_POINT('Ctrl Pts',(-2.50641745463613,-1.25991311958106,
32.9227219138359));
#96147=CARTESIAN_POINT('Ctrl Pts',(-0.295001182690674,-2.78971034840684,
33.0818221813231));
#96148=CARTESIAN_POINT('Ctrl Pts',(2.18746727921893,-1.75627344913702,33.2409224488105));
#96149=CARTESIAN_POINT('Ctrl Pts',(2.66005296337403,0.890857877465394,33.4000227162977));
#96150=CARTESIAN_POINT('Ctrl Pts',(0.688535967781046,2.71945357505306,33.559122983785));
#96151=CARTESIAN_POINT('Ctrl Pts',(-1.9156197861854,2.04936828329418,33.7182232512723));
#96152=CARTESIAN_POINT('Ctrl Pts',(-2.75967094176237,-0.503712039750395,
33.8773235187596));
#96153=CARTESIAN_POINT('Ctrl Pts',(-1.06808869572879,-2.59397302681686,
34.0364237862468));
#96154=CARTESIAN_POINT('Ctrl Pts',(1.60487192110541,-2.30084672297929,34.1955240537341));
#96155=CARTESIAN_POINT('Ctrl Pts',(2.80324845369984,0.106337352922497,34.3546243212214));
#96156=CARTESIAN_POINT('Ctrl Pts',(1.425951812856,2.41581682939948,34.5137245887086));
#96157=CARTESIAN_POINT('Ctrl Pts',(-1.26153402157907,2.50560201113339,34.672824856196));
#96158=CARTESIAN_POINT('Ctrl Pts',(-2.7899005733575,0.293196719928112,34.8319251236832));
#96159=CARTESIAN_POINT('Ctrl Pts',(-1.75485821506492,-2.18860278963914,
34.9910253911705));
#96160=CARTESIAN_POINT('Ctrl Pts',(0.892578229012262,-2.65947619483432,
35.1501256586578));
#96161=CARTESIAN_POINT('Ctrl Pts',(2.71989835531262,-0.686776865193377,
35.3092259261451));
#96162=CARTESIAN_POINT('Ctrl Pts',(2.04812882046954,1.91694492893226,35.4683261936323));
#96163=CARTESIAN_POINT('Ctrl Pts',(-0.505496905774109,2.75934456058861,
35.6274264611197));
#96164=CARTESIAN_POINT('Ctrl Pts',(-2.59466333026019,1.066410675303,35.7865267286069));
#96165=CARTESIAN_POINT('Ctrl Pts',(-2.29980820109672,-1.60635978658748,
35.9456269960942));
#96166=CARTESIAN_POINT('Ctrl Pts',(0.108150488259582,-2.80317908769424,
36.1047272635815));
#96167=CARTESIAN_POINT('Ctrl Pts',(2.41673863807743,-1.42438895004866,36.2638275310687));
#96168=CARTESIAN_POINT('Ctrl Pts',(2.50478551939227,1.26315439580437,36.422927798556));
#96169=CARTESIAN_POINT('Ctrl Pts',(0.291392134504392,2.79008963113125,36.5820280660433));
#96170=CARTESIAN_POINT('Ctrl Pts',(-2.18973738444013,1.75344224683403,36.7411283335306));
#96171=CARTESIAN_POINT('Ctrl Pts',(-2.65889831368176,-0.894298207142014,
36.9002286010178));
#96172=CARTESIAN_POINT('Ctrl Pts',(-0.685017475287161,-2.72034199768123,
37.0593288685051));
#96173=CARTESIAN_POINT('Ctrl Pts',(1.91826926971012,-2.04688850079404,37.2184291359924));
#96174=CARTESIAN_POINT('Ctrl Pts',(2.75901702502127,0.507281560319236,37.3775294034797));
#96175=CARTESIAN_POINT('Ctrl Pts',(1.06473220873587,2.59535254820565,37.536629670967));
#96176=CARTESIAN_POINT('Ctrl Pts',(-1.60784698003624,2.29876871707125,37.6957299384542));
#96177=CARTESIAN_POINT('Ctrl Pts',(-2.80310854895656,-0.109963578351025,
37.8548302059416));
#96178=CARTESIAN_POINT('Ctrl Pts',(-1.42282549133698,-2.4176594356937,38.0139304734288));
#96179=CARTESIAN_POINT('Ctrl Pts',(1.26477424157903,-2.50396797975438,38.1730307409161));
#96180=CARTESIAN_POINT('Ctrl Pts',(2.79027752164898,-0.289587427174506,
38.3321310084034));
#96181=CARTESIAN_POINT('Ctrl Pts',(1.75202554503676,2.1908710631472,38.4912312758906));
#96182=CARTESIAN_POINT('Ctrl Pts',(-0.896017811135028,2.6583193201581,38.650331543378));
#96183=CARTESIAN_POINT('Ctrl Pts',(-2.72078450197331,0.683257798798514,
38.8094318108652));
#96184=CARTESIAN_POINT('Ctrl Pts',(-2.04564732478662,-1.91959280796486,
38.9685320783525));
#96185=CARTESIAN_POINT('Ctrl Pts',(0.509066002639091,-2.75868833519739,
39.1276323458398));
#96186=CARTESIAN_POINT('Ctrl Pts',(2.5960406803649,-1.06305329672964,39.286732613327));
#96187=CARTESIAN_POINT('Ctrl Pts',(2.29772827133774,1.60933350082956,39.4458328808143));
#96188=CARTESIAN_POINT('Ctrl Pts',(-0.111776622438346,2.80303683751629,
39.6049331483016));
#96189=CARTESIAN_POINT('Ctrl Pts',(-2.41857922186304,1.42126143737506,39.7640334157889));
#96190=CARTESIAN_POINT('Ctrl Pts',(-2.50314939256176,-1.26639355822537,
39.9231336832761));
#96191=CARTESIAN_POINT('Ctrl Pts',(-0.287782598693457,-2.79046424483211,
40.0822339507635));
#96192=CARTESIAN_POINT('Ctrl Pts',(2.19200382528608,-1.7506081102658,40.2413342182507));
#96193=CARTESIAN_POINT('Ctrl Pts',(2.65773921450559,0.897737040271954,40.400434485738));
#96194=CARTESIAN_POINT('Ctrl Pts',(0.681497836463564,2.72122586800371,40.5595347532253));
#96195=CARTESIAN_POINT('Ctrl Pts',(-1.92091554314286,2.04440529296648,40.7186350207125));
#96196=CARTESIAN_POINT('Ctrl Pts',(-2.7583584912545,-0.510850231987242,
40.8777352881999));
#96197=CARTESIAN_POINT('Ctrl Pts',(-1.0613739399866,-2.59672772645004,41.036835555687));
#96198=CARTESIAN_POINT('Ctrl Pts',(1.6108193483455,-2.29668686433149,41.1959358231744));
#96199=CARTESIAN_POINT('Ctrl Pts',(2.80296395340346,0.113589619763061,41.3550360906616));
#96200=CARTESIAN_POINT('Ctrl Pts',(1.41969678881716,2.41949799620072,41.514136358149));
#96201=CARTESIAN_POINT('Ctrl Pts',(-1.2680123450661,2.50232975815682,41.6732366256362));
#96202=CARTESIAN_POINT('Ctrl Pts',(-2.79064980060251,0.285977649816169,
41.8323368931235));
#96203=CARTESIAN_POINT('Ctrl Pts',(-1.74918994311403,-2.19313567038289,
41.9914371606108));
#96204=CARTESIAN_POINT('Ctrl Pts',(0.899455893833502,-2.65715799696691,
42.1505374280981));
#96205=CARTESIAN_POINT('Ctrl Pts',(2.72166609558782,-0.679737589018599,
42.3096376955853));
#96206=CARTESIAN_POINT('Ctrl Pts',(2.04316240585326,1.92223747469062,42.4687379630726));
#96207=CARTESIAN_POINT('Ctrl Pts',(-0.512634247617058,2.75802749333056,
42.6278382305599));
#96208=CARTESIAN_POINT('Ctrl Pts',(-2.59741368617366,1.05969413920951,42.7869384980472));
#96209=CARTESIAN_POINT('Ctrl Pts',(-2.29564449648816,-1.61230452196248,
42.9460387655344));
#96210=CARTESIAN_POINT('Ctrl Pts',(0.11540256956664,-2.80288989664852,43.1051390330218));
#96211=CARTESIAN_POINT('Ctrl Pts',(2.42041575832236,-1.41813154631793,43.2642393005089));
#96212=CARTESIAN_POINT('Ctrl Pts',(2.50150907688241,1.26963060142386,43.4233395679963));
#96213=CARTESIAN_POINT('Ctrl Pts',(0.284172581298068,2.79083418888245,43.5824398354835));
#96214=CARTESIAN_POINT('Ctrl Pts',(-2.19426659796431,1.74777104417508,43.7415401029709));
#96215=CARTESIAN_POINT('Ctrl Pts',(-2.65657566778475,-0.901174371100898,
43.900640370458));
#96216=CARTESIAN_POINT('Ctrl Pts',(-0.677977057200952,-2.72210518454085,
44.0597406379455));
#96217=CARTESIAN_POINT('Ctrl Pts',(1.92355860205693,-2.04191866396806,44.2188409054326));
#96218=CARTESIAN_POINT('Ctrl Pts',(2.75769534156078,0.514418048784537,44.37794117292));
#96219=CARTESIAN_POINT('Ctrl Pts',(1.05801389510723,2.59809855924461,44.5370414404072));
#96220=CARTESIAN_POINT('Ctrl Pts',(-1.61378902107108,2.29460116825178,44.6961417078945));
#96221=CARTESIAN_POINT('Ctrl Pts',(-2.8028146672597,-0.117215471105793,
44.8552419753818));
#96222=CARTESIAN_POINT('Ctrl Pts',(-1.41656571057567,-2.42133250781507,
45.014342242869));
#96223=CARTESIAN_POINT('Ctrl Pts',(1.27124832670454,-2.50068734913707,45.1734425103564));
#96224=CARTESIAN_POINT('Ctrl Pts',(2.79101740943663,-0.282367393789022,
45.3325427778436));
#96225=CARTESIAN_POINT('Ctrl Pts',(1.74635141434428,2.19539660735637,45.4916430453309));
#96226=CARTESIAN_POINT('Ctrl Pts',(-0.902892471930827,2.65599222758591,
45.6507433128183));
#96227=CARTESIAN_POINT('Ctrl Pts',(-2.72254313358101,0.676216241016185,
45.8098435803054));
#96228=CARTESIAN_POINT('Ctrl Pts',(-2.04067406992595,-1.92487892329463,
45.9689438477928));
#96229=CARTESIAN_POINT('Ctrl Pts',(0.516201638739318,-2.75736203874416,
46.12804411528));
#96230=CARTESIAN_POINT('Ctrl Pts',(2.59878233775354,-1.05633320330836,46.2871443827674));
#96231=CARTESIAN_POINT('Ctrl Pts',(2.29355689460039,1.61527283537019,46.4462446502545));
#96232=CARTESIAN_POINT('Ctrl Pts',(-0.119028351361985,2.80273828373448,
46.6053449177419));
#96233=CARTESIAN_POINT('Ctrl Pts',(-2.42224819137782,1.41499924701908,46.7644451852291));
#96234=CARTESIAN_POINT('Ctrl Pts',(-2.49986467621169,-1.27286545303251,
46.9235454527165));
#96235=CARTESIAN_POINT('Ctrl Pts',(-0.280561895474226,-2.79119959037926,
47.0826457202037));
#96236=CARTESIAN_POINT('Ctrl Pts',(2.19652533073393,-1.74493080967452,47.241745987691));
#96237=CARTESIAN_POINT('Ctrl Pts',(2.65540837738748,0.904609729110513,47.4008462551782));
#96238=CARTESIAN_POINT('Ctrl Pts',(0.674453804384293,2.72298083242374,47.5599465226655));
#96239=CARTESIAN_POINT('Ctrl Pts',(-1.92619588769776,2.03942692664895,47.7190467901528));
#96240=CARTESIAN_POINT('Ctrl Pts',(-2.7570324497735,-0.517981778342401,
47.8781470576401));
#96241=CARTESIAN_POINT('Ctrl Pts',(-1.05464278435862,-2.59947119907506,
48.0372473251273));
#96242=CARTESIAN_POINT('Ctrl Pts',(1.61673826111253,-2.29249989126509,48.1963475926147));
#96243=CARTESIAN_POINT('Ctrl Pts',(2.80269451719685,0.120818728651149,48.3554478601019));
#96244=CARTESIAN_POINT('Ctrl Pts',(1.41336773306382,2.42320569438391,48.5145481275892));
#96245=CARTESIAN_POINT('Ctrl Pts',(-1.27435908006578,2.49895924442061,48.6736483950764));
#96246=CARTESIAN_POINT('Ctrl Pts',(-2.79161521279367,0.27891219154285,48.8327486625638));
#96247=CARTESIAN_POINT('Ctrl Pts',(-1.74306162992693,-2.19795085039717,
48.991848930051));
#96248=CARTESIAN_POINT('Ctrl Pts',(0.905469678109174,-2.65425291543538,
49.1509491975383));
#96249=CARTESIAN_POINT('Ctrl Pts',(2.72507495425543,-0.67380191912698,49.3100494650256));
#96250=CARTESIAN_POINT('Ctrl Pts',(2.03481676979323,1.92982725944834,49.4691497325128));
#96251=CARTESIAN_POINT('Ctrl Pts',(0.337182413353676,2.47711500076564,49.5752165775044));
#96252=CARTESIAN_POINT('Ctrl Pts',(-0.43944522199609,2.33068358199152,49.6282500000002));
#96253=CARTESIAN_POINT('Ctrl Pts',(-1.12236674703393,2.30288577939295,-0.219489327336945));
#96254=CARTESIAN_POINT('Ctrl Pts',(-1.889731631375,1.92889205520008,-0.166455904841186));
#96255=CARTESIAN_POINT('Ctrl Pts',(-3.00772136534351,0.359822456008,-0.0603890598496661));
#96256=CARTESIAN_POINT('Ctrl Pts',(-1.92664562308743,-2.34132064310475,
0.0987112076376125));
#96257=CARTESIAN_POINT('Ctrl Pts',(0.927249804294889,-2.88380409372784,
0.257811475124891));
#96258=CARTESIAN_POINT('Ctrl Pts',(2.92784522127986,-0.780306587535148,
0.416911742612171));
#96259=CARTESIAN_POINT('Ctrl Pts',(2.23897820574364,2.04207354288632,0.576012010099449));
#96260=CARTESIAN_POINT('Ctrl Pts',(-0.507463326542365,2.98715522008745,
0.735112277586729));
#96261=CARTESIAN_POINT('Ctrl Pts',(-2.78744873331352,1.188114072284,0.894212545074006));
#96262=CARTESIAN_POINT('Ctrl Pts',(-2.50637764055038,-1.70286310223525,
1.05331281256129));
#96263=CARTESIAN_POINT('Ctrl Pts',(0.0776488068570673,-3.02907538336238,
1.21241308004856));
#96264=CARTESIAN_POINT('Ctrl Pts',(2.59030281306776,-1.57219671546807,1.37151334753584));
#96265=CARTESIAN_POINT('Ctrl Pts',(2.72295613408236,1.32928328733925,1.53061361502312));
#96266=CARTESIAN_POINT('Ctrl Pts',(0.353702731598795,3.00937394922191,1.6897138825104));
#96267=CARTESIAN_POINT('Ctrl Pts',(-2.34053491620105,1.9244107020416,1.84881414999768));
#96268=CARTESIAN_POINT('Ctrl Pts',(-2.88425066053474,-0.928740121585945,
2.00791441748496));
#96269=CARTESIAN_POINT('Ctrl Pts',(-0.777865918911568,-2.92854544993387,
2.16701468497224));
#96270=CARTESIAN_POINT('Ctrl Pts',(2.04323491749396,-2.2375541324242,2.32611495245952));
#96271=CARTESIAN_POINT('Ctrl Pts',(2.98697646298292,0.509341455803217,2.48521521994679));
#96272=CARTESIAN_POINT('Ctrl Pts',(1.18623220564852,2.78824487032034,2.64431548743408));
#96273=CARTESIAN_POINT('Ctrl Pts',(-1.7044426413725,2.50526089027857,2.80341575492135));
#96274=CARTESIAN_POINT('Ctrl Pts',(-3.02904614676457,-0.0796002539131367,
2.96251602240864));
#96275=CARTESIAN_POINT('Ctrl Pts',(-1.57050962970762,-2.59132324542585,
3.12161628989591));
#96276=CARTESIAN_POINT('Ctrl Pts',(1.33103829202283,-2.72209364370382,3.28071655738319));
#96277=CARTESIAN_POINT('Ctrl Pts',(3.00960521121801,-0.351757294752259,
3.43981682487047));
#96278=CARTESIAN_POINT('Ctrl Pts',(1.92289479510493,2.34177973278295,3.59891709235775));
#96279=CARTESIAN_POINT('Ctrl Pts',(-0.93060462174736,2.88364903544351,3.75801735984503));
#96280=CARTESIAN_POINT('Ctrl Pts',(-2.92904841423869,0.775971716819205,
3.91711762733231));
#96281=CARTESIAN_POINT('Ctrl Pts',(-2.23623185283338,-2.04468183767635,
4.07621789481958));
#96282=CARTESIAN_POINT('Ctrl Pts',(0.511273219910781,-2.98664634887032,
4.23531816230686));
#96283=CARTESIAN_POINT('Ctrl Pts',(2.78901161367073,-1.18442852753634,4.39441842979414));
#96284=CARTESIAN_POINT('Ctrl Pts',(2.50415788883102,1.70606271447192,4.55351869728142));
#96285=CARTESIAN_POINT('Ctrl Pts',(-0.0815594243589275,3.02899402086515,
4.7126189647687));
#96286=CARTESIAN_POINT('Ctrl Pts',(-2.59233852754708,1.56883322142171,4.87171923225597));
#96287=CARTESIAN_POINT('Ctrl Pts',(-2.72123214602623,-1.33279868152171,
5.03081949974326));
#96288=CARTESIAN_POINT('Ctrl Pts',(-0.349810593385746,-3.00983209944,5.18991976723053));
#96289=CARTESIAN_POINT('Ctrl Pts',(2.34302298393151,-1.92137971645832,5.34902003471782));
#96290=CARTESIAN_POINT('Ctrl Pts',(2.88304651100131,0.932469588486375,5.50812030220509));
#96291=CARTESIAN_POINT('Ctrl Pts',(0.774077029136096,2.92954970447966,5.66722056969238));
#96292=CARTESIAN_POINT('Ctrl Pts',(-2.04612781807473,2.23490887289647,5.82632083717965));
#96293=CARTESIAN_POINT('Ctrl Pts',(-2.98631502950102,-0.513204893416967,
5.98542110466694));
#96294=CARTESIAN_POINT('Ctrl Pts',(-1.18262433072315,-2.78977712558423,
6.14452137215421));
#96295=CARTESIAN_POINT('Ctrl Pts',(1.7076820616722,-2.50305387362997,6.30362163964149));
#96296=CARTESIAN_POINT('Ctrl Pts',(3.0289406341336,0.0835185784442948,6.46272190712876));
#96297=CARTESIAN_POINT('Ctrl Pts',(1.56715615346209,2.59335271583274,6.62182217461605));
#96298=CARTESIAN_POINT('Ctrl Pts',(-1.33455851168292,2.72036951478026,6.78092244210331));
#96299=CARTESIAN_POINT('Ctrl Pts',(-3.01005772939279,0.347863743114754,
6.94002270959062));
#96300=CARTESIAN_POINT('Ctrl Pts',(-1.91986383350621,-2.34426525351674,
7.09912297707787));
#96301=CARTESIAN_POINT('Ctrl Pts',(0.934334164867162,-2.88244278111692,
7.25822324456517));
#96302=CARTESIAN_POINT('Ctrl Pts',(2.93004976925262,-0.772182017243212,
7.41732351205244));
#96303=CARTESIAN_POINT('Ctrl Pts',(2.23358495789849,2.0475729422662,7.57642377953972));
#96304=CARTESIAN_POINT('Ctrl Pts',(-0.515136352183505,2.98598246088455,
7.735524047027));
#96305=CARTESIAN_POINT('Ctrl Pts',(-2.7905414703915,1.18081963909664,7.89462431451428));
#96306=CARTESIAN_POINT('Ctrl Pts',(-2.50194881124659,-1.7093006944224,8.05372458200156));
#96307=CARTESIAN_POINT('Ctrl Pts',(0.0854776975837867,-3.02888598023545,
8.21282484948884));
#96308=CARTESIAN_POINT('Ctrl Pts',(2.59436581917158,-1.56547842986266,8.37192511697612));
#96309=CARTESIAN_POINT('Ctrl Pts',(2.71950574544478,1.33631778351705,8.53102538446339));
#96310=CARTESIAN_POINT('Ctrl Pts',(0.34591674731299,3.01028210006628,8.69012565195066));
#96311=CARTESIAN_POINT('Ctrl Pts',(-2.34550654236051,1.91834714736283,8.84922591943796));
#96312=CARTESIAN_POINT('Ctrl Pts',(-2.88183784533965,-0.936198350361311,
9.00832618692522));
#96313=CARTESIAN_POINT('Ctrl Pts',(-0.770286682302,-2.93054860821643,9.16742645441252));
#96314=CARTESIAN_POINT('Ctrl Pts',(2.04901720983943,-2.23226010846248,9.32652672189978));
#96315=CARTESIAN_POINT('Ctrl Pts',(2.98564864305873,0.517067595438605,9.48562698938708));
#96316=CARTESIAN_POINT('Ctrl Pts',(1.17901445346493,2.79130464775379,9.64472725687434));
#96317=CARTESIAN_POINT('Ctrl Pts',(-1.71091861207316,2.50084270215316,9.80382752436164));
#96318=CARTESIAN_POINT('Ctrl Pts',(-3.02883005917894,-0.0874367809629802,
9.96292779184889));
#96319=CARTESIAN_POINT('Ctrl Pts',(-1.563800051333,-2.59537783713701,10.1220280593362));
#96320=CARTESIAN_POINT('Ctrl Pts',(1.33807649629206,-2.71864083838264,10.2811283268235));
#96321=CARTESIAN_POINT('Ctrl Pts',(3.01050521136452,-0.343969606794242,
10.4402285943107));
#96322=CARTESIAN_POINT('Ctrl Pts',(1.91682965866379,2.34674684994312,10.599328861798));
#96323=CARTESIAN_POINT('Ctrl Pts',(-0.938062144189482,2.88123170392277,
10.7584291292853));
#96324=CARTESIAN_POINT('Ctrl Pts',(-2.93104622116212,0.768391025105277,
10.9175293967726));
#96325=CARTESIAN_POINT('Ctrl Pts',(-2.23093432514284,-2.05046062019015,
11.0766296642599));
#96326=CARTESIAN_POINT('Ctrl Pts',(0.518998622374394,-2.98531357616324,
11.2357299317471));
#96327=CARTESIAN_POINT('Ctrl Pts',(2.79206665735174,-1.17720877458324,11.3948301992344));
#96328=CARTESIAN_POINT('Ctrl Pts',(2.49973554681248,1.71253581394761,11.5539304667217));
#96329=CARTESIAN_POINT('Ctrl Pts',(-0.0893958277622967,3.02877287098748,
11.713030734209));
#96330=CARTESIAN_POINT('Ctrl Pts',(-2.59638876930565,1.56212101857525,11.8721310016962));
#96331=CARTESIAN_POINT('Ctrl Pts',(-2.71777479395565,-1.33983464927223,
12.0312312691835));
#96332=CARTESIAN_POINT('Ctrl Pts',(-0.342022322373068,-3.01072706319415,
12.1903315366708));
#96333=CARTESIAN_POINT('Ctrl Pts',(2.34798617574567,-1.91531136804392,12.3494318041581));
#96334=CARTESIAN_POINT('Ctrl Pts',(2.88062435711988,0.939925545571957,12.5085320716454));
#96335=CARTESIAN_POINT('Ctrl Pts',(0.766495046446107,2.93154260788151,12.6676323391327));
#96336=CARTESIAN_POINT('Ctrl Pts',(-2.05190317271449,2.22960760849421,12.8267326066199));
#96337=CARTESIAN_POINT('Ctrl Pts',(-2.98497726033827,-0.520929432183016,
12.9858328741072));
#96338=CARTESIAN_POINT('Ctrl Pts',(-1.17540260320696,-2.79282749886659,
13.1449331415945));
#96339=CARTESIAN_POINT('Ctrl Pts',(1.71415229936921,-2.49862734568769,13.3040334090818));
#96340=CARTESIAN_POINT('Ctrl Pts',(3.02871441568501,0.0913548371621723,
13.463133676569));
#96341=CARTESIAN_POINT('Ctrl Pts',(1.56044133229185,2.59739861525457,13.6222339440563));
#96342=CARTESIAN_POINT('Ctrl Pts',(-1.34159224172202,2.71690761252612,13.7813342115436));
#96343=CARTESIAN_POINT('Ctrl Pts',(-3.01094765546235,0.34007489486417,13.9404344790309));
#96344=CARTESIAN_POINT('Ctrl Pts',(-1.91379227613845,-2.34922451924968,
14.0995347465181));
#96345=CARTESIAN_POINT('Ctrl Pts',(0.941788553729176,-2.88001580518507,
14.2586350140054));
#96346=CARTESIAN_POINT('Ctrl Pts',(2.9320377681669,-0.764598747117689,14.4177352814927));
#96347=CARTESIAN_POINT('Ctrl Pts',(2.22827995907167,2.05334486680895,14.57683554898));
#96348=CARTESIAN_POINT('Ctrl Pts',(-0.522860024056705,2.98463969572451,
14.7359358164673));
#96349=CARTESIAN_POINT('Ctrl Pts',(-2.79358717198003,1.17359594009171,14.8950360839545));
#96350=CARTESIAN_POINT('Ctrl Pts',(-2.49751809924244,-1.71576806766168,
15.0541363514418));
#96351=CARTESIAN_POINT('Ctrl Pts',(0.0933138083430479,-3.02865469329595,
15.2132366189291));
#96352=CARTESIAN_POINT('Ctrl Pts',(2.59840737456129,-1.55876099318549,15.3723368864164));
#96353=CARTESIAN_POINT('Ctrl Pts',(2.71603929445686,1.34334927290609,15.5314371539037));
#96354=CARTESIAN_POINT('Ctrl Pts',(0.338127325082262,3.01116698807685,15.6905374213909));
#96355=CARTESIAN_POINT('Ctrl Pts',(-2.35046187993708,1.91227238358288,15.8496376888782));
#96356=CARTESIAN_POINT('Ctrl Pts',(-2.87940604837291,-0.943651167881714,
16.0087379563655));
#96357=CARTESIAN_POINT('Ctrl Pts',(-0.762702127913354,-2.93253170181117,
16.1678382238528));
#96358=CARTESIAN_POINT('Ctrl Pts',(2.05478570187039,-2.22695137743062,16.32693849134));
#96359=CARTESIAN_POINT('Ctrl Pts',(2.98430088246319,0.52479039718779,16.4860387588273));
#96360=CARTESIAN_POINT('Ctrl Pts',(1.17178878599336,2.79434567637422,16.6451390263146));
#96361=CARTESIAN_POINT('Ctrl Pts',(-1.71738311814903,2.4964078079408,16.8042392938019));
#96362=CARTESIAN_POINT('Ctrl Pts',(-3.02859370384532,-0.0952727404853469,
16.9633395612892));
#96363=CARTESIAN_POINT('Ctrl Pts',(-1.55708000195918,-2.59941504680378,
17.1224398287764));
#96364=CARTESIAN_POINT('Ctrl Pts',(1.3451057420894,-2.71516984011115,17.2815400962637));
#96365=CARTESIAN_POINT('Ctrl Pts',(3.01138506094589,-0.336179613842111,
17.440640363751));
#96366=CARTESIAN_POINT('Ctrl Pts',(1.91075169101307,2.3516982572902,17.5997406312383));
#96367=CARTESIAN_POINT('Ctrl Pts',(-0.945513387250341,2.87879508693854,
17.7588408987256));
#96368=CARTESIAN_POINT('Ctrl Pts',(-2.93302440860768,0.760805189626565,
17.9179411662128));
#96369=CARTESIAN_POINT('Ctrl Pts',(-2.22562186412688,-2.05622567729603,
18.0770414337001));
#96370=CARTESIAN_POINT('Ctrl Pts',(0.526720550768654,-2.98396082069605,
18.2361417011874));
#96371=CARTESIAN_POINT('Ctrl Pts',(2.79510301173186,-1.16998114166793,18.3952419686747));
#96372=CARTESIAN_POINT('Ctrl Pts',(2.49529647224726,1.71899745015561,18.554342236162));
#96373=CARTESIAN_POINT('Ctrl Pts',(-0.0972316327695509,3.02853144735862,
18.7134425036492));
#96374=CARTESIAN_POINT('Ctrl Pts',(-2.60042163156048,1.55539835931616,18.8725427711365));
#96375=CARTESIAN_POINT('Ctrl Pts',(-2.7142992498527,-1.34686164853714,19.0316430386238));
#96376=CARTESIAN_POINT('Ctrl Pts',(-0.334231761958541,-3.01160187397823,
19.1907433061111));
#96377=CARTESIAN_POINT('Ctrl Pts',(2.35293365079182,-1.90923019906519,19.3498435735984));
#96378=CARTESIAN_POINT('Ctrl Pts',(2.87818292113752,0.947375211056012,19.5089438410856));
#96379=CARTESIAN_POINT('Ctrl Pts',(0.758907933050889,2.93351588835028,19.6680441085729));
#96380=CARTESIAN_POINT('Ctrl Pts',(-2.05766479248342,2.22429141971667,19.8271443760602));
#96381=CARTESIAN_POINT('Ctrl Pts',(-2.98361951056537,-0.528650483991836,
19.9862446435475));
#96382=CARTESIAN_POINT('Ctrl Pts',(-1.16817300787164,-2.79585917773611,
20.1453449110348));
#96383=CARTESIAN_POINT('Ctrl Pts',(1.72061106300608,-2.49418409262673,20.304445178522));
#96384=CARTESIAN_POINT('Ctrl Pts',(3.02846792386189,0.0991904843761558,
20.4635454460093));
#96385=CARTESIAN_POINT('Ctrl Pts',(1.55371606595995,2.60142712841028,20.6226457134966));
#96386=CARTESIAN_POINT('Ctrl Pts',(-1.34861699151466,2.71342752404575,20.7817459809838));
#96387=CARTESIAN_POINT('Ctrl Pts',(-3.01181742708317,0.332283770246491,
20.9408462484712));
#96388=CARTESIAN_POINT('Ctrl Pts',(-1.90770790837581,-2.35416805992508,
21.0999465159584));
#96389=CARTESIAN_POINT('Ctrl Pts',(0.949236638519778,-2.87756955122596,
21.2590467834457));
#96390=CARTESIAN_POINT('Ctrl Pts',(2.93400614083337,-0.757010358980113,
21.418147050933));
#96391=CARTESIAN_POINT('Ctrl Pts',(2.22296004475659,2.05910304683056,21.5772473184203));
#96392=CARTESIAN_POINT('Ctrl Pts',(-0.530580196049953,2.98327695221391,
21.7363475859076));
#96393=CARTESIAN_POINT('Ctrl Pts',(-2.79661417407061,1.16636438536093,21.8954478533948));
#96394=CARTESIAN_POINT('Ctrl Pts',(-2.49307066954462,-1.72222395602531,
22.0545481208821));
#96395=CARTESIAN_POINT('Ctrl Pts',(0.101149294485621,-3.02840313338171,
22.2136483883694));
#96396=CARTESIAN_POINT('Ctrl Pts',(2.60243153693252,-1.55203312259438,22.3727486558567));
#96397=CARTESIAN_POINT('Ctrl Pts',(2.71255466305499,1.35037177028763,22.5318489233439));
#96398=CARTESIAN_POINT('Ctrl Pts',(0.330335639520905,3.01203172017053,22.6909491908313));
#96399=CARTESIAN_POINT('Ctrl Pts',(-2.35540148417356,1.90618481958177,22.8500494583184));
#96400=CARTESIAN_POINT('Ctrl Pts',(-2.87695497746049,-0.951097668862907,
23.0091497258058));
#96401=CARTESIAN_POINT('Ctrl Pts',(-0.755112468208078,-2.93449516585184,
23.168249993293));
#96402=CARTESIAN_POINT('Ctrl Pts',(2.06054043973563,-2.22162773980366,23.3273502607804));
#96403=CARTESIAN_POINT('Ctrl Pts',(2.98293314578502,0.532509686135592,23.4864505282676));
#96404=CARTESIAN_POINT('Ctrl Pts',(1.16455527489253,2.79736800041952,23.6455507957549));
#96405=CARTESIAN_POINT('Ctrl Pts',(-1.72383612853853,2.49195620346673,23.8046510632421));
#96406=CARTESIAN_POINT('Ctrl Pts',(-3.0283370759452,-0.103108062278441,
23.9637513307295));
#96407=CARTESIAN_POINT('Ctrl Pts',(-1.55034952992354,-2.603434856707,24.1228515982167));
#96408=CARTESIAN_POINT('Ctrl Pts',(1.35212598412189,-2.71168066724558,24.281951865704));
#96409=CARTESIAN_POINT('Ctrl Pts',(3.01224475315065,-0.328387370596837,
24.4410521331913));
#96410=CARTESIAN_POINT('Ctrl Pts',(1.90466093332031,2.35663392302125,24.6001524006786));
#96411=CARTESIAN_POINT('Ctrl Pts',(-0.952958301306824,2.87633920009819,
24.7592526681658));
#96412=CARTESIAN_POINT('Ctrl Pts',(-2.93498296320111,0.75321426152879,24.9183529356531));
#96413=CARTESIAN_POINT('Ctrl Pts',(-2.22029450541524,-2.06197697059738,
25.0774532031404));
#96414=CARTESIAN_POINT('Ctrl Pts',(0.534438953441636,-2.9825880914225,25.2365534706277));
#96415=CARTESIAN_POINT('Ctrl Pts',(2.79812065646745,-1.16274567722322,25.395653738115));
#96416=CARTESIAN_POINT('Ctrl Pts',(2.4908406948593,1.72544757987134,25.5547540056022));
#96417=CARTESIAN_POINT('Ctrl Pts',(-0.105066786935228,3.02826975157997,
25.7138542730895));
#96418=CARTESIAN_POINT('Ctrl Pts',(-2.60443708731396,1.54866528865171,25.8729545405768));
#96419=CARTESIAN_POINT('Ctrl Pts',(-2.71080553698318,-1.3538796322836,26.0320548080641));
#96420=CARTESIAN_POINT('Ctrl Pts',(-0.326438964289283,-3.01245652593442,
26.1911550755514));
#96421=CARTESIAN_POINT('Ctrl Pts',(2.35786537595255,-1.90313625022889,26.3502553430386));
#96422=CARTESIAN_POINT('Ctrl Pts',(2.8757222193967,0.954818535073085,26.5093556105259));
#96423=CARTESIAN_POINT('Ctrl Pts',(0.751315739736407,2.93546953267709,26.6684558780132));
#96424=CARTESIAN_POINT('Ctrl Pts',(-2.06341263881479,2.21896034214911,26.8275561455005));
#96425=CARTESIAN_POINT('Ctrl Pts',(-2.98224178927072,-0.536367997160897,
26.9866564129878));
#96426=CARTESIAN_POINT('Ctrl Pts',(-1.16093559311012,-2.79887214189952,
27.145756680475));
#96427=CARTESIAN_POINT('Ctrl Pts',(1.72705830934953,-2.48972414418904,27.3048569479623));
#96428=CARTESIAN_POINT('Ctrl Pts',(3.02820116031421,0.107025467636496,27.4639572154496));
#96429=CARTESIAN_POINT('Ctrl Pts',(1.54698039948354,2.60543822833412,27.6230574829369));
#96430=CARTESIAN_POINT('Ctrl Pts',(-1.35563271403909,2.70992927263389,27.7821577504241));
#96431=CARTESIAN_POINT('Ctrl Pts',(-3.01266703843323,0.324490421413414,
27.9412580179114));
#96432=CARTESIAN_POINT('Ctrl Pts',(-1.90161077094541,-2.35909584245226,
28.1003582853987));
#96433=CARTESIAN_POINT('Ctrl Pts',(0.956678369383513,-2.87510403561414,
28.2594585528859));
#96434=CARTESIAN_POINT('Ctrl Pts',(2.93595487407624,-0.749416903625118,
28.4185588203733));
#96435=CARTESIAN_POINT('Ctrl Pts',(2.21762525056339,2.06484744378726,28.5776590878605));
#96436=CARTESIAN_POINT('Ctrl Pts',(-0.538296816486407,2.98189423947457,
28.7367593553478));
#96437=CARTESIAN_POINT('Ctrl Pts',(-2.79962245640135,1.15912502331042,28.8958596228351));
#96438=CARTESIAN_POINT('Ctrl Pts',(-2.48860655192302,-1.72866831629926,
29.0549598903224));
#96439=CARTESIAN_POINT('Ctrl Pts',(0.10898410356279,-3.02813130217658,29.2140601578096));
#96440=CARTESIAN_POINT('Ctrl Pts',(2.60643827934863,-1.54529486312395,29.3731604252969));
#96441=CARTESIAN_POINT('Ctrl Pts',(2.70905187456434,1.35738522865492,29.5322606927842));
#96442=CARTESIAN_POINT('Ctrl Pts',(0.322541742784441,3.01287629055901,29.6913609602715));
#96443=CARTESIAN_POINT('Ctrl Pts',(-2.3603253220056,1.90008449610808,29.8504612277587));
#96444=CARTESIAN_POINT('Ctrl Pts',(-2.87448464900915,-0.958537803459974,
30.0095614952461));
#96445=CARTESIAN_POINT('Ctrl Pts',(-0.747517753989358,-2.93643898719551,
30.1686617627333));
#96446=CARTESIAN_POINT('Ctrl Pts',(2.0662813849145,-2.21628923121666,30.3277620302206));
#96447=CARTESIAN_POINT('Ctrl Pts',(2.98154544217944,0.540225410611193,30.4868622977078));
#96448=CARTESIAN_POINT('Ctrl Pts',(1.15731396858162,2.80037159965905,30.6459625651952));
#96449=CARTESIAN_POINT('Ctrl Pts',(-1.73027760004697,2.48748791852882,30.8050628326824));
#96450=CARTESIAN_POINT('Ctrl Pts',(-3.02806017719635,-0.110942693894748,
30.9641631001697));
#96451=CARTESIAN_POINT('Ctrl Pts',(-1.54360868027803,-2.60743723993914,
31.123263367657));
#96452=CARTESIAN_POINT('Ctrl Pts',(1.35913717539795,-2.70817334314153,31.2823636351443));
#96453=CARTESIAN_POINT('Ctrl Pts',(3.01308428222424,-0.320592929217562,
31.4414639026316));
#96454=CARTESIAN_POINT('Ctrl Pts',(1.89855742635539,2.36155381409824,31.6005641701188));
#96455=CARTESIAN_POINT('Ctrl Pts',(-0.960396836524605,2.8738640598408,31.7596644376061));
#96456=CARTESIAN_POINT('Ctrl Pts',(-2.93692187183235,0.74561829162367,31.9187647050934));
#96457=CARTESIAN_POINT('Ctrl Pts',(-2.21495228466786,-2.0677144615966,32.0778649725806));
#96458=CARTESIAN_POINT('Ctrl Pts',(0.542153778728399,-2.98119539753127,
32.236965240068));
#96459=CARTESIAN_POINT('Ctrl Pts',(2.80111957135917,-1.15550242968141,32.3960655075552));
#96460=CARTESIAN_POINT('Ctrl Pts',(2.48636824447444,1.73188615991936,32.5551657750425));
#96461=CARTESIAN_POINT('Ctrl Pts',(-0.112901237812935,3.02798778540327,
32.7142660425298));
#96462=CARTESIAN_POINT('Ctrl Pts',(-2.60843510968768,1.54192185165126,32.8733663100171));
#96463=CARTESIAN_POINT('Ctrl Pts',(-2.70729367873307,-1.36088855353519,
33.0324665775044));
#96464=CARTESIAN_POINT('Ctrl Pts',(-0.318643981528126,-3.01329101334189,
33.1915668449916));
#96465=CARTESIAN_POINT('Ctrl Pts',(2.3627813182162,-1.89702956232622,33.3506671124789));
#96466=CARTESIAN_POINT('Ctrl Pts',(2.87324226836875,0.962255467799642,33.5097673799662));
#96467=CARTESIAN_POINT('Ctrl Pts',(0.743718517322665,2.93740352778477,33.6688676474535));
#96468=CARTESIAN_POINT('Ctrl Pts',(-2.06914667323407,2.21361441147628,33.8279679149407));
#96469=CARTESIAN_POINT('Ctrl Pts',(-2.98084410567647,-0.544081920031316,
33.987068182428));
#96470=CARTESIAN_POINT('Ctrl Pts',(-1.15369040736763,-2.80186637118884,
34.1461684499153));
#96471=CARTESIAN_POINT('Ctrl Pts',(1.73349399524354,-2.48524753022827,34.3052687174026));
#96472=CARTESIAN_POINT('Ctrl Pts',(3.0279141268276,0.11485973449802,34.4643689848899));
#96473=CARTESIAN_POINT('Ctrl Pts',(1.5402343779493,2.60943188817684,34.6234692523771));
#96474=CARTESIAN_POINT('Ctrl Pts',(-1.36263936233399,2.70641288170692,34.7825695198644));
#96475=CARTESIAN_POINT('Ctrl Pts',(-3.01349648382547,0.316694900531439,
34.9416697873517));
#96476=CARTESIAN_POINT('Ctrl Pts',(-1.89550090465978,-2.36400783384594,
35.100770054839));
#96477=CARTESIAN_POINT('Ctrl Pts',(0.964113696507479,-2.87261927485314,
35.2598703223262));
#96478=CARTESIAN_POINT('Ctrl Pts',(2.93788395485126,-0.741818431881178,
35.4189705898135));
#96479=CARTESIAN_POINT('Ctrl Pts',(2.21227561220165,2.07057801922768,35.5780708573008));
#96480=CARTESIAN_POINT('Ctrl Pts',(-0.546009833713229,2.98049156676203,
35.7371711247881));
#96481=CARTESIAN_POINT('Ctrl Pts',(-2.80261199883563,1.15187790239839,35.8962713922753));
#96482=CARTESIAN_POINT('Ctrl Pts',(-2.48412577625919,-1.73510110534684,
36.0553716597627));
#96483=CARTESIAN_POINT('Ctrl Pts',(0.116818183130627,-3.02783920150017,
36.2144719272499));
#96484=CARTESIAN_POINT('Ctrl Pts',(2.61042757498959,-1.53854625987814,36.3735721947372));
#96485=CARTESIAN_POINT('Ctrl Pts',(2.70553095243158,1.36438960106188,36.5326724622244));
#96486=CARTESIAN_POINT('Ctrl Pts',(0.314745687042946,3.01370069358903,36.6917727297118));
#96487=CARTESIAN_POINT('Ctrl Pts',(-2.36523336047438,1.89397145399557,36.850872997199));
#96488=CARTESIAN_POINT('Ctrl Pts',(-2.87199507955459,-0.96597152187078,
37.0099732646863));
#96489=CARTESIAN_POINT('Ctrl Pts',(-0.739918036094069,-2.93836315283081,
37.1690735321736));
#96490=CARTESIAN_POINT('Ctrl Pts',(2.07200849897867,-2.21093588740406,37.3281737996609));
#96491=CARTESIAN_POINT('Ctrl Pts',(2.98013778093542,0.54793751896766,37.4872740671482));
#96492=CARTESIAN_POINT('Ctrl Pts',(1.15006491553191,2.80335645398756,37.6463743346354));
#96493=CARTESIAN_POINT('Ctrl Pts',(-1.73670748955686,2.48300298303649,37.8054746021227));
#96494=CARTESIAN_POINT('Ctrl Pts',(-3.02776300945232,-0.11877658289139,
37.96457486961));
#96495=CARTESIAN_POINT('Ctrl Pts',(-1.53685749814404,-2.61142216970936,
38.1236751370973));
#96496=CARTESIAN_POINT('Ctrl Pts',(1.36613926898657,-2.70464789127603,38.2827754045845));
#96497=CARTESIAN_POINT('Ctrl Pts',(3.01390364254712,-0.312796341878149,
38.4418756720718));
#96498=CARTESIAN_POINT('Ctrl Pts',(1.89244121097349,2.36645789758878,38.6009759395591));
#96499=CARTESIAN_POINT('Ctrl Pts',(-0.967828943112242,2.87136968273423,
38.7600762070464));
#96500=CARTESIAN_POINT('Ctrl Pts',(-2.93884112152294,0.738017330756449,
38.9191764745336));
#96501=CARTESIAN_POINT('Ctrl Pts',(-2.20959523764404,-2.07343811188851,
39.0782767420209));
#96502=CARTESIAN_POINT('Ctrl Pts',(0.549864974988074,-2.97978274834466,
39.2373770095082));
#96503=CARTESIAN_POINT('Ctrl Pts',(2.80409973633321,-1.14825144752673,39.3964772769955));
#96504=CARTESIAN_POINT('Ctrl Pts',(2.48187915102991,1.73831314720165,39.5555775444828));
#96505=CARTESIAN_POINT('Ctrl Pts',(-0.120734932961047,3.02768555071591,
39.7146778119701));
#96506=CARTESIAN_POINT('Ctrl Pts',(-2.61241567192003,1.5351680934535,39.8737780794573));
#96507=CARTESIAN_POINT('Ctrl Pts',(-2.70376369860974,-1.36788836537608,
40.0328783469446));
#96508=CARTESIAN_POINT('Ctrl Pts',(-0.310846865852554,-3.01410533061485,
40.1919786144319));
#96509=CARTESIAN_POINT('Ctrl Pts',(2.36768144467684,-1.8909101762337,40.3510788819192));
#96510=CARTESIAN_POINT('Ctrl Pts',(2.87074308465372,0.969685959454866,40.5101791494065));
#96511=CARTESIAN_POINT('Ctrl Pts',(0.736116316663445,2.9393178607277,40.6692794168937));
#96512=CARTESIAN_POINT('Ctrl Pts',(-2.07486685735924,2.20825366348239,40.828379684381));
#96513=CARTESIAN_POINT('Ctrl Pts',(-2.97942646913829,-0.551792200968217,
40.9874799518683));
#96514=CARTESIAN_POINT('Ctrl Pts',(-1.14643749914141,-2.8048418455616,41.1465802193556));
#96515=CARTESIAN_POINT('Ctrl Pts',(1.7399180776094,-2.4807542807096,41.3056804868429));
#96516=CARTESIAN_POINT('Ctrl Pts',(3.02760682532339,0.122693232520313,41.4647807543301));
#96517=CARTESIAN_POINT('Ctrl Pts',(1.53347804651323,2.61340808120603,41.6238810218174));
#96518=CARTESIAN_POINT('Ctrl Pts',(-1.36963688949883,2.70287837480253,41.7829812893047));
#96519=CARTESIAN_POINT('Ctrl Pts',(-3.01430575770784,0.308897259781596,
41.942081556792));
#96520=CARTESIAN_POINT('Ctrl Pts',(-1.88937835041663,-2.36890400122672,
42.1011818242792));
#96521=CARTESIAN_POINT('Ctrl Pts',(0.971542570121709,-2.87011528557518,
42.2602820917666));
#96522=CARTESIAN_POINT('Ctrl Pts',(2.93979337024567,-0.73421499461035,42.4193823592538));
#96523=CARTESIAN_POINT('Ctrl Pts',(2.2069111654804,2.07629473479296,42.578482626741));
#96524=CARTESIAN_POINT('Ctrl Pts',(-0.553719196101618,2.97906894346535,
42.7375828942284));
#96525=CARTESIAN_POINT('Ctrl Pts',(-2.8055827813623,1.14462307113504,42.8966831617156));
#96526=CARTESIAN_POINT('Ctrl Pts',(-2.47962837254616,-1.74152228010872,
43.0557834292029));
#96527=CARTESIAN_POINT('Ctrl Pts',(0.124651480749879,-3.02752683330764,
43.2148836966902));
#96528=CARTESIAN_POINT('Ctrl Pts',(2.61439939715218,-1.53178735803035,43.3739839641774));
#96529=CARTESIAN_POINT('Ctrl Pts',(2.70199192022476,1.37138484062318,43.5330842316648));
#96530=CARTESIAN_POINT('Ctrl Pts',(0.306947524481237,3.01450492374214,43.692184499152));
#96531=CARTESIAN_POINT('Ctrl Pts',(-2.37012556672716,1.88784573416347,43.8512847666393));
#96532=CARTESIAN_POINT('Ctrl Pts',(-2.86948628576077,-0.973398774336397,
44.0103850341266));
#96533=CARTESIAN_POINT('Ctrl Pts',(-0.732313365393594,-2.94026764987723,
44.1694853016138));
#96534=CARTESIAN_POINT('Ctrl Pts',(2.07772174359431,-2.20556774420093,44.3285855691012));
#96535=CARTESIAN_POINT('Ctrl Pts',(2.97871017147186,0.555645959584653,44.4876858365884));
#96536=CARTESIAN_POINT('Ctrl Pts',(1.14280816427329,2.80632254342081,44.6467861040757));
#96537=CARTESIAN_POINT('Ctrl Pts',(-1.74312575404136,2.47850142701921,44.8058863715629));
#96538=CARTESIAN_POINT('Ctrl Pts',(-3.02744557467754,-0.126609676846878,
44.9649866390503));
#96539=CARTESIAN_POINT('Ctrl Pts',(-1.53009602875911,-2.61538961931251,
45.1240869065375));
#96540=CARTESIAN_POINT('Ctrl Pts',(1.37313221810741,-2.70110433530689,45.2831871740248));
#96541=CARTESIAN_POINT('Ctrl Pts',(3.01470282846356,-0.304997660653436,
45.4422874415121));
#96542=CARTESIAN_POINT('Ctrl Pts',(1.88631232844131,2.37134614045018,45.6013877089993));
#96543=CARTESIAN_POINT('Ctrl Pts',(-0.97525457194413,2.86885608588752,45.7604879764867));
#96544=CARTESIAN_POINT('Ctrl Pts',(-2.9407406982379,0.730411429019182,45.9195882439739));
#96545=CARTESIAN_POINT('Ctrl Pts',(-2.20422340246865,-2.07914788166006,
46.0786885114613));
#96546=CARTESIAN_POINT('Ctrl Pts',(0.557572494927398,-2.97835015618116,
46.2377887789484));
#96547=CARTESIAN_POINT('Ctrl Pts',(2.80706112319388,-1.14099277383441,46.3968890464358));
#96548=CARTESIAN_POINT('Ctrl Pts',(2.47737346030718,1.7447284882806,46.555989313923));
#96549=CARTESIAN_POINT('Ctrl Pts',(-0.128567849955195,3.02736306941306,
46.7150895814104));
#96550=CARTESIAN_POINT('Ctrl Pts',(-2.61637869011417,1.52840402135752,46.8741898488976));
#96551=CARTESIAN_POINT('Ctrl Pts',(-2.70021572945777,-1.37487894863602,
47.0332901163849));
#96552=CARTESIAN_POINT('Ctrl Pts',(-0.303047461110431,-3.01489961025401,
47.1923903838722));
#96553=CARTESIAN_POINT('Ctrl Pts',(2.37256532509137,-1.88477786975195,47.3514906513594));
#96554=CARTESIAN_POINT('Ctrl Pts',(2.86822544315535,0.977109458287476,47.5105909188468));
#96555=CARTESIAN_POINT('Ctrl Pts',(0.728507742327304,2.9412134763491,47.669691186334));
#96556=CARTESIAN_POINT('Ctrl Pts',(-2.08057039385854,2.20287630719366,47.8287914538213));
#96557=CARTESIAN_POINT('Ctrl Pts',(-2.97799415238172,-0.55949530339084,
47.9878917213085));
#96558=CARTESIAN_POINT('Ctrl Pts',(-1.1391668766645,-2.80780519314034,48.1469919887959));
#96559=CARTESIAN_POINT('Ctrl Pts',(1.74631136021662,-2.47623174369378,48.306092256283));
#96560=CARTESIAN_POINT('Ctrl Pts',(3.0273157952168,0.130501716601606,48.4651925237705));
#96561=CARTESIAN_POINT('Ctrl Pts',(1.52664175010871,2.6174129319684,48.6242927912576));
#96562=CARTESIAN_POINT('Ctrl Pts',(-1.37649228204864,2.69923773205355,48.783393058745));
#96563=CARTESIAN_POINT('Ctrl Pts',(-3.01534854262687,0.301265542054237,
48.9424933262322));
#96564=CARTESIAN_POINT('Ctrl Pts',(-1.88275888504304,-2.37410509268517,
49.1015935937195));
#96565=CARTESIAN_POINT('Ctrl Pts',(0.978038327691813,-2.86697737698299,
49.2606938612068));
#96566=CARTESIAN_POINT('Ctrl Pts',(2.94347543107135,-0.727803611882825,
49.419794128694));
#96567=CARTESIAN_POINT('Ctrl Pts',(2.19789667042551,2.08449280102471,49.5788943961813));
#96568=CARTESIAN_POINT('Ctrl Pts',(0.364205816777854,2.67564278674459,49.6849612411729));
#96569=CARTESIAN_POINT('Ctrl Pts',(-0.474664453624529,2.51747565713019,
49.7379946636686));
#96570=CARTESIAN_POINT('Ctrl Pts',(-1.20564430054339,2.47375567929515,-0.109744663668484));
#96571=CARTESIAN_POINT('Ctrl Pts',(-2.0299462514768,2.07201230690486,-0.0567112411727241));
#96572=CARTESIAN_POINT('Ctrl Pts',(-3.23088877261529,0.386520622104858,
0.049355603818795));
#96573=CARTESIAN_POINT('Ctrl Pts',(-2.06959919365079,-2.51504233938102,
0.208455871306074));
#96574=CARTESIAN_POINT('Ctrl Pts',(0.996050038619305,-3.09777706678723,
0.367556138793353));
#96575=CARTESIAN_POINT('Ctrl Pts',(3.1450859652048,-0.838203904761194,0.526656406280632));
#96576=CARTESIAN_POINT('Ctrl Pts',(2.40510628092737,2.19359165333219,0.685756673767911));
#96577=CARTESIAN_POINT('Ctrl Pts',(-0.545116174367747,3.20879665711233,
0.844856941255189));
#96578=CARTESIAN_POINT('Ctrl Pts',(-2.99427231540609,1.27626995670517,1.00395720874247));
#96579=CARTESIAN_POINT('Ctrl Pts',(-2.69234626321946,-1.82921242030833,
1.16305747622975));
#96580=CARTESIAN_POINT('Ctrl Pts',(0.0834102058696828,-3.25382721959455,
1.32215774371703));
#96581=CARTESIAN_POINT('Ctrl Pts',(2.78249852956668,-1.6888508273664,1.4812580112043));
#96582=CARTESIAN_POINT('Ctrl Pts',(2.92499448363151,1.42791366852541,1.64035827869159));
#96583=CARTESIAN_POINT('Ctrl Pts',(0.379946825371875,3.2326639751856,1.79945854617886));
#96584=CARTESIAN_POINT('Ctrl Pts',(-2.51419831298256,2.0671984455636,1.95855881366614));
#96585=CARTESIAN_POINT('Ctrl Pts',(-3.09825676803193,-0.997650934719184,
2.11765908115342));
#96586=CARTESIAN_POINT('Ctrl Pts',(-0.83558214300345,-3.14583814954029,
2.2767593486407));
#96587=CARTESIAN_POINT('Ctrl Pts',(2.19483919980503,-2.40357654398027,2.43585961612798));
#96588=CARTESIAN_POINT('Ctrl Pts',(3.20860463655859,0.54713365737409,2.59495988361525));
#96589=CARTESIAN_POINT('Ctrl Pts',(1.27424845901785,2.99512752431821,2.75406015110254));
#96590=CARTESIAN_POINT('Ctrl Pts',(-1.8309091583517,2.69114665212629,2.91316041858981));
#96591=CARTESIAN_POINT('Ctrl Pts',(-3.25379581369482,-0.085506446717136,
3.0722606860771));
#96592=CARTESIAN_POINT('Ctrl Pts',(-1.6870385629377,-2.78359467613364,3.23136095356437));
#96593=CARTESIAN_POINT('Ctrl Pts',(1.42979889133674,-2.92406799804922,3.39046122105165));
#96594=CARTESIAN_POINT('Ctrl Pts',(3.23291239639753,-0.377857040680476,
3.54956148853893));
#96595=CARTESIAN_POINT('Ctrl Pts',(2.06557006111335,2.51553549267108,3.70866175602621));
#96596=CARTESIAN_POINT('Ctrl Pts',(-0.999653777371921,3.09761050346267,
3.86776202351349));
#96597=CARTESIAN_POINT('Ctrl Pts',(-3.14637843287376,0.833547394590984,
4.02686229100077));
#96598=CARTESIAN_POINT('Ctrl Pts',(-2.40215615366969,-2.19639347881041,
4.18596255848805));
#96599=CARTESIAN_POINT('Ctrl Pts',(0.549208754834378,-3.20825002858447,
4.34506282597533));
#96600=CARTESIAN_POINT('Ctrl Pts',(2.99595115861851,-1.27231095129882,4.5041630934626));
#96601=CARTESIAN_POINT('Ctrl Pts',(2.68996180999494,1.83264943790287,4.66326336094988));
#96602=CARTESIAN_POINT('Ctrl Pts',(-0.0876109840156688,3.2537398201493,
4.82236362843716));
#96603=CARTESIAN_POINT('Ctrl Pts',(-2.7846852903256,1.68523776823255,4.98146389592444));
#96604=CARTESIAN_POINT('Ctrl Pts',(-2.92314257882448,-1.43168989850679,
5.14056416341172));
#96605=CARTESIAN_POINT('Ctrl Pts',(-0.375765897644029,-3.23315611930934,
5.29966443089899));
#96606=CARTESIAN_POINT('Ctrl Pts',(2.51687099077396,-2.06394256641075,5.45876469838628));
#96607=CARTESIAN_POINT('Ctrl Pts',(3.09696327281227,1.00165712122146,5.61786496587355));
#96608=CARTESIAN_POINT('Ctrl Pts',(0.831512124557827,3.14691691793094,5.77696523336084));
#96609=CARTESIAN_POINT('Ctrl Pts',(-2.19794674830152,2.40073501104863,5.93606550084811));
#96610=CARTESIAN_POINT('Ctrl Pts',(-3.20789412592581,-0.551283754970828,
6.0951657683354));
#96611=CARTESIAN_POINT('Ctrl Pts',(-1.27037288639211,-2.99677347011156,
6.25426603582267));
#96612=CARTESIAN_POINT('Ctrl Pts',(1.83438893769452,-2.68877587889142,6.41336630330995));
#96613=CARTESIAN_POINT('Ctrl Pts',(3.25368247222021,0.0897155037398571,
6.57246657079723));
#96614=CARTESIAN_POINT('Ctrl Pts',(1.68343626490711,2.7857747295214,6.73156683828451));
#96615=CARTESIAN_POINT('Ctrl Pts',(-1.43358030483734,2.92221594192265,6.89066710577178));
#96616=CARTESIAN_POINT('Ctrl Pts',(-3.23339849059068,0.373674594654671,
7.04976737325906));
#96617=CARTESIAN_POINT('Ctrl Pts',(-2.06231420772467,-2.51820543448332,
7.20886764074635));
#96618=CARTESIAN_POINT('Ctrl Pts',(1.0036600457489,-3.09631474727808,7.36796790823362));
#96619=CARTESIAN_POINT('Ctrl Pts',(3.14745408659262,-0.829476506259126,
7.52706817572091));
#96620=CARTESIAN_POINT('Ctrl Pts',(2.39931286398669,2.19949909805673,7.68616844320817));
#96621=CARTESIAN_POINT('Ctrl Pts',(-0.553358524434341,3.20753688132814,
7.84526871069548));
#96622=CARTESIAN_POINT('Ctrl Pts',(-2.99759452790126,1.26843428995784,8.00436897818272));
#96623=CARTESIAN_POINT('Ctrl Pts',(-2.68758882290656,-1.8361276700252,8.16346924567004));
#96624=CARTESIAN_POINT('Ctrl Pts',(0.0918199859252528,-3.25362376310308,
8.32256951315728));
#96625=CARTESIAN_POINT('Ctrl Pts',(2.78686300326932,-1.6816340572946,8.48166978064459));
#96626=CARTESIAN_POINT('Ctrl Pts',(2.92128808248718,1.43547011141395,8.64077004813185));
#96627=CARTESIAN_POINT('Ctrl Pts',(0.371583135336417,3.23363950915651,8.79987031561914));
#96628=CARTESIAN_POINT('Ctrl Pts',(-2.519538824682,2.06068498625201,8.95897058310642));
#96629=CARTESIAN_POINT('Ctrl Pts',(-3.09566492637596,-1.00566255038664,
9.11807085059368));
#96630=CARTESIAN_POINT('Ctrl Pts',(-0.827440540942498,-3.14798993849237,
9.27717111808098));
#96631=CARTESIAN_POINT('Ctrl Pts',(2.20105052763421,-2.39788971315312,9.43627138556825));
#96632=CARTESIAN_POINT('Ctrl Pts',(3.20717829483208,0.555433062395866,9.59537165305553));
#96633=CARTESIAN_POINT('Ctrl Pts',(1.26649516286409,2.99841433162368,9.75447192054281));
#96634=CARTESIAN_POINT('Ctrl Pts',(-1.83786563419738,2.6864006425477,9.91357218803009));
#96635=CARTESIAN_POINT('Ctrl Pts',(-3.25356369280678,-0.0939244296970033,
10.0726724555174));
#96636=CARTESIAN_POINT('Ctrl Pts',(-1.67983114615723,-2.78795011111111,
10.2317727230046));
#96637=CARTESIAN_POINT('Ctrl Pts',(1.43735931745029,-2.9203590009078,10.3908729904919));
#96638=CARTESIAN_POINT('Ctrl Pts',(3.23387917490375,-0.369491520563451,
10.5499732579792));
#96639=CARTESIAN_POINT('Ctrl Pts',(2.05905490267551,2.52087116081175,10.7090735254665));
#96640=CARTESIAN_POINT('Ctrl Pts',(-1.0076646342975,3.09501381037799,10.8681737929538));
#96641=CARTESIAN_POINT('Ctrl Pts',(-3.1485244734057,0.825404229459601,11.027274060441));
#96642=CARTESIAN_POINT('Ctrl Pts',(-2.39646555914347,-2.20260103638484,
11.1863743279283));
#96643=CARTESIAN_POINT('Ctrl Pts',(0.557507367987582,-3.20681836658766,
11.3454745954156));
#96644=CARTESIAN_POINT('Ctrl Pts',(2.9992328809358,-1.26455550592212,11.5045748629029));
#96645=CARTESIAN_POINT('Ctrl Pts',(2.68521133831194,1.83960282948396,11.6636751303901));
#96646=CARTESIAN_POINT('Ctrl Pts',(-0.0960288341747119,3.25350226135644,
11.8227753978775));
#96647=CARTESIAN_POINT('Ctrl Pts',(-2.78903605259199,1.67802753224925,11.9818756653647));
#96648=CARTESIAN_POINT('Ctrl Pts',(-2.9194286975732,-1.43924792215604,12.140975932852));
#96649=CARTESIAN_POINT('Ctrl Pts',(-0.367399751210757,-3.23411748773212,
12.3000762003393));
#96650=CARTESIAN_POINT('Ctrl Pts',(2.52220244231514,-2.05742395767715,12.4591764678265));
#96651=CARTESIAN_POINT('Ctrl Pts',(3.09436139955658,1.00966629664392,12.6182767353138));
#96652=CARTESIAN_POINT('Ctrl Pts',(0.823367572662327,3.14905769110897,12.7773770028011));
#96653=CARTESIAN_POINT('Ctrl Pts',(-2.20415062365994,2.39504040255355,12.9364772702884));
#96654=CARTESIAN_POINT('Ctrl Pts',(-3.20645709674549,-0.559581440341695,
13.0955775377757));
#96655=CARTESIAN_POINT('Ctrl Pts',(-1.26261531994337,-3.0000501754952,13.2546778052629));
#96656=CARTESIAN_POINT('Ctrl Pts',(1.8413392551582,-2.68402091069683,13.4137780727502));
#96657=CARTESIAN_POINT('Ctrl Pts',(3.25343946877775,0.0981331984780143,
13.5728783402375));
#96658=CARTESIAN_POINT('Ctrl Pts',(1.67622321632521,2.79012082725763,13.7319786077248));
#96659=CARTESIAN_POINT('Ctrl Pts',(-1.44113592474108,2.91849717287255,13.8910788752121));
#96660=CARTESIAN_POINT('Ctrl Pts',(-3.23435444754192,0.365307828153497,
14.0501791426993));
#96661=CARTESIAN_POINT('Ctrl Pts',(-2.05579215193925,-2.52353266863525,
14.2092794101866));
#96662=CARTESIAN_POINT('Ctrl Pts',(1.01166753658848,-3.09370769418467,14.3683796776739));
#96663=CARTESIAN_POINT('Ctrl Pts',(3.14958959137911,-0.821330571402732,
14.5274799451612));
#96664=CARTESIAN_POINT('Ctrl Pts',(2.39361424397959,2.20569928881124,14.6865802126485));
#96665=CARTESIAN_POINT('Ctrl Pts',(-0.561655278590501,3.2060944854567,14.8456804801357));
#96666=CARTESIAN_POINT('Ctrl Pts',(-3.00086621495993,1.26067460573952,15.004780747623));
#96667=CARTESIAN_POINT('Ctrl Pts',(-2.68282936020039,-1.84307491049364,
15.1638810151103));
#96668=CARTESIAN_POINT('Ctrl Pts',(0.100237521726537,-3.253375315097,15.3229812825976));
#96669=CARTESIAN_POINT('Ctrl Pts',(2.79120443465422,-1.67441819913995,15.4820815500848));
#96670=CARTESIAN_POINT('Ctrl Pts',(2.91756442719559,1.44302332441552,15.6411818175721));
#96671=CARTESIAN_POINT('Ctrl Pts',(0.363215752266829,3.23459005423402,15.8002820850594));
#96672=CARTESIAN_POINT('Ctrl Pts',(-2.52486183921557,2.05415948614449,15.9593823525467));
#96673=CARTESIAN_POINT('Ctrl Pts',(-3.09305269453573,-1.01366835329394,
16.118482620034));
#96674=CARTESIAN_POINT('Ctrl Pts',(-0.819293226533021,-3.15012017399361,
16.2775828875212));
#96675=CARTESIAN_POINT('Ctrl Pts',(2.20724703119086,-2.39218708401822,16.4366831550085));
#96676=CARTESIAN_POINT('Ctrl Pts',(3.20573053287298,0.563728881866405,16.5957834224958));
#96677=CARTESIAN_POINT('Ctrl Pts',(1.25873336412252,3.0016809989886,16.7548836899831));
#96678=CARTESIAN_POINT('Ctrl Pts',(-1.84480979476415,2.68163668732114,16.9139839574703));
#96679=CARTESIAN_POINT('Ctrl Pts',(-3.25330980034103,-0.10234180303989,
17.0730842249576));
#96680=CARTESIAN_POINT('Ctrl Pts',(-1.67261248144863,-2.7922868743284,17.2321844924449));
#96681=CARTESIAN_POINT('Ctrl Pts',(1.44491012038977,-2.91663046093255,17.3912847599322));
#96682=CARTESIAN_POINT('Ctrl Pts',(3.23482430770986,-0.361123524425976,
17.5503850274195));
#96683=CARTESIAN_POINT('Ctrl Pts',(2.0525259609759,2.52618995350001,17.7094852949067));
#96684=CARTESIAN_POINT('Ctrl Pts',(-1.01566874592325,3.0923964008838,17.868585562394));
#96685=CARTESIAN_POINT('Ctrl Pts',(-3.15064943873048,0.817255538905519,
18.0276858298813));
#96686=CARTESIAN_POINT('Ctrl Pts',(-2.3907589232665,-2.20879385015127,18.1867860973686));
#96687=CARTESIAN_POINT('Ctrl Pts',(0.565802249301867,-3.2053652391466,18.3458863648559));
#96688=CARTESIAN_POINT('Ctrl Pts',(3.00249452724035,-1.25679159590449,18.5049866323432));
#96689=CARTESIAN_POINT('Ctrl Pts',(2.68044289255802,1.84654390724392,18.6640868998304));
#96690=CARTESIAN_POINT('Ctrl Pts',(-0.104446041537755,3.25324292453723,
18.8231871673177));
#96691=CARTESIAN_POINT('Ctrl Pts',(-2.79336814582734,1.67080606400668,18.982287434805));
#96692=CARTESIAN_POINT('Ctrl Pts',(-2.91569527447413,-1.44679631187451,
19.1413877022923));
#96693=CARTESIAN_POINT('Ctrl Pts',(-0.359031145506217,-3.23505720787144,
19.3004879697795));
#96694=CARTESIAN_POINT('Ctrl Pts',(2.52751701093296,-2.05089157711685,19.4595882372668));
#96695=CARTESIAN_POINT('Ctrl Pts',(3.09173881350344,1.01766871363955,19.6186885047541));
#96696=CARTESIAN_POINT('Ctrl Pts',(0.81521750937268,3.15117738536831,19.7777887722414));
#96697=CARTESIAN_POINT('Ctrl Pts',(-2.21033974504533,2.38932976232191,19.9368890397287));
#96698=CARTESIAN_POINT('Ctrl Pts',(-3.2049986044304,-0.567875380029503,
20.0959893072159));
#96699=CARTESIAN_POINT('Ctrl Pts',(-1.25484930189775,-3.00330679937484,
20.2550895747032));
#96700=CARTESIAN_POINT('Ctrl Pts',(1.84827724720752,-2.67924797641044,20.4141898421905));
#96701=CARTESIAN_POINT('Ctrl Pts',(3.25317468771359,0.106550236339809,20.5732901096778));
#96702=CARTESIAN_POINT('Ctrl Pts',(1.66899894756981,2.7944482486987,20.732390377165));
#96703=CARTESIAN_POINT('Ctrl Pts',(-1.44868189808057,2.91475886821159,20.8914906446523));
#96704=CARTESIAN_POINT('Ctrl Pts',(-3.2352887546213,0.356938616382969,21.0505909121396));
#96705=CARTESIAN_POINT('Ctrl Pts',(-2.04925633525114,-2.52884301095924,
21.2096911796269));
#96706=CARTESIAN_POINT('Ctrl Pts',(1.01966825560611,-3.09107993266975,21.3687914471141));
#96707=CARTESIAN_POINT('Ctrl Pts',(3.15170401368621,-0.813179138787187,
21.5278917146015));
#96708=CARTESIAN_POINT('Ctrl Pts',(2.38789960178238,2.21188471522636,21.6869919820887));
#96709=CARTESIAN_POINT('Ctrl Pts',(-0.569948273182041,3.20463062887773,
21.846092249576));
#96710=CARTESIAN_POINT('Ctrl Pts',(-3.00411781505223,1.25290648291489,22.0051925170633));
#96711=CARTESIAN_POINT('Ctrl Pts',(-2.67805193937835,-1.85000981392972,
22.1642927845506));
#96712=CARTESIAN_POINT('Ctrl Pts',(0.108654386565719,-3.25310508989865,
22.3233930520378));
#96713=CARTESIAN_POINT('Ctrl Pts',(2.79552718249057,-1.66719113289409,22.4824933195252));
#96714=CARTESIAN_POINT('Ctrl Pts',(2.91382124253668,1.45056687821914,22.6415935870124));
#96715=CARTESIAN_POINT('Ctrl Pts',(0.354845937931631,3.23551894786259,22.8006938544997));
#96716=CARTESIAN_POINT('Ctrl Pts',(-2.53016795302409,2.04762023606288,22.959794121987));
#96717=CARTESIAN_POINT('Ctrl Pts',(-3.09041975865839,-1.02166737098641,
23.1188943894742));
#96718=CARTESIAN_POINT('Ctrl Pts',(-0.811140428001784,-3.15222932346388,
23.2779946569615));
#96719=CARTESIAN_POINT('Ctrl Pts',(2.21342876004792,-2.38646844224622,23.4370949244488));
#96720=CARTESIAN_POINT('Ctrl Pts',(3.20426131264257,0.572020927892142,23.596195191936));
#96721=CARTESIAN_POINT('Ctrl Pts',(1.25096313976878,3.00492757393324,23.7552954594234));
#96722=CARTESIAN_POINT('Ctrl Pts',(-1.8517416066857,2.67685478196211,23.9143957269106));
#96723=CARTESIAN_POINT('Ctrl Pts',(-3.25303413112153,-0.110758491335166,
24.0734959943979));
#96724=CARTESIAN_POINT('Ctrl Pts',(-1.66538262073583,-2.7966049467516,24.2325962618851));
#96725=CARTESIAN_POINT('Ctrl Pts',(1.45245125150157,-2.91288239784167,24.3916965293725));
#96726=CARTESIAN_POINT('Ctrl Pts',(3.235747787499,-0.352753111027735,24.5507967968597));
#96727=CARTESIAN_POINT('Ctrl Pts',(2.04598328023658,2.53149183657321,24.709897064347));
#96728=CARTESIAN_POINT('Ctrl Pts',(-1.0236660589441,3.08975829174553,24.8689973318343));
#96729=CARTESIAN_POINT('Ctrl Pts',(-3.15275331448154,0.809101377869387,
25.0280975993216));
#96730=CARTESIAN_POINT('Ctrl Pts',(-2.38503628431215,-2.21497187886412,
25.1871978668089));
#96731=CARTESIAN_POINT('Ctrl Pts',(0.574093343292813,-3.2038906558794,25.3462981342961));
#96732=CARTESIAN_POINT('Ctrl Pts',(3.00573607567908,-1.24901927327234,25.5053984017834));
#96733=CARTESIAN_POINT('Ctrl Pts',(2.67565650466255,1.853472624751,25.6644986692707));
#96734=CARTESIAN_POINT('Ctrl Pts',(-0.112862549767962,3.25296181141192,
25.823598936758));
#96735=CARTESIAN_POINT('Ctrl Pts',(-2.79768154103088,1.66357341185158,25.9826992042453));
#96736=CARTESIAN_POINT('Ctrl Pts',(-2.91194233451933,-1.4543350171396,26.1417994717325));
#96737=CARTESIAN_POINT('Ctrl Pts',(-0.350660136546753,-3.23597527343481,
26.3008997392198));
#96738=CARTESIAN_POINT('Ctrl Pts',(2.53281466105276,-2.04434546845699,26.4600000067071));
#96739=CARTESIAN_POINT('Ctrl Pts',(3.08909553220792,1.025664318643,26.6191002741944));
#96740=CARTESIAN_POINT('Ctrl Pts',(0.807061989243078,3.15327598651996,26.7782005416816));
#96741=CARTESIAN_POINT('Ctrl Pts',(-2.21651407102935,2.38360312857937,26.9373008091689));
#96742=CARTESIAN_POINT('Ctrl Pts',(-3.20351865874329,-0.576165518516979,
27.0964010766562));
#96743=CARTESIAN_POINT('Ctrl Pts',(-1.24707488423887,-3.00654331995151,
27.2555013441435));
#96744=CARTESIAN_POINT('Ctrl Pts',(1.85520286740139,-2.67445710798101,27.4146016116308));
#96745=CARTESIAN_POINT('Ctrl Pts',(3.25288813080007,0.114966560983826,27.5737018791181));
#96746=CARTESIAN_POINT('Ctrl Pts',(1.66176350699827,2.79875696487802,27.7328021466053));
#96747=CARTESIAN_POINT('Ctrl Pts',(-1.4562181743451,2.91100105296294,27.8919024140926));
#96748=CARTESIAN_POINT('Ctrl Pts',(-3.23620140557482,0.348567015364339,
28.0510026815798));
#96749=CARTESIAN_POINT('Ctrl Pts',(-2.04270680140936,-2.53413642590931,
28.2101029490672));
#96750=CARTESIAN_POINT('Ctrl Pts',(1.02766214924716,-3.08843148032283,28.3692032165544));
#96751=CARTESIAN_POINT('Ctrl Pts',(3.15379733936052,-0.805022262975986,
28.5283034840417));
#96752=CARTESIAN_POINT('Ctrl Pts',(2.38216897564738,2.21805533589845,28.687403751529));
#96753=CARTESIAN_POINT('Ctrl Pts',(-0.578237452697781,3.20314532138989,
28.8465040190163));
#96754=CARTESIAN_POINT('Ctrl Pts',(-3.00734930641285,1.24512997348174,29.0056042865036));
#96755=CARTESIAN_POINT('Ctrl Pts',(-2.6732565924192,-1.85693233391303,29.1647045539908));
#96756=CARTESIAN_POINT('Ctrl Pts',(0.117070524102486,-3.2528130893168,29.3238048214781));
#96757=CARTESIAN_POINT('Ctrl Pts',(2.79983121784309,-1.65995290693313,29.4829050889654));
#96758=CARTESIAN_POINT('Ctrl Pts',(2.91005855356632,1.45810072233022,29.6420053564527));
#96759=CARTESIAN_POINT('Ctrl Pts',(0.346473748356187,3.23642618382443,29.80110562394));
#96760=CARTESIAN_POINT('Ctrl Pts',(-2.53545713058987,2.04106727977924,29.9602058914272));
#96761=CARTESIAN_POINT('Ctrl Pts',(-3.08776613636808,-1.02965954992073,
30.1193061589145));
#96762=CARTESIAN_POINT('Ctrl Pts',(-0.802982199921472,-3.15431737278507,
30.2784064264018));
#96763=CARTESIAN_POINT('Ctrl Pts',(2.21959567282659,-2.38073382611621,30.437506693889));
#96764=CARTESIAN_POINT('Ctrl Pts',(3.20277064397537,0.580309144968386,30.5966069613764));
#96765=CARTESIAN_POINT('Ctrl Pts',(1.24318454181467,3.00815403472587,30.7557072288636));
#96766=CARTESIAN_POINT('Ctrl Pts',(-1.85866102356239,2.67205495847942,30.9148074963509));
#96767=CARTESIAN_POINT('Ctrl Pts',(-3.25273668699353,-0.119174438243803,
31.0739077638382));
#96768=CARTESIAN_POINT('Ctrl Pts',(-1.65814161241355,-2.80090429947669,
31.2330080313254));
#96769=CARTESIAN_POINT('Ctrl Pts',(1.45998266030742,-2.90911483672372,31.3921082988128));
#96770=CARTESIAN_POINT('Ctrl Pts',(3.23664960808963,-0.344380336397985,
31.5512085663));
#96771=CARTESIAN_POINT('Ctrl Pts',(2.0394269042525,2.53677677454196,31.7103088337873));
#96772=CARTESIAN_POINT('Ctrl Pts',(-1.03165651982814,3.08709950062199,31.8694091012746));
#96773=CARTESIAN_POINT('Ctrl Pts',(-3.15483608657604,0.800941800933051,
32.0285093687618));
#96774=CARTESIAN_POINT('Ctrl Pts',(-2.37929768058629,-2.22113508116935,
32.1876096362491));
#96775=CARTESIAN_POINT('Ctrl Pts',(0.582380594462059,-3.20239462665651,
32.3467099037364));
#96776=CARTESIAN_POINT('Ctrl Pts',(3.00895750455389,-1.24123859005156,32.5058101712237));
#96777=CARTESIAN_POINT('Ctrl Pts',(2.67085220666439,1.86038893562621,32.6649104387109));
#96778=CARTESIAN_POINT('Ctrl Pts',(-0.121278302527527,3.25265892386221,
32.8240107061983));
#96779=CARTESIAN_POINT('Ctrl Pts',(-2.80197620932986,1.65632962419737,32.9831109736855));
#96780=CARTESIAN_POINT('Ctrl Pts',(-2.90816990283,-1.46186398748932,33.1422112411728));
#96781=CARTESIAN_POINT('Ctrl Pts',(-0.342286780365579,-3.23687167827694,
33.3013115086601));
#96782=CARTESIAN_POINT('Ctrl Pts',(2.53809535721348,-2.03778567551542,33.4604117761474));
#96783=CARTESIAN_POINT('Ctrl Pts',(3.08643157336347,1.03365305813389,33.6195120436347));
#96784=CARTESIAN_POINT('Ctrl Pts',(0.798901066864283,3.15535348051648,33.7786123111219));
#96785=CARTESIAN_POINT('Ctrl Pts',(-2.22267356028275,2.37786053965839,33.9377125786092));
#96786=CARTESIAN_POINT('Ctrl Pts',(-3.20201726959057,-0.584451800312236,
34.0968128460964));
#96787=CARTESIAN_POINT('Ctrl Pts',(-1.23929211900646,-3.00975971556083,
34.2559131135838));
#96788=CARTESIAN_POINT('Ctrl Pts',(1.86211606938167,-2.66964833747724,34.415013381071));
#96789=CARTESIAN_POINT('Ctrl Pts',(3.25257979995536,0.12338211607354,34.5741136485583));
#96790=CARTESIAN_POINT('Ctrl Pts',(1.6545169430426,2.80304694695421,34.7332139160456));
#96791=CARTESIAN_POINT('Ctrl Pts',(-1.46374470308892,2.90722375228044,34.8923141835329));
#96792=CARTESIAN_POINT('Ctrl Pts',(-3.23709239429345,0.34019308113477,35.0514144510202));
#96793=CARTESIAN_POINT('Ctrl Pts',(-2.03614359425464,-2.53941287805274,
35.2105147185074));
#96794=CARTESIAN_POINT('Ctrl Pts',(1.0356491640027,-3.08576235487196,35.3696149859947));
#96795=CARTESIAN_POINT('Ctrl Pts',(3.1558695543899,-0.796859998568978,35.528715253482));
#96796=CARTESIAN_POINT('Ctrl Pts',(2.37642240393377,2.2242111095231,35.6878155209692));
#96797=CARTESIAN_POINT('Ctrl Pts',(-0.586522761652353,3.20163857293545,
35.8469157884566));
#96798=CARTESIAN_POINT('Ctrl Pts',(-3.01056066741105,1.23734512949377,36.0060160559438));
#96799=CARTESIAN_POINT('Ctrl Pts',(-2.66844335142165,-1.86384242410619,
36.1651163234311));
#96800=CARTESIAN_POINT('Ctrl Pts',(0.125485878001671,-3.25249931530609,
36.3242165909184));
#96801=CARTESIAN_POINT('Ctrl Pts',(2.80411651190175,-1.65270356970762,36.4833168584056));
#96802=CARTESIAN_POINT('Ctrl Pts',(2.90627638547088,1.46562480631938,36.642417125893));
#96803=CARTESIAN_POINT('Ctrl Pts',(0.338099239581502,3.2373117560468,36.8015173933802));
#96804=CARTESIAN_POINT('Ctrl Pts',(-2.54072933650863,2.03450066115712,36.9606176608675));
#96805=CARTESIAN_POINT('Ctrl Pts',(-3.08509184542742,-1.03764483659955,
37.1197179283548));
#96806=CARTESIAN_POINT('Ctrl Pts',(-0.794818596900981,-3.15638430798038,
37.2788181958421));
#96807=CARTESIAN_POINT('Ctrl Pts',(2.22574772824722,-2.37498327401409,37.4379184633293));
#96808=CARTESIAN_POINT('Ctrl Pts',(3.20125853684957,0.588593477616085,37.5970187308166));
#96809=CARTESIAN_POINT('Ctrl Pts',(1.23539762232795,3.01136035976947,37.7561189983039));
#96810=CARTESIAN_POINT('Ctrl Pts',(-1.86556799907749,2.66723724900174,37.9152192657912));
#96811=CARTESIAN_POINT('Ctrl Pts',(-3.25241746994808,-0.127589587431759,
38.0743195332785));
#96812=CARTESIAN_POINT('Ctrl Pts',(-1.65088950495109,-2.80518490372502,
38.2334198007657));
#96813=CARTESIAN_POINT('Ctrl Pts',(1.46750429639411,-2.90532780279767,38.392520068253));
#96814=CARTESIAN_POINT('Ctrl Pts',(3.23752976344525,-0.33600525658179,38.5516203357403));
#96815=CARTESIAN_POINT('Ctrl Pts',(2.03285687691022,2.54204473203035,38.7107206032276));
#96816=CARTESIAN_POINT('Ctrl Pts',(-1.03964007508946,3.08442004531035,38.8698208707148));
#96817=CARTESIAN_POINT('Ctrl Pts',(-3.15689774107258,0.792776862714387,
39.0289211382022));
#96818=CARTESIAN_POINT('Ctrl Pts',(-2.37354315050146,-2.22728341581217,
39.1880214056894));
#96819=CARTESIAN_POINT('Ctrl Pts',(0.590663947337058,-3.20087716149193,
39.3471216731767));
#96820=CARTESIAN_POINT('Ctrl Pts',(3.01215879230152,-1.23344959832382,39.5062219406639));
#96821=CARTESIAN_POINT('Ctrl Pts',(2.66603003072207,1.86729279357374,39.6653222081512));
#96822=CARTESIAN_POINT('Ctrl Pts',(-0.129693243483748,3.25233426391553,
39.8244224756385));
#96823=CARTESIAN_POINT('Ctrl Pts',(-2.80625212197701,1.64907474953194,39.9835227431257));
#96824=CARTESIAN_POINT('Ctrl Pts',(-2.90437800465771,-1.46938317252679,
40.1426230106131));
#96825=CARTESIAN_POINT('Ctrl Pts',(-0.333911133011649,-3.23774641639759,
40.3017232781004));
#96826=CARTESIAN_POINT('Ctrl Pts',(2.5433590640676,-2.03121224220161,40.4608235455876));
#96827=CARTESIAN_POINT('Ctrl Pts',(3.08374695480184,1.04163487863778,40.6199238130749));
#96828=CARTESIAN_POINT('Ctrl Pts',(0.790734796863326,3.15740985345169,40.7790240805622));
#96829=CARTESIAN_POINT('Ctrl Pts',(-2.22881817157562,2.3721020339983,40.9381243480495));
#96830=CARTESIAN_POINT('Ctrl Pts',(-3.20049444702208,-0.592734169949194,
41.0972246155367));
#96831=CARTESIAN_POINT('Ctrl Pts',(-1.23150105829622,-3.01295596467317,
41.2563248830241));
#96832=CARTESIAN_POINT('Ctrl Pts',(1.86901680687331,-2.66482169708772,41.4154251505113));
#96833=CARTESIAN_POINT('Ctrl Pts',(3.25224969724331,0.13179684527757,41.5745254179986));
#96834=CARTESIAN_POINT('Ctrl Pts',(1.64725930420931,2.80731816621134,41.7336256854858));
#96835=CARTESIAN_POINT('Ctrl Pts',(-1.47126143393157,2.90342699144824,41.8927259529732));
#96836=CARTESIAN_POINT('Ctrl Pts',(-3.23796171481316,0.331816869747021,
42.0518262204604));
#96837=CARTESIAN_POINT('Ctrl Pts',(-2.02956675771925,-2.54467233207055,
42.2109264879477));
#96838=CARTESIAN_POINT('Ctrl Pts',(1.04362924640992,-3.08307257418346,42.370026755435));
#96839=CARTESIAN_POINT('Ctrl Pts',(3.1579206449035,-0.788692400202103,42.5291270229223));
#96840=CARTESIAN_POINT('Ctrl Pts',(2.37065992510754,2.2303519948953,42.6882272904095));
#96841=CARTESIAN_POINT('Ctrl Pts',(-0.594804144586184,3.20011039360014,
42.8473275578968));
#96842=CARTESIAN_POINT('Ctrl Pts',(-3.01375187655094,1.22955200306058,43.0064278253841));
#96843=CARTESIAN_POINT('Ctrl Pts',(-2.66361224860416,-1.87074003825496,
43.1655280928714));
#96844=CARTESIAN_POINT('Ctrl Pts',(0.133900391933119,-3.25216376996676,
43.3246283603587));
#96845=CARTESIAN_POINT('Ctrl Pts',(2.80838303598201,-1.64544316974277,43.4837286278459));
#96846=CARTESIAN_POINT('Ctrl Pts',(2.90247476356711,1.47313907982251,43.6428288953332));
#96847=CARTESIAN_POINT('Ctrl Pts',(0.329722467664408,3.23817565860181,43.8019291628205));
#96848=CARTESIAN_POINT('Ctrl Pts',(-2.54598453549002,2.02792042415186,43.9610294303078));
#96849=CARTESIAN_POINT('Ctrl Pts',(-3.08239690373679,-1.0456231775719,44.120129697795));
#96850=CARTESIAN_POINT('Ctrl Pts',(-0.786649673586238,-3.15843011521361,
44.2792299652823));
#96851=CARTESIAN_POINT('Ctrl Pts',(2.23188488513169,-2.36921682443382,44.4383302327696));
#96852=CARTESIAN_POINT('Ctrl Pts',(3.19972500138294,0.596873870384775,44.5974305002568));
#96853=CARTESIAN_POINT('Ctrl Pts',(1.22760243343935,3.014546527597,44.7565307677442));
#96854=CARTESIAN_POINT('Ctrl Pts',(-1.87246248701163,2.66240168578663,44.9156310352314));
#96855=CARTESIAN_POINT('Ctrl Pts',(-3.25207648209538,-0.136003882587964,
45.0747313027187));
#96856=CARTESIAN_POINT('Ctrl Pts',(-1.64362634694256,-2.80944673080995,
45.233831570206));
#96857=CARTESIAN_POINT('Ctrl Pts',(1.47501610951029,-2.90152132147672,45.3929318376933));
#96858=CARTESIAN_POINT('Ctrl Pts',(3.23838824749048,-0.327627927517849,
45.5520321051805));
#96859=CARTESIAN_POINT('Ctrl Pts',(2.02627324253834,2.54729567354398,45.7111323726678));
#96860=CARTESIAN_POINT('Ctrl Pts',(-1.04761667195744,3.08171994418912,45.8702326401551));
#96861=CARTESIAN_POINT('Ctrl Pts',(-3.15893826289477,0.784606617022181,
46.0293329076424));
#96862=CARTESIAN_POINT('Ctrl Pts',(-2.36777273501135,-2.23341684002548,
46.1884331751296));
#96863=CARTESIAN_POINT('Ctrl Pts',(0.598943351115479,-3.19933827361817,
46.347533442617));
#96864=CARTESIAN_POINT('Ctrl Pts',(3.01533990863423,-1.22565234436046,46.5066337101042));
#96865=CARTESIAN_POINT('Ctrl Pts',(2.66119002601396,1.87418414119101,46.6657339775915));
#96866=CARTESIAN_POINT('Ctrl Pts',(-0.138107348548404,3.25198785509165,
46.8248342450789));
#96867=CARTESIAN_POINT('Ctrl Pts',(-2.81050918885052,1.64180879569596,46.983934512566));
#96868=CARTESIAN_POINT('Ctrl Pts',(-2.90056678270385,-1.47689244423952,
47.1430347800534));
#96869=CARTESIAN_POINT('Ctrl Pts',(-0.325533026746636,-3.23859963012878,
47.3021350475406));
#96870=CARTESIAN_POINT('Ctrl Pts',(2.54860531944881,-2.02462492982939,47.461235315028));
#96871=CARTESIAN_POINT('Ctrl Pts',(3.08104250892322,1.04960918746444,47.6203355825151));
#96872=CARTESIAN_POINT('Ctrl Pts',(0.782561680270313,3.15944612027446,47.7794358500025));
#96873=CARTESIAN_POINT('Ctrl Pts',(-2.23494490001932,2.36632568773837,47.9385361174897));
#96874=CARTESIAN_POINT('Ctrl Pts',(-3.19895585498994,-0.601008828439279,
48.0976363849771));
#96875=CARTESIAN_POINT('Ctrl Pts',(-1.22369096897038,-3.01613918720563,
48.2567366524642));
#96876=CARTESIAN_POINT('Ctrl Pts',(1.87588445932071,-2.65996359612247,48.4158369199516));
#96877=CARTESIAN_POINT('Ctrl Pts',(3.25193707323675,0.140184704552063,48.5749371874387));
#96878=CARTESIAN_POINT('Ctrl Pts',(1.63991576715359,2.81162016955288,48.7340374549263));
#96879=CARTESIAN_POINT('Ctrl Pts',(-1.4786254840315,2.8995162196865,48.8931377224133));
#96880=CARTESIAN_POINT('Ctrl Pts',(-3.23908187246008,0.323618892565623,
49.0522379899008));
#96881=CARTESIAN_POINT('Ctrl Pts',(-2.02245614015915,-2.55025933497318,
49.2113382573879));
#96882=CARTESIAN_POINT('Ctrl Pts',(1.05060697727445,-3.07970183853061,49.3704385248753));
#96883=CARTESIAN_POINT('Ctrl Pts',(3.16187590788727,-0.781805304638667,
49.5295387923625));
#96884=CARTESIAN_POINT('Ctrl Pts',(2.36097657105778,2.23915834260108,49.6886390598498));
#96885=CARTESIAN_POINT('Ctrl Pts',(0.391229220202036,2.87417057272355,49.7947059048413));
#96886=CARTESIAN_POINT('Ctrl Pts',(-0.509883685252968,2.70426773226887,
49.8477393273371));
#96887=CARTESIAN_POINT('Ctrl Pts',(-1.28892185405285,2.64462557919736,-2.24820162486594E-14));
#96888=CARTESIAN_POINT('Ctrl Pts',(-2.17016087157859,2.21513255860965,0.0530334224957372));
#96889=CARTESIAN_POINT('Ctrl Pts',(-3.45405617988707,0.413218788201715,
0.159100267487257));
#96890=CARTESIAN_POINT('Ctrl Pts',(-2.21255276421415,-2.68876403565728,
0.318200534974535));
#96891=CARTESIAN_POINT('Ctrl Pts',(1.06485027294372,-3.31175003984662,0.477300802461814));
#96892=CARTESIAN_POINT('Ctrl Pts',(3.36232670912974,-0.896101221987242,
0.636401069949093));
#96893=CARTESIAN_POINT('Ctrl Pts',(2.5712343561111,2.34510976377807,0.795501337436372));
#96894=CARTESIAN_POINT('Ctrl Pts',(-0.582769022193126,3.4304380941372,0.954601604923651));
#96895=CARTESIAN_POINT('Ctrl Pts',(-3.20109589749867,1.36442584112634,1.11370187241093));
#96896=CARTESIAN_POINT('Ctrl Pts',(-2.87831488588854,-1.95556173838141,
1.27280213989821));
#96897=CARTESIAN_POINT('Ctrl Pts',(0.0891716048822917,-3.47857905582672,
1.43190240738549));
#96898=CARTESIAN_POINT('Ctrl Pts',(2.97469424606561,-1.80550493926474,1.59100267487277));
#96899=CARTESIAN_POINT('Ctrl Pts',(3.12703283318065,1.52654404971158,1.75010294236005));
#96900=CARTESIAN_POINT('Ctrl Pts',(0.406190919144961,3.45595400114929,1.90920320984732));
#96901=CARTESIAN_POINT('Ctrl Pts',(-2.68786170976409,2.20998618908559,2.0683034773346));
#96902=CARTESIAN_POINT('Ctrl Pts',(-3.31226287552911,-1.06656174785242,
2.22740374482188));
#96903=CARTESIAN_POINT('Ctrl Pts',(-0.893298367095335,-3.3631308491467,
2.38650401230916));
#96904=CARTESIAN_POINT('Ctrl Pts',(2.34644348211611,-2.56959895553633,2.54560427979644));
#96905=CARTESIAN_POINT('Ctrl Pts',(3.43023281013426,0.584925858944962,2.70470454728372));
#96906=CARTESIAN_POINT('Ctrl Pts',(1.36226471238718,3.20201017831608,2.863804814771));
#96907=CARTESIAN_POINT('Ctrl Pts',(-1.9573756753309,2.87703241397402,3.02290508225827));
#96908=CARTESIAN_POINT('Ctrl Pts',(-3.47854548062508,-0.0914126395211362,
3.18200534974556));
#96909=CARTESIAN_POINT('Ctrl Pts',(-1.80356749616777,-2.97586610684143,
3.34110561723283));
#96910=CARTESIAN_POINT('Ctrl Pts',(1.52855949065065,-3.12604235239462,3.50020588472011));
#96911=CARTESIAN_POINT('Ctrl Pts',(3.45621958157706,-0.403956786608693,
3.65930615220739));
#96912=CARTESIAN_POINT('Ctrl Pts',(2.20824532712176,2.68929125255921,3.81840641969467));
#96913=CARTESIAN_POINT('Ctrl Pts',(-1.06870293299648,3.31157197148184,3.97750668718195));
#96914=CARTESIAN_POINT('Ctrl Pts',(-3.36370845150885,0.891123072362765,
4.13660695466923));
#96915=CARTESIAN_POINT('Ctrl Pts',(-2.56808045450599,-2.34810511994446,
4.2957072221565));
#96916=CARTESIAN_POINT('Ctrl Pts',(0.587144289757969,-3.42985370829862,
4.45480748964379));
#96917=CARTESIAN_POINT('Ctrl Pts',(3.20289070356629,-1.3601933750613,4.61390775713106));
#96918=CARTESIAN_POINT('Ctrl Pts',(2.87576573115885,1.95923616133382,4.77300802461835));
#96919=CARTESIAN_POINT('Ctrl Pts',(-0.0936625436724054,3.47848561943344,
4.93210829210562));
#96920=CARTESIAN_POINT('Ctrl Pts',(-2.97703205310412,1.80164231504339,5.0912085595929));
#96921=CARTESIAN_POINT('Ctrl Pts',(-3.12505301162273,-1.53058111549187,
5.25030882708019));
#96922=CARTESIAN_POINT('Ctrl Pts',(-0.401721201902316,-3.45648013917867,
5.40940909456745));
#96923=CARTESIAN_POINT('Ctrl Pts',(2.69071899761642,-2.20650541636319,5.56850936205474));
#96924=CARTESIAN_POINT('Ctrl Pts',(3.31088003462323,1.07084465395654,5.72760962954202));
#96925=CARTESIAN_POINT('Ctrl Pts',(0.888947219979559,3.36428413138222,5.8867098970293));
#96926=CARTESIAN_POINT('Ctrl Pts',(-2.34976567852831,2.56656114920079,6.04581016451657));
#96927=CARTESIAN_POINT('Ctrl Pts',(-3.42947322235061,-0.589362616524685,
6.20491043200386));
#96928=CARTESIAN_POINT('Ctrl Pts',(-1.35812144206107,-3.2037698146389,6.36401069949113));
#96929=CARTESIAN_POINT('Ctrl Pts',(1.96109581371684,-2.87449788415286,6.52311096697842));
#96930=CARTESIAN_POINT('Ctrl Pts',(3.47842431030683,0.0959124290354176,
6.68221123446568));
#96931=CARTESIAN_POINT('Ctrl Pts',(1.79971637635214,2.97819674321007,6.84131150195298));
#96932=CARTESIAN_POINT('Ctrl Pts',(-1.53260209799175,3.12406236906506,7.00041176944024));
#96933=CARTESIAN_POINT('Ctrl Pts',(-3.45673925178857,0.399485446194586,
7.15951203692754));
#96934=CARTESIAN_POINT('Ctrl Pts',(-2.20476458194314,-2.69214561544991,
7.3186123044148));
#96935=CARTESIAN_POINT('Ctrl Pts',(1.07298592663064,-3.31018671343923,7.47771257190209));
#96936=CARTESIAN_POINT('Ctrl Pts',(3.36485840393263,-0.886770995275038,
7.63681283938936));
#96937=CARTESIAN_POINT('Ctrl Pts',(2.56504077007488,2.35142525384727,7.79591310687664));
#96938=CARTESIAN_POINT('Ctrl Pts',(-0.591580696685175,3.42909130177173,
7.95501337436392));
#96939=CARTESIAN_POINT('Ctrl Pts',(-3.20464758541102,1.35604894081905,8.11411364185121));
#96940=CARTESIAN_POINT('Ctrl Pts',(-2.87322883456653,-1.96295464562801,
8.27321390933847));
#96941=CARTESIAN_POINT('Ctrl Pts',(0.098162274266716,-3.47836154597072,
8.43231417682577));
#96942=CARTESIAN_POINT('Ctrl Pts',(2.97936018736707,-1.79778968472654,8.59141444431303));
#96943=CARTESIAN_POINT('Ctrl Pts',(3.12307041952958,1.53462243931086,8.75051471180032));
#96944=CARTESIAN_POINT('Ctrl Pts',(0.397249523359848,3.45699691824673,8.90961497928758));
#96945=CARTESIAN_POINT('Ctrl Pts',(-2.6935711070035,2.20302282514118,9.06871524677488));
#96946=CARTESIAN_POINT('Ctrl Pts',(-3.30949200741227,-1.07512675041197,
9.22781551426215));
#96947=CARTESIAN_POINT('Ctrl Pts',(-0.884594399583002,-3.3654312687683,
9.38691578174943));
#96948=CARTESIAN_POINT('Ctrl Pts',(2.35308384542899,-2.56351931784376,9.54601604923671));
#96949=CARTESIAN_POINT('Ctrl Pts',(3.42870794660542,0.593798529353127,9.70511631672399));
#96950=CARTESIAN_POINT('Ctrl Pts',(1.35397587226326,3.20552401549357,9.86421658421125));
#96951=CARTESIAN_POINT('Ctrl Pts',(-1.9648126563216,2.87195858294223,10.0233168516986));
#96952=CARTESIAN_POINT('Ctrl Pts',(-3.47829732643462,-0.100412078431024,
10.1824171191858));
#96953=CARTESIAN_POINT('Ctrl Pts',(-1.79586224098147,-2.98052238508522,
10.3415173866731));
#96954=CARTESIAN_POINT('Ctrl Pts',(1.53664213860852,-3.12207716343297,10.5006176541604));
#96955=CARTESIAN_POINT('Ctrl Pts',(3.45725313844298,-0.395013434332659,
10.6597179216477));
#96956=CARTESIAN_POINT('Ctrl Pts',(2.20128014668724,2.69499547168037,10.8188181891349));
#96957=CARTESIAN_POINT('Ctrl Pts',(-1.07726712440552,3.30879591683321,10.9779184566222));
#96958=CARTESIAN_POINT('Ctrl Pts',(-3.36600272564927,0.882417433813924,
11.1370187241095));
#96959=CARTESIAN_POINT('Ctrl Pts',(-2.56199679314412,-2.35474145257953,
11.2961189915968));
#96960=CARTESIAN_POINT('Ctrl Pts',(0.596016113600773,-3.42832315701208,
11.455219259084));
#96961=CARTESIAN_POINT('Ctrl Pts',(3.20639910451986,-1.35190223726101,11.6143195265713));
#96962=CARTESIAN_POINT('Ctrl Pts',(2.87068712981141,1.96666984502031,11.7734197940586));
#96963=CARTESIAN_POINT('Ctrl Pts',(-0.102661840587129,3.47823165172538,
11.9325200615459));
#96964=CARTESIAN_POINT('Ctrl Pts',(-2.98168333587832,1.79393404592325,12.0916203290332));
#96965=CARTESIAN_POINT('Ctrl Pts',(-3.12108260119075,-1.53866119503986,
12.2507205965204));
#96966=CARTESIAN_POINT('Ctrl Pts',(-0.39277718004845,-3.45750791227009,
12.4098208640077));
#96967=CARTESIAN_POINT('Ctrl Pts',(2.69641870888462,-2.19953654731037,12.568921131495));
#96968=CARTESIAN_POINT('Ctrl Pts',(3.30809844199328,1.07940704771587,12.7280213989823));
#96969=CARTESIAN_POINT('Ctrl Pts',(0.880240098878547,3.36657277433645,12.8871216664696));
#96970=CARTESIAN_POINT('Ctrl Pts',(-2.3563980746054,2.56047319661288,13.0462219339568));
#96971=CARTESIAN_POINT('Ctrl Pts',(-3.42793693315271,-0.598233448500373,
13.2053222014441));
#96972=CARTESIAN_POINT('Ctrl Pts',(-1.34982803667978,-3.2072728521238,13.3644224689314));
#96973=CARTESIAN_POINT('Ctrl Pts',(1.96852621094718,-2.86941447570597,13.5235227364187));
#96974=CARTESIAN_POINT('Ctrl Pts',(3.47816452187051,0.104911559793856,13.6826230039059));
#96975=CARTESIAN_POINT('Ctrl Pts',(1.79200510035857,2.98284303926069,13.8417232713933));
#96976=CARTESIAN_POINT('Ctrl Pts',(-1.54067960776015,3.12008673321898,14.0008235388805));
#96977=CARTESIAN_POINT('Ctrl Pts',(-3.45776123962148,0.390540761442825,
14.1599238063678));
#96978=CARTESIAN_POINT('Ctrl Pts',(-2.19779202774005,-2.69784081802083,
14.3190240738551));
#96979=CARTESIAN_POINT('Ctrl Pts',(1.08154651944778,-3.30739958318427,14.4781243413423));
#96980=CARTESIAN_POINT('Ctrl Pts',(3.36714141459133,-0.87806239568778,14.6372246088297));
#96981=CARTESIAN_POINT('Ctrl Pts',(2.5589485288875,2.35805371081355,14.7963248763169));
#96982=CARTESIAN_POINT('Ctrl Pts',(-0.600450533124296,3.42754927518888,
14.9554251438042));
#96983=CARTESIAN_POINT('Ctrl Pts',(-3.20814525793984,1.34775327138733,15.1145254112915));
#96984=CARTESIAN_POINT('Ctrl Pts',(-2.86814062115834,-1.9703817533256,15.2736256787788));
#96985=CARTESIAN_POINT('Ctrl Pts',(0.107161235110024,-3.47809593689805,
15.432725946266));
#96986=CARTESIAN_POINT('Ctrl Pts',(2.98400149474715,-1.79007540509441,15.5918262137533));
#96987=CARTESIAN_POINT('Ctrl Pts',(3.11908955993432,1.54269737592496,15.7509264812406));
#96988=CARTESIAN_POINT('Ctrl Pts',(0.388304179451396,3.45801312039119,15.9100267487279));
#96989=CARTESIAN_POINT('Ctrl Pts',(-2.69926179849407,2.1960465887061,16.0691270162151));
#96990=CARTESIAN_POINT('Ctrl Pts',(-3.30669934069854,-1.08368553870617,
16.2282272837024));
#96991=CARTESIAN_POINT('Ctrl Pts',(-0.875884325152688,-3.36770864617604,
16.3873275511897));
#96992=CARTESIAN_POINT('Ctrl Pts',(2.35970836051133,-2.55742279060582,16.546427818677));
#96993=CARTESIAN_POINT('Ctrl Pts',(3.42716018328277,0.60266736654502,16.7055280861643));
#96994=CARTESIAN_POINT('Ctrl Pts',(1.34567794225167,3.20901632160298,16.8646283536515));
#96995=CARTESIAN_POINT('Ctrl Pts',(-1.97223647137926,2.86686556670147,17.0237286211388));
#96996=CARTESIAN_POINT('Ctrl Pts',(-3.47802589683674,-0.109410865594434,
17.1828288886261));
#96997=CARTESIAN_POINT('Ctrl Pts',(-1.78814496093809,-2.98515870185301,
17.3419291561134));
#96998=CARTESIAN_POINT('Ctrl Pts',(1.54471449869015,-3.11809108175395,17.5010294236007));
#96999=CARTESIAN_POINT('Ctrl Pts',(3.45826355447384,-0.386067435009841,
17.6601296910879));
#97000=CARTESIAN_POINT('Ctrl Pts',(2.19430023093872,2.70068164970982,17.8192299585752));
#97001=CARTESIAN_POINT('Ctrl Pts',(-1.08582410459616,3.30599771482907,17.9783302260625));
#97002=CARTESIAN_POINT('Ctrl Pts',(-3.36827446885328,0.873705888184473,
18.1374304935498));
#97003=CARTESIAN_POINT('Ctrl Pts',(-2.55589598240612,-2.3613620230065,18.2965307610371));
#97004=CARTESIAN_POINT('Ctrl Pts',(0.604883947835077,-3.42676965759715,
18.4556310285243));
#97005=CARTESIAN_POINT('Ctrl Pts',(3.20988604274885,-1.34360205014104,18.6147312960116));
#97006=CARTESIAN_POINT('Ctrl Pts',(2.86558931286877,1.97409036433223,18.7738315634989));
#97007=CARTESIAN_POINT('Ctrl Pts',(-0.111660450305955,3.47795440171584,
18.9329318309861));
#97008=CARTESIAN_POINT('Ctrl Pts',(-2.98631466009421,1.7862137686972,19.0920320984735));
#97009=CARTESIAN_POINT('Ctrl Pts',(-3.11709129909556,-1.54673097521187,
19.2511323659607));
#97010=CARTESIAN_POINT('Ctrl Pts',(-0.383830529053899,-3.45851254176464,
19.410232633448));
#97011=CARTESIAN_POINT('Ctrl Pts',(2.70210037107411,-2.1925529551685,19.5693329009353));
#97012=CARTESIAN_POINT('Ctrl Pts',(3.30529470586936,1.08796221622309,19.7284331684226));
#97013=CARTESIAN_POINT('Ctrl Pts',(0.871527085694471,3.36883888238634,19.8875334359098));
#97014=CARTESIAN_POINT('Ctrl Pts',(-2.36301469760723,2.55436810492716,20.0466337033971));
#97015=CARTESIAN_POINT('Ctrl Pts',(-3.42637769829543,-0.607100276067174,
20.2057339708844));
#97016=CARTESIAN_POINT('Ctrl Pts',(-1.34152559592387,-3.21075442101357,
20.3648342383717));
#97017=CARTESIAN_POINT('Ctrl Pts',(1.97594343140896,-2.86431186019415,20.5239345058589));
#97018=CARTESIAN_POINT('Ctrl Pts',(3.47788145156528,0.113909988303468,20.6830347733463));
#97019=CARTESIAN_POINT('Ctrl Pts',(1.78428182917969,2.9874693689871,20.8421350408335));
#97020=CARTESIAN_POINT('Ctrl Pts',(-1.54874680464648,3.11609021237743,21.0012353083208));
#97021=CARTESIAN_POINT('Ctrl Pts',(-3.45876008215943,0.381593462519445,
21.1603355758081));
#97022=CARTESIAN_POINT('Ctrl Pts',(-2.19080476212648,-2.7035179619934,21.3194358432953));
#97023=CARTESIAN_POINT('Ctrl Pts',(1.09009987269245,-3.30459031411354,21.4785361107827));
#97024=CARTESIAN_POINT('Ctrl Pts',(3.36940188653905,-0.869347918594261,
21.6376363782699));
#97025=CARTESIAN_POINT('Ctrl Pts',(2.55283915880816,2.36466638362217,21.7967366457572));
#97026=CARTESIAN_POINT('Ctrl Pts',(-0.609316350314126,3.42598430554155,
21.9558369132444));
#97027=CARTESIAN_POINT('Ctrl Pts',(-3.21162145603384,1.33944858046886,22.1149371807317));
#97028=CARTESIAN_POINT('Ctrl Pts',(-2.86303320921208,-1.97779567183414,
22.274037448219));
#97029=CARTESIAN_POINT('Ctrl Pts',(0.116159478645818,-3.47780704641558,
22.4331377157063));
#97030=CARTESIAN_POINT('Ctrl Pts',(2.98862282804862,-1.7823491431938,22.5922379831935));
#97031=CARTESIAN_POINT('Ctrl Pts',(3.11508782201838,1.55076198615064,22.7513382506809));
#97032=CARTESIAN_POINT('Ctrl Pts',(0.379356236342356,3.45900617555466,22.9104385181681));
#97033=CARTESIAN_POINT('Ctrl Pts',(-2.70493442187461,2.189055652544,23.0695387856555));
#97034=CARTESIAN_POINT('Ctrl Pts',(-3.30388453985629,-1.09223707310991,
23.2286390531427));
#97035=CARTESIAN_POINT('Ctrl Pts',(-0.867168387795486,-3.36996348107591,
23.38773932063));
#97036=CARTESIAN_POINT('Ctrl Pts',(2.3663170803602,-2.55130914468877,23.5468395881172));
#97037=CARTESIAN_POINT('Ctrl Pts',(3.42558947950012,0.611532169648694,23.7059398556046));
#97038=CARTESIAN_POINT('Ctrl Pts',(1.33737100464502,3.21248714744695,23.8650401230918));
#97039=CARTESIAN_POINT('Ctrl Pts',(-1.97964708483286,2.86175336045749,24.0241403905791));
#97040=CARTESIAN_POINT('Ctrl Pts',(-3.47773118629787,-0.118408920391893,
24.1832406580664));
#97041=CARTESIAN_POINT('Ctrl Pts',(-1.78041571154812,-2.98977503679619,
24.3423409255536));
#97042=CARTESIAN_POINT('Ctrl Pts',(1.55277651888125,-3.11408412843777,24.5014411930409));
#97043=CARTESIAN_POINT('Ctrl Pts',(3.45925082184736,-0.377118851458631,
24.6605414605282));
#97044=CARTESIAN_POINT('Ctrl Pts',(2.18730562715285,2.70634975012517,24.8196417280154));
#97045=CARTESIAN_POINT('Ctrl Pts',(-1.09437381658139,3.30317738339288,24.9787419955028));
#97046=CARTESIAN_POINT('Ctrl Pts',(-3.37052366576197,0.864988494209978,
25.13784226299));
#97047=CARTESIAN_POINT('Ctrl Pts',(-2.54977806320906,-2.36796678713085,
25.2969425304773));
#97048=CARTESIAN_POINT('Ctrl Pts',(0.613747733143994,-3.4251932203363,25.4560427979646));
#97049=CARTESIAN_POINT('Ctrl Pts',(3.21335149489072,-1.33529286932145,25.6151430654519));
#97050=CARTESIAN_POINT('Ctrl Pts',(2.86047231446579,1.98149766963065,25.7742433329392));
#97051=CARTESIAN_POINT('Ctrl Pts',(-0.120658312600698,3.47765387124387,
25.9333436004265));
#97052=CARTESIAN_POINT('Ctrl Pts',(-2.9909259947478,1.77848153505145,26.0924438679137));
#97053=CARTESIAN_POINT('Ctrl Pts',(-3.11307913205549,-1.5547904019956,26.251544135401));
#97054=CARTESIAN_POINT('Ctrl Pts',(-0.374881308804223,-3.45949402093519,
26.4106444028883));
#97055=CARTESIAN_POINT('Ctrl Pts',(2.70776394615297,-2.1855546866851,26.5697446703756));
#97056=CARTESIAN_POINT('Ctrl Pts',(3.30246884501914,1.0965101022129,26.7288449378628));
#97057=CARTESIAN_POINT('Ctrl Pts',(0.862808238749752,3.37108244036284,26.8879452053501));
#97058=CARTESIAN_POINT('Ctrl Pts',(-2.36961550324391,2.54824591500962,27.0470454728374));
#97059=CARTESIAN_POINT('Ctrl Pts',(-3.42479552821586,-0.61596303987306,
27.2061457403247));
#97060=CARTESIAN_POINT('Ctrl Pts',(-1.33321417536761,-3.21421449800351,
27.365246007812));
#97061=CARTESIAN_POINT('Ctrl Pts',(1.98334742545324,-2.85919007177297,27.5243462752992));
#97062=CARTESIAN_POINT('Ctrl Pts',(3.47757510128594,0.122907654331153,27.6834465427865));
#97063=CARTESIAN_POINT('Ctrl Pts',(1.77654661451301,2.99207570142192,27.8425468102738));
#97064=CARTESIAN_POINT('Ctrl Pts',(-1.55680363465111,3.112072833292,28.0016470777611));
#97065=CARTESIAN_POINT('Ctrl Pts',(-3.45973577271641,0.372643609315264,
28.1607473452483));
#97066=CARTESIAN_POINT('Ctrl Pts',(-2.18380283187331,-2.70917700936636,
28.3198476127356));
#97067=CARTESIAN_POINT('Ctrl Pts',(1.0986459291108,-3.30175892503151,28.4789478802229));
#97068=CARTESIAN_POINT('Ctrl Pts',(3.37163980464479,-0.860627622326853,
28.6380481477102));
#97069=CARTESIAN_POINT('Ctrl Pts',(2.54671270073136,2.37126322800964,28.7971484151974));
#97070=CARTESIAN_POINT('Ctrl Pts',(-0.618178088909158,3.4243964033052,28.9562486826848));
#97071=CARTESIAN_POINT('Ctrl Pts',(-3.21507615642433,1.33113492365306,29.115348950172));
#97072=CARTESIAN_POINT('Ctrl Pts',(-2.85790663291539,-1.9851963515268,29.2744492176593));
#97073=CARTESIAN_POINT('Ctrl Pts',(0.125156944642189,-3.47749487645702,
29.4335494851466));
#97074=CARTESIAN_POINT('Ctrl Pts',(2.99322415633754,-1.77461095074231,29.5926497526339));
#97075=CARTESIAN_POINT('Ctrl Pts',(3.11106523256831,1.55881621600552,29.7517500201211));
#97076=CARTESIAN_POINT('Ctrl Pts',(0.370405753927932,3.45997607708985,29.9108502876084));
#97077=CARTESIAN_POINT('Ctrl Pts',(-2.71058893917414,2.1820500634504,30.0699505550957));
#97078=CARTESIAN_POINT('Ctrl Pts',(-3.30104762372702,-1.10078129638149,
30.2290508225829));
#97079=CARTESIAN_POINT('Ctrl Pts',(-0.858446645853591,-3.37219575837462,
30.3881510900703));
#97080=CARTESIAN_POINT('Ctrl Pts',(2.37290996073868,-2.54517842101576,30.5472513575575));
#97081=CARTESIAN_POINT('Ctrl Pts',(3.4239958457713,0.620392879325578,30.7063516250448));
#97082=CARTESIAN_POINT('Ctrl Pts',(1.32905511504771,3.21593646979268,30.8654518925321));
#97083=CARTESIAN_POINT('Ctrl Pts',(-1.9870444470778,2.85662199843003,31.0245521600194));
#97084=CARTESIAN_POINT('Ctrl Pts',(-3.4774131967907,-0.12740618259286,31.1836524275066));
#97085=CARTESIAN_POINT('Ctrl Pts',(-1.77267454454907,-2.99437135901425,
31.3427526949939));
#97086=CARTESIAN_POINT('Ctrl Pts',(1.56082814521689,-3.11005633030592,31.5018529624812));
#97087=CARTESIAN_POINT('Ctrl Pts',(3.46021493395502,-0.368167743578406,
31.6609532299685));
#97088=CARTESIAN_POINT('Ctrl Pts',(2.18029638214961,2.71199973498569,31.8200534974558));
#97089=CARTESIAN_POINT('Ctrl Pts',(-1.10291620313167,3.30033494140318,31.979153764943));
#97090=CARTESIAN_POINT('Ctrl Pts',(-3.37275030131974,0.856265310242433,
32.1382540324303));
#97091=CARTESIAN_POINT('Ctrl Pts',(-2.54364307650471,-2.37455570074209,
32.2973542999176));
#97092=CARTESIAN_POINT('Ctrl Pts',(0.622607410195718,-3.42359385578174,
32.4564545674049));
#97093=CARTESIAN_POINT('Ctrl Pts',(3.21679543774861,-1.3269747504217,32.6155548348921));
#97094=CARTESIAN_POINT('Ctrl Pts',(2.85533616885434,1.98889171133305,32.7746551023795));
#97095=CARTESIAN_POINT('Ctrl Pts',(-0.12965536724212,3.47733006232115,32.9337553698667));
#97096=CARTESIAN_POINT('Ctrl Pts',(-2.99551730897204,1.77073739674347,33.092855637354));
#97097=CARTESIAN_POINT('Ctrl Pts',(-3.10904612692694,-1.56283942144345,
33.2519559048413));
#97098=CARTESIAN_POINT('Ctrl Pts',(-0.36592957920303,-3.460452343212,33.4110561723285));
#97099=CARTESIAN_POINT('Ctrl Pts',(2.71340939621074,-2.17854178870462,33.5701564398158));
#97100=CARTESIAN_POINT('Ctrl Pts',(3.29962087835819,1.10505064846814,33.7292567073031));
#97101=CARTESIAN_POINT('Ctrl Pts',(0.8540836164059,3.37330343324819,33.8883569747904));
#97102=CARTESIAN_POINT('Ctrl Pts',(-2.37620044733142,2.54210666784049,34.0474572422777));
#97103=CARTESIAN_POINT('Ctrl Pts',(-3.42319043350467,-0.624821680593156,
34.2065575097649));
#97104=CARTESIAN_POINT('Ctrl Pts',(-1.3248938306453,-3.21765305993281,34.3656577772522));
#97105=CARTESIAN_POINT('Ctrl Pts',(1.9907381435198,-2.85404914472622,34.5247580447395));
#97106=CARTESIAN_POINT('Ctrl Pts',(3.47724547308312,0.131904497649062,34.6838583122268));
#97107=CARTESIAN_POINT('Ctrl Pts',(1.76879950813591,2.99666200573157,34.8429585797141));
#97108=CARTESIAN_POINT('Ctrl Pts',(-1.56485004384385,3.10803462285397,35.0020588472013));
#97109=CARTESIAN_POINT('Ctrl Pts',(-3.46068830476142,0.363691261738097,
35.1611591146886));
#97110=CARTESIAN_POINT('Ctrl Pts',(-2.17678628384951,-2.71481792225954,
35.3202593821759));
#97111=CARTESIAN_POINT('Ctrl Pts',(1.10718463149792,-3.29890543489078,35.4793596496632));
#97112=CARTESIAN_POINT('Ctrl Pts',(3.37385515392854,-0.851901565256779,
35.6384599171505));
#97113=CARTESIAN_POINT('Ctrl Pts',(2.54056919566589,2.37784419981852,35.7975601846377));
#97114=CARTESIAN_POINT('Ctrl Pts',(-0.627035689591476,3.42278557910887,
35.956660452125));
#97115=CARTESIAN_POINT('Ctrl Pts',(-3.21850933598648,1.32281235658916,36.1157607196123));
#97116=CARTESIAN_POINT('Ctrl Pts',(-2.85276092658412,-1.99258374286554,
36.2748609870995));
#97117=CARTESIAN_POINT('Ctrl Pts',(0.134153572872717,-3.47715942911201,
36.4339612545869));
#97118=CARTESIAN_POINT('Ctrl Pts',(2.99780544881391,-1.76686087953711,36.5930615220741));
#97119=CARTESIAN_POINT('Ctrl Pts',(3.10702181851019,1.56686001157689,36.7521617895614));
#97120=CARTESIAN_POINT('Ctrl Pts',(0.361452792120057,3.46092281850458,36.9112620570486));
#97121=CARTESIAN_POINT('Ctrl Pts',(-2.71622531254288,2.17502986831866,37.070362324536));
#97122=CARTESIAN_POINT('Ctrl Pts',(-3.29818861130025,-1.10931815132831,
37.2294625920232));
#97123=CARTESIAN_POINT('Ctrl Pts',(-0.849719157707888,-3.37440546312996,
37.3885628595105));
#97124=CARTESIAN_POINT('Ctrl Pts',(2.37948695751577,-2.53903066062412,37.5476631269978));
#97125=CARTESIAN_POINT('Ctrl Pts',(3.42237929276372,0.629249436264508,37.7067633944851));
#97126=CARTESIAN_POINT('Ctrl Pts',(1.32073032912399,3.21936426555138,37.8658636619724));
#97127=CARTESIAN_POINT('Ctrl Pts',(-1.99442850859811,2.85147151496698,38.0249639294596));
#97128=CARTESIAN_POINT('Ctrl Pts',(-3.47707193044383,-0.136402591972126,
38.1840641969469));
#97129=CARTESIAN_POINT('Ctrl Pts',(-1.76492151175815,-2.99894763774068,
38.3431644644342));
#97130=CARTESIAN_POINT('Ctrl Pts',(1.56886932380165,-3.10600771431932,38.5022647319215));
#97131=CARTESIAN_POINT('Ctrl Pts',(3.46115588434339,-0.359214171285433,
38.6613649994088));
#97132=CARTESIAN_POINT('Ctrl Pts',(2.17327254284694,2.71763156647193,38.820465266896));
#97133=CARTESIAN_POINT('Ctrl Pts',(-1.11145120706667,3.29747040788648,38.9795655343833));
#97134=CARTESIAN_POINT('Ctrl Pts',(-3.37495436062222,0.847536394672323,
39.1386658018706));
#97135=CARTESIAN_POINT('Ctrl Pts',(-2.53749106335888,-2.38112871973583,
39.2977660693578));
#97136=CARTESIAN_POINT('Ctrl Pts',(0.631462919686039,-3.4219715746392,39.4568663368451));
#97137=CARTESIAN_POINT('Ctrl Pts',(3.22021784826983,-1.31864774912091,39.6159666043324));
#97138=CARTESIAN_POINT('Ctrl Pts',(2.85018091041424,1.99627243994583,39.7750668718197));
#97139=CARTESIAN_POINT('Ctrl Pts',(-0.138651554006447,3.47698297711515,
39.934167139307));
#97140=CARTESIAN_POINT('Ctrl Pts',(-3.00008857203401,1.76298140561038,40.0932674067942));
#97141=CARTESIAN_POINT('Ctrl Pts',(-3.10499231070567,-1.57087797967749,
40.2523676742816));
#97142=CARTESIAN_POINT('Ctrl Pts',(-0.356975400170752,-3.46138750218032,
40.4114679417688));
#97143=CARTESIAN_POINT('Ctrl Pts',(2.71903668345837,-2.17151430816952,40.5705682092561));
#97144=CARTESIAN_POINT('Ctrl Pts',(3.29675082494996,1.11358379782068,40.7296684767434));
#97145=CARTESIAN_POINT('Ctrl Pts',(0.845353277063212,3.37550184617569,40.8887687442307));
#97146=CARTESIAN_POINT('Ctrl Pts',(-2.382769485792,2.53595040451421,41.0478690117179));
#97147=CARTESIAN_POINT('Ctrl Pts',(-3.42156242490587,-0.633676138930166,
41.2069692792052));
#97148=CARTESIAN_POINT('Ctrl Pts',(-1.31656461745104,-3.22107008378474,
41.3660695466925));
#97149=CARTESIAN_POINT('Ctrl Pts',(1.99811553613721,-2.84888911346582,41.5251698141798));
#97150=CARTESIAN_POINT('Ctrl Pts',(3.47689256916324,0.140900458034825,41.684270081667));
#97151=CARTESIAN_POINT('Ctrl Pts',(1.76104056190537,3.00122825121666,41.8433703491544));
#97152=CARTESIAN_POINT('Ctrl Pts',(-1.5728859783643,3.10397560809395,42.0024706166416));
#97153=CARTESIAN_POINT('Ctrl Pts',(-3.4616176719185,0.354736479712447,42.1615708841289));
#97154=CARTESIAN_POINT('Ctrl Pts',(-2.16975516502185,-2.72044066291438,
42.3206711516162));
#97155=CARTESIAN_POINT('Ctrl Pts',(1.11571592269813,-3.29602986279173,42.4797714191035));
#97156=CARTESIAN_POINT('Ctrl Pts',(3.37604791956135,-0.843169805793855,
42.6388716865907));
#97157=CARTESIAN_POINT('Ctrl Pts',(2.53440868473468,2.38440925499764,42.797971954078));
#97158=CARTESIAN_POINT('Ctrl Pts',(-0.635889093070747,3.42115184373492,
42.9570722215653));
#97159=CARTESIAN_POINT('Ctrl Pts',(-3.22192097173958,1.31448093498611,43.1161724890526));
#97160=CARTESIAN_POINT('Ctrl Pts',(-2.84759612466217,-1.99995779640121,
43.2752727565398));
#97161=CARTESIAN_POINT('Ctrl Pts',(0.143149303116361,-3.47680070662587,
43.4343730240271));
#97162=CARTESIAN_POINT('Ctrl Pts',(3.00236667481184,-1.75909898145519,43.5934732915144));
#97163=CARTESIAN_POINT('Ctrl Pts',(3.10295760690946,1.57489331902183,43.7525735590017));
#97164=CARTESIAN_POINT('Ctrl Pts',(0.352497410847578,3.46184639346149,43.911673826489));
#97165=CARTESIAN_POINT('Ctrl Pts',(-2.72184350425287,2.16799511414025,44.0707740939763));
#97166=CARTESIAN_POINT('Ctrl Pts',(-3.29530752171281,-1.1178475808074,44.2298743614635));
#97167=CARTESIAN_POINT('Ctrl Pts',(-0.840985981778881,-3.37659258055,44.3889746289508));
#97168=CARTESIAN_POINT('Ctrl Pts',(2.38604802666906,-2.53286590466669,44.548074896438));
#97169=CARTESIAN_POINT('Ctrl Pts',(3.42073983129402,0.638101781184889,44.7071751639254));
#97170=CARTESIAN_POINT('Ctrl Pts',(1.31239670260541,3.2227705117732,44.8662754314126));
#97171=CARTESIAN_POINT('Ctrl Pts',(-2.0017992199819,2.84630194455405,45.0253756988999));
#97172=CARTESIAN_POINT('Ctrl Pts',(-3.47670738951322,-0.145398088329049,
45.1844759663872));
#97173=CARTESIAN_POINT('Ctrl Pts',(-1.757156665126,-3.00350384230738,45.3435762338744));
#97174=CARTESIAN_POINT('Ctrl Pts',(1.57690000091316,-3.10193830764655,45.5026765013618));
#97175=CARTESIAN_POINT('Ctrl Pts',(3.46207366651742,-0.350258194382263,
45.661776768849));
#97176=CARTESIAN_POINT('Ctrl Pts',(2.16623415663537,2.72324520663779,45.8208770363364));
#97177=CARTESIAN_POINT('Ctrl Pts',(-1.11997877197074,3.29458380249072,45.9799773038235));
#97178=CARTESIAN_POINT('Ctrl Pts',(-3.37713582755165,0.838801805025182,
46.1390775713109));
#97179=CARTESIAN_POINT('Ctrl Pts',(-2.53132206755406,-2.38768579839091,
46.2981778387981));
#97180=CARTESIAN_POINT('Ctrl Pts',(0.640314207303564,-3.42032639105517,
46.4572781062854));
#97181=CARTESIAN_POINT('Ctrl Pts',(3.22361869407457,-1.31031191488652,46.6163783737727));
#97182=CARTESIAN_POINT('Ctrl Pts',(2.84500659172074,2.00363979410143,46.77547864126));
#97183=CARTESIAN_POINT('Ctrl Pts',(-0.147646847141617,3.47661264077023,
46.9345789087473));
#97184=CARTESIAN_POINT('Ctrl Pts',(-3.00463968758686,1.75521357003441,47.0936791762345));
#97185=CARTESIAN_POINT('Ctrl Pts',(-3.10091783594993,-1.57890593984303,
47.2527794437217));
#97186=CARTESIAN_POINT('Ctrl Pts',(-0.348018592382841,-3.46229965000353,
47.4118797112091));
#97187=CARTESIAN_POINT('Ctrl Pts',(2.72464531380624,-2.16447198990683,47.5709799786964));
#97188=CARTESIAN_POINT('Ctrl Pts',(3.29385957469109,1.1221089166414,47.7300802461837));
#97189=CARTESIAN_POINT('Ctrl Pts',(0.836615618213322,3.37767876419982,47.8891805136709));
#97190=CARTESIAN_POINT('Ctrl Pts',(-2.3893194061801,2.52977506828308,48.0482807811582));
#97191=CARTESIAN_POINT('Ctrl Pts',(-3.41991755759816,-0.642522353487716,
48.2073810486454));
#97192=CARTESIAN_POINT('Ctrl Pts',(-1.30821506127625,-3.22447318127091,
48.3664813161328));
#97193=CARTESIAN_POINT('Ctrl Pts',(2.0054575584248,-2.84369544855116,48.52558158362));
#97194=CARTESIAN_POINT('Ctrl Pts',(3.47655835125671,0.14986769250252,48.6846818511074));
#97195=CARTESIAN_POINT('Ctrl Pts',(1.75318978419848,3.00582740713737,48.8437821185946));
#97196=CARTESIAN_POINT('Ctrl Pts',(-1.58075868601436,3.09979470731945,49.0028823860818));
#97197=CARTESIAN_POINT('Ctrl Pts',(-3.46281520229328,0.345972243077007,
49.1619826535692));
#97198=CARTESIAN_POINT('Ctrl Pts',(-2.16215339527527,-2.72641357726118,
49.3210829210564));
#97199=CARTESIAN_POINT('Ctrl Pts',(1.12317562685709,-3.29242630007822,49.4801831885437));
#97200=CARTESIAN_POINT('Ctrl Pts',(3.38027638470318,-0.83580699739451,49.639283456031));
#97201=CARTESIAN_POINT('Ctrl Pts',(2.52405647169005,2.39382388417745,49.7983837235182));
#97202=CARTESIAN_POINT('Ctrl Pts',(0.418252623626215,3.0726983587025,49.9044505685098));
#97203=CARTESIAN_POINT('Ctrl Pts',(-0.545102916881406,2.89105980740755,
49.9574839910056));
#97204=CARTESIAN_POINT('Ctrl Pts',(-2.943409633743,-0.00255526730400832,
48.1778238829104));
#97205=CARTESIAN_POINT('Ctrl Pts',(-2.94507379928574,-0.184399871474338,
48.1876762714888));
#97206=CARTESIAN_POINT('Ctrl Pts',(-2.92967483134683,-0.36596345305782,
48.1975286600671));
#97207=CARTESIAN_POINT('Ctrl Pts',(-2.89620078297484,-0.544131254489774,
48.2073810486455));
#97208=CARTESIAN_POINT('Ctrl Pts',(-2.71601672549087,-1.50317262941543,
48.2604144711412));
#97209=CARTESIAN_POINT('Ctrl Pts',(-2.01211589338358,-2.36382290534315,
48.313447893637));
#97210=CARTESIAN_POINT('Ctrl Pts',(-1.10788670737978,-2.73068508785373,
48.3664813161328));
#97211=CARTESIAN_POINT('Ctrl Pts',(-0.203657521375925,-3.09754727036433,
48.4195147386285));
#97212=CARTESIAN_POINT('Ctrl Pts',(0.900900018524468,-2.97062135945774,
48.4725481611243));
#97213=CARTESIAN_POINT('Ctrl Pts',(1.69836225394665,-2.4082312138288,48.52558158362));
#97214=CARTESIAN_POINT('Ctrl Pts',(2.49582448936878,-1.8458410681999,48.5786150061158));
#97215=CARTESIAN_POINT('Ctrl Pts',(2.98619142031275,-0.847986687848688,
48.6316484286116));
#97216=CARTESIAN_POINT('Ctrl Pts',(2.94414679127502,0.126933788099391,48.6846818511073));
#97217=CARTESIAN_POINT('Ctrl Pts',(2.9021021622373,1.10185426404747,48.7377152736031));
#97218=CARTESIAN_POINT('Ctrl Pts',(2.32764597321789,2.05384083559242,48.7907486960988));
#97219=CARTESIAN_POINT('Ctrl Pts',(1.48475980033937,2.54549533806191,48.8437821185946));
#97220=CARTESIAN_POINT('Ctrl Pts',(0.641873627460864,3.0371498405314,48.8968155410903));
#97221=CARTESIAN_POINT('Ctrl Pts',(-0.469442529276749,3.06847227392542,
48.9498489635861));
#97222=CARTESIAN_POINT('Ctrl Pts',(-1.33877669369204,2.62516307991536,49.0028823860819));
#97223=CARTESIAN_POINT('Ctrl Pts',(-1.63994290539553,2.47158605966431,49.0212549240546));
#97224=CARTESIAN_POINT('Ctrl Pts',(-1.91206741640369,2.26104566981987,49.0396274620273));
#97225=CARTESIAN_POINT('Ctrl Pts',(-2.1431563177438,2.01106840053142,49.0580000000001));
#97226=CARTESIAN_POINT('Ctrl Pts',(-1.3800144223764,-1.93381244560185,-1.49186218934005E-16));
#97227=CARTESIAN_POINT('Ctrl Pts',(-1.42855884494822,-1.90739843349394,
-1.70198841695918E-16));
#97228=CARTESIAN_POINT('Ctrl Pts',(-1.47602780810136,-1.87922026048844,
-6.28080395559761E-17));
#97229=CARTESIAN_POINT('Ctrl Pts',(-1.52231351314505,-1.84929882574418,
-5.72458747072346E-17));
#97230=CARTESIAN_POINT('Ctrl Pts',(-1.59072873207763,-1.80507174727851,
-2.99424423574721E-17));
#97231=CARTESIAN_POINT('Ctrl Pts',(-1.65656007365294,-1.7570385764509,1.23091517206865E-16));
#97232=CARTESIAN_POINT('Ctrl Pts',(-1.7197220395774,-1.70555950061155,9.0205620750794E-17));
#97233=CARTESIAN_POINT('Ctrl Pts',(-1.75666514687009,-1.67544965532371,
7.09708299489081E-17));
#97234=CARTESIAN_POINT('Ctrl Pts',(-1.79269476886278,-1.64415997886869,
-2.72191750387666E-16));
#97235=CARTESIAN_POINT('Ctrl Pts',(-1.82779071816502,-1.6117550919015,-2.98372437868011E-16));
#97236=CARTESIAN_POINT('Ctrl Pts',(-1.84338700953533,-1.59735468191086,
-3.10006875412424E-16));
#97237=CARTESIAN_POINT('Ctrl Pts',(-1.85879888268092,-1.58273396999838,
2.67280072439625E-17));
#97238=CARTESIAN_POINT('Ctrl Pts',(-1.87402439060531,-1.5678983186799,4.85722573273506E-17));
#97239=CARTESIAN_POINT('Ctrl Pts',(-1.88610726792344,-1.55612482936802,
6.59077311371403E-17));
#97240=CARTESIAN_POINT('Ctrl Pts',(-1.89807318870411,-1.54421540327689,
-6.57475537402881E-16));
#97241=CARTESIAN_POINT('Ctrl Pts',(-1.9099098864946,-1.53218449300995,-6.24500451351651E-16));
#97242=CARTESIAN_POINT('Ctrl Pts',(-1.96985570454349,-1.47125510454453,
-4.57501298077507E-16));
#97243=CARTESIAN_POINT('Ctrl Pts',(-2.02656004093552,-1.40714582547612,
-1.46167834437222E-16));
#97244=CARTESIAN_POINT('Ctrl Pts',(-2.07992731810956,-1.34024875153828,
-5.55111512312578E-17));
#97245=CARTESIAN_POINT('Ctrl Pts',(-2.12630479673919,-1.28211354619851,
2.3271739908326E-17));
#97246=CARTESIAN_POINT('Ctrl Pts',(-2.17016203790517,-1.22187184995567,
-9.84142147220768E-17));
#97247=CARTESIAN_POINT('Ctrl Pts',(-2.21142070906362,-1.15975295612777,
-6.93889390390723E-17));
#97248=CARTESIAN_POINT('Ctrl Pts',(-2.23103383926374,-1.13022350405562,
-5.55911967686331E-17));
#97249=CARTESIAN_POINT('Ctrl Pts',(-2.25005951597988,-1.10026950536354,
4.3764560536828E-17));
#97250=CARTESIAN_POINT('Ctrl Pts',(-2.26848790511312,-1.06991389685038,
6.93889390390723E-17));
#97251=CARTESIAN_POINT('Ctrl Pts',(-2.27568158581329,-1.05806432315601,
7.93916362771505E-17));
#97252=CARTESIAN_POINT('Ctrl Pts',(-2.28278479302695,-1.04615259821836,
-6.14134180165296E-16));
#97253=CARTESIAN_POINT('Ctrl Pts',(-2.28979518299867,-1.03418298191949,
-5.96744875736022E-16));
#97254=CARTESIAN_POINT('Ctrl Pts',(-2.33451667273546,-0.957825022572966,
-4.85813015639582E-16));
#97255=CARTESIAN_POINT('Ctrl Pts',(-2.37532290647229,-0.879355576208141,
3.37797804077662E-17));
#97256=CARTESIAN_POINT('Ctrl Pts',(-2.41211780815156,-0.79917323765487,
4.16333634234434E-17));
#97257=CARTESIAN_POINT('Ctrl Pts',(-2.44958736980381,-0.717520700462878,
4.96309473159603E-17));
#97258=CARTESIAN_POINT('Ctrl Pts',(-2.48289779686268,-0.634091186714558,
-9.2208182772125E-17));
#97259=CARTESIAN_POINT('Ctrl Pts',(-2.51191518147983,-0.549262804099503,
2.77555756156289E-17));
#97260=CARTESIAN_POINT('Ctrl Pts',(-2.54089888650409,-0.464532879199711,
1.47580095729576E-16));
#97261=CARTESIAN_POINT('Ctrl Pts',(-2.5656000783497,-0.378406464546764,
1.91681516741294E-16));
#97262=CARTESIAN_POINT('Ctrl Pts',(-2.58584421344203,-0.29123000762658,
2.77555756156289E-16));
#97263=CARTESIAN_POINT('Ctrl Pts',(-2.59738512851483,-0.241531856479369,
3.26511530236505E-16));
#97264=CARTESIAN_POINT('Ctrl Pts',(-2.60747670761929,-0.191491957172924,
-3.4674691487661E-16));
#97265=CARTESIAN_POINT('Ctrl Pts',(-2.6160795223077,-0.141171741385976,
-4.44089209850063E-16));
#97266=CARTESIAN_POINT('Ctrl Pts',(-2.61852700899685,-0.126855722409087,
-4.71782933342707E-16));
#97267=CARTESIAN_POINT('Ctrl Pts',(-2.62085423679858,-0.112515203783535,
-1.06649609279466E-16));
#97268=CARTESIAN_POINT('Ctrl Pts',(-2.62305934562411,-0.0981572642000985,
-1.11022302462516E-16));
#97269=CARTESIAN_POINT('Ctrl Pts',(-2.63712528078298,-0.00657092394452452,
-1.38914811925222E-16));
#97270=CARTESIAN_POINT('Ctrl Pts',(-2.64617739573217,0.0853990681092962,
3.71900126169414E-17));
#97271=CARTESIAN_POINT('Ctrl Pts',(-2.65008474750347,0.177354999775061,
0.));
#97272=CARTESIAN_POINT('Ctrl Pts',(-2.65202414172285,0.222996859722445,
-1.84590739994191E-17));
#97273=CARTESIAN_POINT('Ctrl Pts',(-2.65269545055373,0.268635769706036,
-6.63948877319936E-16));
#97274=CARTESIAN_POINT('Ctrl Pts',(-2.65207858378913,0.314225566990061,
-6.10622663543836E-16));
#97275=CARTESIAN_POINT('Ctrl Pts',(-2.65087965130116,0.402833175991634,
-5.06978677799186E-16));
#97276=CARTESIAN_POINT('Ctrl Pts',(-2.6448180687798,0.491254842453244,-1.68823756050878E-16));
#97277=CARTESIAN_POINT('Ctrl Pts',(-2.63413908118019,0.57922885720872,-1.11022302462516E-16));
#97278=CARTESIAN_POINT('Ctrl Pts',(-2.62324360658611,0.668986302263057,
-5.20490839622738E-17));
#97279=CARTESIAN_POINT('Ctrl Pts',(-2.60754152358555,0.758278489974549,
-4.16879648018951E-17));
#97280=CARTESIAN_POINT('Ctrl Pts',(-2.58723933329292,0.846831256180718,
0.));
#97281=CARTESIAN_POINT('Ctrl Pts',(-2.58290125787064,0.865752789922496,
8.90768596419273E-18));
#97282=CARTESIAN_POINT('Ctrl Pts',(-2.57835296575468,0.884640553812132,
2.73591279314061E-16));
#97283=CARTESIAN_POINT('Ctrl Pts',(-2.57359616799277,0.903491843796352,
3.05311331771918E-16));
#97284=CARTESIAN_POINT('Ctrl Pts',(-2.56983477539876,0.91839832207933,3.30393661601536E-16));
#97285=CARTESIAN_POINT('Ctrl Pts',(-2.56594255180041,0.933283371413798,
-3.67694354189373E-16));
#97286=CARTESIAN_POINT('Ctrl Pts',(-2.56192538081525,0.948127790528015,
-3.60822483003176E-16));
#97287=CARTESIAN_POINT('Ctrl Pts',(-2.53775413356268,1.0374463995828,-3.19474554786378E-16));
#97288=CARTESIAN_POINT('Ctrl Pts',(-2.50902828076505,1.12543873737851,1.53403928884733E-16));
#97289=CARTESIAN_POINT('Ctrl Pts',(-2.47603795129406,1.21182189566662,1.11022302462516E-16));
#97290=CARTESIAN_POINT('Ctrl Pts',(-2.44240452892675,1.29988895333818,6.78145150615047E-17));
#97291=CARTESIAN_POINT('Ctrl Pts',(-2.40433858917601,1.38628426565922,-5.02419088652809E-16));
#97292=CARTESIAN_POINT('Ctrl Pts',(-2.36209206550289,1.47071144652719,-5.55111512312578E-16));
#97293=CARTESIAN_POINT('Ctrl Pts',(-2.31947143010013,1.55588626757751,-6.08270550785587E-16));
#97294=CARTESIAN_POINT('Ctrl Pts',(-2.27259555516532,1.63905881902964,-3.99435617532735E-16));
#97295=CARTESIAN_POINT('Ctrl Pts',(-2.2216707389484,1.71991558864889,-4.44089209850063E-16));
#97296=CARTESIAN_POINT('Ctrl Pts',(-2.19223846647794,1.76664719518778,-4.69896994610052E-16));
#97297=CARTESIAN_POINT('Ctrl Pts',(-2.16145276924779,1.81260501793967,-5.62079449352428E-16));
#97298=CARTESIAN_POINT('Ctrl Pts',(-2.12934619443225,1.8577253685959,-6.10622663543836E-16));
#97299=CARTESIAN_POINT('Ctrl Pts',(-2.1208366219097,1.8696841308855,-6.23488626481735E-16));
#97300=CARTESIAN_POINT('Ctrl Pts',(-2.11223277684254,1.88158602620125,-3.37626995517435E-16));
#97301=CARTESIAN_POINT('Ctrl Pts',(-2.10353995800366,1.89342337724526,-3.33066907387547E-16));
#97302=CARTESIAN_POINT('Ctrl Pts',(-2.04535171670342,1.97266057885621,-3.02542458026509E-16));
#97303=CARTESIAN_POINT('Ctrl Pts',(-1.98333354102214,2.04880176073276,2.26492193510099E-16));
#97304=CARTESIAN_POINT('Ctrl Pts',(-1.91775995208173,2.12153850276279,1.66533453693773E-16));
#97305=CARTESIAN_POINT('Ctrl Pts',(-1.85197384149148,2.1945109819649,1.06380389752237E-16));
#97306=CARTESIAN_POINT('Ctrl Pts',(-1.78260884177838,2.26405782067553,-1.44367353459688E-16));
#97307=CARTESIAN_POINT('Ctrl Pts',(-1.70989166532765,2.32985284092625,0.));
#97308=CARTESIAN_POINT('Ctrl Pts',(-1.63853532905585,2.39441656327046,1.416656410899E-16));
#97309=CARTESIAN_POINT('Ctrl Pts',(-1.5639505801766,2.4553683545156,-2.41362646891836E-16));
#97310=CARTESIAN_POINT('Ctrl Pts',(-1.48631019665298,2.51237350747524,-2.22044604925031E-16));
#97311=CARTESIAN_POINT('Ctrl Pts',(-1.42254976981509,2.5591877131722,-2.06180095431707E-16));
#97312=CARTESIAN_POINT('Ctrl Pts',(-1.35672772912532,2.60333998688217,-1.8151660154858E-16));
#97313=CARTESIAN_POINT('Ctrl Pts',(-1.28892185405323,2.64462557919718,-1.66533453693773E-16));
#97314=CARTESIAN_POINT('Origin',(0.,0.,0.));
#97315=CARTESIAN_POINT('Origin',(-1.44337567297407,-2.5,-6.));
#97316=CARTESIAN_POINT('',(-1.44337567297407,-2.5,-6.));
#97317=CARTESIAN_POINT('',(1.44337567297406,-2.5,-6.));
#97318=CARTESIAN_POINT('',(-0.721687836487033,-2.5,-6.));
#97319=CARTESIAN_POINT('',(-1.44337567297407,-2.5,-3.));
#97320=CARTESIAN_POINT('',(-1.44337567297407,-2.5,-6.));
#97321=CARTESIAN_POINT('',(1.44337567297406,-2.5,-3.));
#97322=CARTESIAN_POINT('',(-1.44337567297407,-2.5,-3.));
#97323=CARTESIAN_POINT('',(1.44337567297406,-2.5,-6.));
#97324=CARTESIAN_POINT('Origin',(-2.88675134594813,3.53525079574969E-16,
-6.));
#97325=CARTESIAN_POINT('',(-2.88675134594813,3.53525079574969E-16,-6.));
#97326=CARTESIAN_POINT('',(-2.52590742770461,-0.625,-6.));
#97327=CARTESIAN_POINT('',(-2.88675134594813,5.55111512312578E-16,-3.));
#97328=CARTESIAN_POINT('',(-2.88675134594813,3.53525079574969E-16,-6.));
#97329=CARTESIAN_POINT('',(-2.88675134594813,3.53525079574969E-16,-3.));
#97330=CARTESIAN_POINT('Origin',(-1.44337567297406,2.5,-6.));
#97331=CARTESIAN_POINT('',(-1.44337567297406,2.5,-6.));
#97332=CARTESIAN_POINT('',(-1.80421959121758,1.875,-6.));
#97333=CARTESIAN_POINT('',(-1.44337567297406,2.5,-3.));
#97334=CARTESIAN_POINT('',(-1.44337567297406,2.5,-6.));
#97335=CARTESIAN_POINT('',(-1.44337567297406,2.5,-3.));
#97336=CARTESIAN_POINT('Origin',(1.44337567297406,2.5,-6.));
#97337=CARTESIAN_POINT('',(1.44337567297406,2.5,-6.));
#97338=CARTESIAN_POINT('',(0.721687836487033,2.5,-6.));
#97339=CARTESIAN_POINT('',(1.44337567297406,2.5,-3.));
#97340=CARTESIAN_POINT('',(1.44337567297406,2.5,-6.));
#97341=CARTESIAN_POINT('',(1.44337567297406,2.5,-3.));
#97342=CARTESIAN_POINT('Origin',(2.88675134594813,0.,-6.));
#97343=CARTESIAN_POINT('',(2.88675134594813,0.,-6.));
#97344=CARTESIAN_POINT('',(2.52590742770461,0.625,-6.));
#97345=CARTESIAN_POINT('',(2.88675134594813,0.,-3.));
#97346=CARTESIAN_POINT('',(2.88675134594813,0.,-6.));
#97347=CARTESIAN_POINT('',(2.88675134594813,0.,-3.));
#97348=CARTESIAN_POINT('Origin',(1.44337567297406,-2.5,-6.));
#97349=CARTESIAN_POINT('',(1.80421959121758,-1.875,-6.));
#97350=CARTESIAN_POINT('',(1.44337567297406,-2.5,-3.));
#97351=CARTESIAN_POINT('Origin',(0.,0.,-3.));
#97352=CARTESIAN_POINT('Origin',(0.,0.,0.));
#97353=CARTESIAN_POINT('',(-5.,-6.12323399573677E-16,0.));
#97354=CARTESIAN_POINT('Origin',(0.,0.,0.));
#97355=CARTESIAN_POINT('Origin',(0.,0.,-6.));
#97356=CARTESIAN_POINT('',(-5.,-6.12323399573677E-16,-6.));
#97357=CARTESIAN_POINT('',(-5.,-6.12323399573677E-16,-6.));
#97358=CARTESIAN_POINT('Origin',(0.,0.,-6.));
#97359=CARTESIAN_POINT('Origin',(0.,0.,-6.));
#97360=CARTESIAN_POINT('Origin',(0.,0.,50.));
#97449=UNCERTAINTY_MEASURE_WITH_UNIT(LENGTH_MEASURE(0.01),#97476,
'DISTANCE_ACCURACY_VALUE',
'Maximum model space distance between geometric entities at asserted c
onnectivities');
#97452=UNCERTAINTY_MEASURE_WITH_UNIT(LENGTH_MEASURE(0.01),#97476,
'DISTANCE_ACCURACY_VALUE',
'Maximum model space distance between geometric entities at asserted c
onnectivities');
#97472=(
GEOMETRIC_REPRESENTATION_CONTEXT(3)
GLOBAL_UNCERTAINTY_ASSIGNED_CONTEXT((#97449))
GLOBAL_UNIT_ASSIGNED_CONTEXT((#97476,#97478,#97479))
REPRESENTATION_CONTEXT('','3D')
);
#97475=(
GEOMETRIC_REPRESENTATION_CONTEXT(3)
GLOBAL_UNCERTAINTY_ASSIGNED_CONTEXT((#97452))
GLOBAL_UNIT_ASSIGNED_CONTEXT((#97476,#97478,#97479))
REPRESENTATION_CONTEXT('','3D')
);
#97476=(
LENGTH_UNIT()
NAMED_UNIT(*)
SI_UNIT(.MILLI.,.METRE.)
);
#97478=(
NAMED_UNIT(*)
PLANE_ANGLE_UNIT()
SI_UNIT($,.RADIAN.)
);
#97479=(
NAMED_UNIT(*)
SI_UNIT($,.STERADIAN.)
SOLID_ANGLE_UNIT()
);
#97499=SHAPE_DEFINITION_REPRESENTATION(#97561,#97622);
#97561=PRODUCT_DEFINITION_SHAPE('',$,#97645);
#97622=SHAPE_REPRESENTATION('',(#23325),#97472);
#97625=PRODUCT_DEFINITION_CONTEXT('part definition',#97693,'design');
#97645=PRODUCT_DEFINITION('Socket head cap screw M6x50',
'Socket head cap screw M6x50',#97667,#97625);
#97667=PRODUCT_DEFINITION_FORMATION('',$,#97714);
#97693=APPLICATION_CONTEXT(
'Core Data for Automotive Mechanical Design Process');
#97694=PRODUCT_CONTEXT('part definition',#97693,'mechanical');
#97714=PRODUCT('Socket head cap screw M6x50',
'Socket head cap screw M6x50',$,(#97694));
#97720=PRESENTATION_STYLE_ASSIGNMENT((#97727));
#97727=SURFACE_STYLE_USAGE(.BOTH.,#97734);
#97734=SURFACE_SIDE_STYLE('',(#97741));
#97741=SURFACE_STYLE_FILL_AREA(#97748);
#97748=FILL_AREA_STYLE('Dark gray',(#97755));
#97755=FILL_AREA_STYLE_COLOUR('Dark gray',#97762);
#97762=COLOUR_RGB('Dark gray',0.250980392156863,0.282352941176471,0.32156862745098);
ENDSEC;
END-ISO-10303-21;
